ISO-10303-21;
HEADER;
FILE_DESCRIPTION (('STEP AP214'),
    '1' );
FILE_NAME ('screw coil.step',
    '2026-10-05T20:10:51',
    ( '' ),
    ( '' ),
    'SwSTEP 2.0',
    'SolidWorks 2020',
    '' );
FILE_SCHEMA (( 'AUTOMOTIVE_DESIGN' ));
ENDSEC;

DATA;
#51=CARTESIAN_POINT ( 'NONE',  ( -1.626862140677534470E-15, 1.125000000682806034, 1.224999999999975886 ) ) ;
#58=PRESENTATION_STYLE_ASSIGNMENT (( #85603 ) ) ;
#60=CARTESIAN_POINT ( 'NONE',  ( 1.360316468749959373, -0.4531249996586189654, -4.163336342344337027E-14 ) ) ;
#97=CARTESIAN_POINT ( 'NONE',  ( 0.6801582343749935644, 0.9739583336747514863, 1.178068619123805227 ) ) ;
#123=CARTESIAN_POINT ( 'NONE',  ( -1.772826578343124959, 3.950000000000009059, -0.4500000000000423661 ) ) ;
#161=CARTESIAN_POINT ( 'NONE',  ( 1.224999999999948797, 0.4583333340161501734, -0.7072540797573277915 ) ) ;
#225=ORIENTED_EDGE ( 'NONE', *, *, #185632, .T. ) ;
#239=STYLED_ITEM ( 'NONE', ( #58 ), #85152 ) ;
#240=EDGE_CURVE ( 'NONE', #112800, #149263, #151353, .T. ) ;
#272=CARTESIAN_POINT ( 'NONE',  ( -0.3000000000000346279, 3.999999999999980904, -1.007084189318430356 ) ) ;
#344=CARTESIAN_POINT ( 'NONE',  ( -0.3817069231125022055, 3.999999999999974243, 1.007084182327149913 ) ) ;
#351=CARTESIAN_POINT ( 'NONE',  ( 1.360316468749973584, 2.786458333674735499, -0.7853790794159101196 ) ) ;
#383=CARTESIAN_POINT ( 'NONE',  ( -0.6125000000000089262, 1.041666666666662966, 1.060881119635898040 ) ) ;
#470=( BOUNDED_CURVE ( )  B_SPLINE_CURVE ( 3, ( #109998, #93702, #77422, #159743 ),
 .UNSPECIFIED., .F., .T. ) 
 B_SPLINE_CURVE_WITH_KNOTS ( ( 4, 4 ),
 ( 0.000000000000000000, 1.570796326794826836 ),
 .UNSPECIFIED. ) 
 CURVE ( )  GEOMETRIC_REPRESENTATION_ITEM ( )  RATIONAL_B_SPLINE_CURVE ( ( 1.000000000000000000, 0.8047378541243814798, 0.8047378541243814798, 1.000000000000000000 ) ) 
 REPRESENTATION_ITEM ( '' )  );
#637=CARTESIAN_POINT ( 'NONE',  ( -0.3978093821460775281, 3.011896635411767775, -0.3978093821461013424 ) ) ;
#654=( BOUNDED_CURVE ( )  B_SPLINE_CURVE ( 2, ( #165198, #117577, #152154, #180388, #116506, #83937, #35178, #199813, #213916 ),
 .UNSPECIFIED., .F., .T. ) 
 B_SPLINE_CURVE_WITH_KNOTS ( ( 3, 2, 2, 2, 3 ),
 ( 0.5468749999999997780, 0.5520833333333333703, 0.5625000000000000000, 0.5729166666666666297, 0.5781250000000001110 ),
 .UNSPECIFIED. ) 
 CURVE ( )  GEOMETRIC_REPRESENTATION_ITEM ( )  RATIONAL_B_SPLINE_CURVE ( ( 0.9330127018922194093, 0.9330127018922165227, 1.000000000000000000, 0.8660254037844387076, 1.000000000000000000, 0.8660254037844387076, 1.000000000000000000, 0.9330127018922178550, 0.9330127018922192983 ) ) 
 REPRESENTATION_ITEM ( '' )  );
#687=VECTOR ( 'NONE', #83277, 1000.000000000000000 ) ;
#694=DIRECTION ( 'NONE',  ( -1.276756478318932191E-15, 1.000000000000000000, -3.330669073875483426E-16 ) ) ;
#768=CARTESIAN_POINT ( 'NONE',  ( 0.6801582343749952297, 2.088541667008066316, -1.178068619123855409 ) ) ;
#819=CARTESIAN_POINT ( 'NONE',  ( 1.743066579297358008E-15, 0.7500000006828128063, -1.225000000000021849 ) ) ;
#850=DIRECTION ( 'NONE',  ( -2.103352214621884660E-13, 0.000000000000000000, 1.000000000000000000 ) ) ;
#892=CARTESIAN_POINT ( 'NONE',  ( -0.3000000000000117573, 3.322650755865466543, -0.5865692111442739609 ) ) ;
#901=CARTESIAN_POINT ( 'NONE',  ( 1.360316468750001784, -0.7552083329919376808, 0.7853790794158941324 ) ) ;
#907=B_SPLINE_CURVE_WITH_KNOTS ( 'NONE', 3,
 ( #57698, #90211, #123855, #54496 ),
 .UNSPECIFIED., .F., .F.,
 ( 4, 4 ),
 ( 0.000000000000000000, 2.032232339064896589E-05 ),
 .UNSPECIFIED. ) ;
#925=CARTESIAN_POINT ( 'NONE',  ( 1.360316468749992236, 2.015625000341400685, -1.040834085586084257E-14 ) ) ;
#1095=CARTESIAN_POINT ( 'NONE',  ( -1.975475456537005874E-15, 2.812500000000000888, 1.224999999999953904 ) ) ;
#1173=CARTESIAN_POINT ( 'NONE',  ( 0.6801582343749831283, 1.223958333674737720, 1.178068619123822547 ) ) ;
#1182=CARTESIAN_POINT ( 'NONE',  ( -0.6125000000000383471, 1.854166667349464781, 1.060881119635894487 ) ) ;
#1238=EDGE_CURVE ( 'NONE', #81519, #74569, #198321, .T. ) ;
#1314=DIRECTION ( 'NONE',  ( -5.421010862427534989E-16, 0.5005768354468326242, 0.8656921114426506803 ) ) ;
#1318=AXIS2_PLACEMENT_3D ( 'NONE', #155804, #120166, #185069 ) ;
#1330=EDGE_LOOP ( 'NONE', ( #91029, #12999, #122001, #37714, #25958, #53087 ) ) ;
#1342=DIRECTION ( 'NONE',  ( -3.330669073875479482E-16, 3.330669073875479482E-16, 1.000000000000000000 ) ) ;
#1347=CARTESIAN_POINT ( 'NONE',  ( -0.3000000000000289102, 3.999999999999980904, -0.9782388782689288576 ) ) ;
#1371=ORIENTED_EDGE ( 'NONE', *, *, #22519, .F. ) ;
#1376=CARTESIAN_POINT ( 'NONE',  ( -0.3282377607281257714, 2.761164550367435133, -1.225000000000007638 ) ) ;
#1383=CARTESIAN_POINT ( 'NONE',  ( 2.672702088255949078E-15, 1.937500000000013323, -1.225000000000018074 ) ) ;
#1428=CARTESIAN_POINT ( 'NONE',  ( -3.755786496842897795E-14, 1.453125000341440876, 1.570758158831776052 ) ) ;
#1473=FACE_OUTER_BOUND ( 'NONE', #175970, .T. ) ;
#1654=ORIENTED_EDGE ( 'NONE', *, *, #41993, .T. ) ;
#1680=CARTESIAN_POINT ( 'NONE',  ( -2.754243431018125239E-14, 1.984375000341467299, 1.570758158831788265 ) ) ;
#1703=CARTESIAN_POINT ( 'NONE',  ( 1.224999999999959233, 0.8541666666667160346, 0.7072540797572558491 ) ) ;
#1750=CARTESIAN_POINT ( 'NONE',  ( 1.082249783303695034, -6.507923190189534549E-15, 0.8432277037082082094 ) ) ;
#1804=ORIENTED_EDGE ( 'NONE', *, *, #177588, .F. ) ;
#1847=CARTESIAN_POINT ( 'NONE',  ( -5.558564015327488080E-14, 0.6093750003414449834, -1.570758158831798257 ) ) ;
#1914=AXIS2_PLACEMENT_3D ( 'NONE', #35016, #51290, #50222 ) ;
#1916=ORIENTED_EDGE ( 'NONE', *, *, #31157, .F. ) ;
#1970=CARTESIAN_POINT ( 'NONE',  ( 0.6801582343749952297, -0.1927083329918907739, -1.178068619123876282 ) ) ;
#1993=CARTESIAN_POINT ( 'NONE',  ( 1.360316468749985575, 2.036458333674739940, -0.7853790794159022370 ) ) ;
#2064=CARTESIAN_POINT ( 'NONE',  ( 0.6125000000000019318, 2.666666666666678509, -1.060881119635941339 ) ) ;
#2078=CARTESIAN_POINT ( 'NONE',  ( -1.899436509991837552, 3.291494839451070131, -0.4074537448170277854 ) ) ;
#2114=CARTESIAN_POINT ( 'NONE',  ( -0.4500000000000389244, 3.999999999999948042, 0.4999999999999779066 ) ) ;
#2144=ORIENTED_EDGE ( 'NONE', *, *, #54770, .T. ) ;
#2170=CARTESIAN_POINT ( 'NONE',  ( 0.6124999999999932720, 1.666666666666712038, -1.060881119635983083 ) ) ;
#2174=EDGE_CURVE ( 'NONE', #22696, #43310, #35303, .T. ) ;
#2191=CARTESIAN_POINT ( 'NONE',  ( -3.355169270512988773E-14, -0.6406249996585449136, -1.570758158831794260 ) ) ;
#2232=CARTESIAN_POINT ( 'NONE',  ( -0.6801582343750299797, 0.9322916670080338974, 1.178068619123803451 ) ) ;
#2245=B_SPLINE_CURVE_WITH_KNOTS ( 'NONE', 3,
 ( #47719, #113835, #179833, #97531, #32504, #164640, #184071, #102839, #103912, #101766, #186200, #7444, #23703, #122383, #54089, #37835, #169957, #185128, #204571, #168895, #20498, #134303 ),
 .UNSPECIFIED., .F., .F.,
 ( 4, 3, 3, 3, 3, 3, 3, 4 ),
 ( 0.000000000000000000, 1.209865308640946775E-05, 2.418763075658931773E-05, 3.626888754244386227E-05, 5.481069466193077340E-05, 8.058589917397381919E-05, 0.0001081451638904062126, 0.0001095998438940776838 ),
 .UNSPECIFIED. ) ;
#2299=DIRECTION ( 'NONE',  ( 3.330669073875478989E-16, -4.632576442341012461E-16, -1.000000000000000000 ) ) ;
#2408=( BOUNDED_SURFACE ( )  B_SPLINE_SURFACE ( 1, 2, ( 
 ( #177587, #146173, #93153, #94221, #147230, #194889, #145118, #142985, #193814, #211124, #62748, #64885, #30268, #112648, #76866, #178657, #212188, #63825, #208985, #114774, #86479, #182902, #117976, #200203, #85407, #82198, #35580, #168790, #167728, #151492, #202331, #32399, #50775, #164529, #68057, #101660, #150428, #149346, #185023, #70197, #180771, #1993, #925, #199130, #49709, #183969, #83260, #17185, #19329, #134194, #136310, #165593, #66993, #18256, #3061, #69131, #51856, #132071, #201266, #115838, #133131, #135253, #116903, #52907, #98465, #119040, #36649, #102734, #20395, #152543, #34518, #4129, #16115, #181824, #148292, #33456, #214290, #99533, #100591, #166666, #84340, #65924, #198082, #24662, #74503, #188233, #57183, #189310, #205545, #39873, #90769, #103807, #203397, #40949, #187169, #153620, #55050, #105982, #6269, #172005, #156830, #123345, #8417, #140607, #23595, #206619, #138446, #9494, #58247, #5192, #7339, #104879, #121200, #124404, #122275, #190362, #89704, #107055, #75566, #155754, #141675, #42024, #170922, #25732, #108133, #174160, #137381, #173081, #53982, #91842, #73416, #157900, #169856, #120118, #21444, #87552, #22518, #186098, #139519, #37728, #71267, #38798, #88629, #154685, #72340, #204464, #56118, #143810, #194637, #163223, #208742, #79818, #161083, #177335, #175218, #192493, #60369, #28949, #129733, #62504, #142733, #125464, #126532, #76620, #210879, #44145, #207687, #179472, #61442, #128669, #78749, #178407, #26802, #46279, #47352, #112395, #30018, #80896, #191426, #209807, #43092, #12673, #96103, #95033, #27877, #63577, #14805, #59307, #144872, #93973, #77689, #110266, #162158 ),
 ( #13745, #11615, #176275, #145930, #127609, #45217, #211942, #109205, #158951, #193574, #195717, #113467, #10545, #92905, #31096, #97168, #111332, #160014, #168265, #84876, #202869, #85951, #201801, #87011, #146986, #101117, #3594, #186640, #185565, #167204, #183442, #153083, #37194, #152026, #103270, #69672, #104343, #70731, #134728, #170387, #21976, #102199, #88086, #4659, #18793, #35046, #200735, #150965, #2530, #53443, #187705, #52385, #154158, #19866, #184497, #136844, #68605, #213003, #130780, #135778, #118513, #36116, #199677, #171466, #119581, #169332, #20916, #54517, #120661, #38266, #64640, #5725, #71804, #137915, #117448, #203935, #55583, #121738, #39333, #105430, #23055, #51320, #90233, #57722, #72881, #6805, #140065, #43627, #40417, #8962, #175753, #155224, #123880, #106520, #172546, #122820, #42565, #189845, #91311, #93447, #142202, #190901, #141152, #159485, #89172, #207161, #24131, #58784, #107604, #108667, #124938, #156298, #41492, #109742, #138989, #205010, #173635, #25206, #73970, #56657, #191960, #27344, #7882, #174697, #188779, #75037, #206087, #157368, #26271, #92388, #158424, #10024, #76099, #208217, #59849, #126001, #55213, #200368, #184127, #22679, #35750, #154849, #136474, #69294, #52016, #4288, #118142, #21601, #121359, #103971, #102893, #138606, #23761, #134364, #170013, #168952, #152706, #3227, #137543, #36811, #185187, #203561, #87707, #89866, #119201, #20555, #186259, #187334, #71431, #153779, #85567, #6433, #135405, #86639, #5349, #70360, #38963, #155917, #72508, #105048, #171083, #88791, #204629, #202495, #56280, #101824, #201428, #122439, #53068, #167892, #54147, #120284, #37893 ) ),
 .UNSPECIFIED., .F., .F., .T. ) 
 B_SPLINE_SURFACE_WITH_KNOTS ( ( 2, 2 ),
 ( 3, 2, 2, 2, 2, 2, 2, 2, 2, 2, 2, 2, 2, 2, 2, 2, 2, 2, 2, 2, 2, 2, 2, 2, 2, 2, 2, 2, 2, 2, 2, 2, 2, 2, 2, 2, 2, 2, 2, 2, 2, 2, 2, 2, 2, 2, 2, 2, 2, 2, 2, 2, 2, 2, 2, 2, 2, 2, 2, 2, 2, 2, 2, 2, 2, 2, 2, 2, 2, 2, 2, 2, 2, 2, 2, 2, 2, 2, 2, 2, 2, 2, 2, 2, 2, 2, 2, 2, 2, 2, 2, 2, 2, 2, 2, 2, 3 ),
 ( 0.000000000000000000, 1.000000000000000000 ),
 ( 0.000000000000000000, 0.01041666666666666609, 0.02083333333333333218, 0.03125000000000000000, 0.04166666666666666435, 0.05208333333333333565, 0.06250000000000000000, 0.07291666666666667129, 0.08333333333333332871, 0.09375000000000000000, 0.1041666666666666713, 0.1145833333333333287, 0.1250000000000000000, 0.1354166666666666574, 0.1458333333333333426, 0.1562500000000000000, 0.1666666666666666574, 0.1770833333333333426, 0.1875000000000000000, 0.1979166666666666574, 0.2083333333333333426, 0.2187500000000000000, 0.2291666666666666574, 0.2395833333333333426, 0.2500000000000000000, 0.2604166666666666852, 0.2708333333333333148, 0.2812500000000000000, 0.2916666666666666852, 0.3020833333333333148, 0.3125000000000000000, 0.3229166666666666852, 0.3333333333333333148, 0.3437500000000000000, 0.3541666666666666852, 0.3645833333333333148, 0.3750000000000000000, 0.3854166666666666852, 0.3958333333333333148, 0.4062500000000000000, 0.4166666666666666852, 0.4270833333333333148, 0.4375000000000000000, 0.4479166666666666852, 0.4583333333333333148, 0.4687500000000000000, 0.4791666666666666852, 0.4895833333333333148, 0.5000000000000000000, 0.5104166666666666297, 0.5208333333333333703, 0.5312500000000000000, 0.5416666666666666297, 0.5520833333333333703, 0.5625000000000000000, 0.5729166666666666297, 0.5833333333333333703, 0.5937500000000000000, 0.6041666666666666297, 0.6145833333333333703, 0.6250000000000000000, 0.6354166666666666297, 0.6458333333333333703, 0.6562500000000000000, 0.6666666666666666297, 0.6770833333333333703, 0.6875000000000000000, 0.6979166666666666297, 0.7083333333333333703, 0.7187500000000000000, 0.7291666666666666297, 0.7395833333333333703, 0.7500000000000000000, 0.7604166666666666297, 0.7708333333333333703, 0.7812500000000000000, 0.7916666666666666297, 0.8020833333333333703, 0.8125000000000000000, 0.8229166666666666297, 0.8333333333333333703, 0.8437500000000000000, 0.8541666666666666297, 0.8645833333333333703, 0.8750000000000000000, 0.8854166666666666297, 0.8958333333333333703, 0.9062500000000000000, 0.9166666666666666297, 0.9270833333333333703, 0.9375000000000000000, 0.9479166666666666297, 0.9583333333333333703, 0.9687500000000000000, 0.9791666666666666297, 0.9895833333333333703, 1.000000000000000000 ),
 .UNSPECIFIED. ) 
 GEOMETRIC_REPRESENTATION_ITEM ( )  RATIONAL_B_SPLINE_SURFACE ( (
 ( 1.000000000000000000, 0.8660254037844387076, 1.000000000000000000, 0.8660254037844387076, 1.000000000000000000, 0.8660254037844387076, 1.000000000000000000, 0.8660254037844387076, 1.000000000000000000, 0.8660254037844387076, 1.000000000000000000, 0.8660254037844387076, 1.000000000000000000, 0.8660254037844387076, 1.000000000000000000, 0.8660254037844387076, 1.000000000000000000, 0.8660254037844387076, 1.000000000000000000, 0.8660254037844387076, 1.000000000000000000, 0.8660254037844387076, 1.000000000000000000, 0.8660254037844387076, 1.000000000000000000, 0.8660254037844387076, 1.000000000000000000, 0.8660254037844387076, 1.000000000000000000, 0.8660254037844387076, 1.000000000000000000, 0.8660254037844387076, 1.000000000000000000, 0.8660254037844387076, 1.000000000000000000, 0.8660254037844387076, 1.000000000000000000, 0.8660254037844387076, 1.000000000000000000, 0.8660254037844387076, 1.000000000000000000, 0.8660254037844387076, 1.000000000000000000, 0.8660254037844387076, 1.000000000000000000, 0.8660254037844387076, 1.000000000000000000, 0.8660254037844387076, 1.000000000000000000, 0.8660254037844387076, 1.000000000000000000, 0.8660254037844387076, 1.000000000000000000, 0.8660254037844387076, 1.000000000000000000, 0.8660254037844387076, 1.000000000000000000, 0.8660254037844387076, 1.000000000000000000, 0.8660254037844387076, 1.000000000000000000, 0.8660254037844387076, 1.000000000000000000, 0.8660254037844387076, 1.000000000000000000, 0.8660254037844387076, 1.000000000000000000, 0.8660254037844387076, 1.000000000000000000, 0.8660254037844387076, 1.000000000000000000, 0.8660254037844387076, 1.000000000000000000, 0.8660254037844387076, 1.000000000000000000, 0.8660254037844387076, 1.000000000000000000, 0.8660254037844387076, 1.000000000000000000, 0.8660254037844387076, 1.000000000000000000, 0.8660254037844387076, 1.000000000000000000, 0.8660254037844387076, 1.000000000000000000, 0.8660254037844387076, 1.000000000000000000, 0.8660254037844387076, 1.000000000000000000, 0.8660254037844387076, 1.000000000000000000, 0.8660254037844387076, 1.000000000000000000, 0.8660254037844387076, 1.000000000000000000, 0.8660254037844387076, 1.000000000000000000, 0.8660254037844387076, 1.000000000000000000, 0.8660254037844387076, 1.000000000000000000, 0.8660254037844387076, 1.000000000000000000, 0.8660254037844387076, 1.000000000000000000, 0.8660254037844387076, 1.000000000000000000, 0.8660254037844387076, 1.000000000000000000, 0.8660254037844387076, 1.000000000000000000, 0.8660254037844387076, 1.000000000000000000, 0.8660254037844387076, 1.000000000000000000, 0.8660254037844387076, 1.000000000000000000, 0.8660254037844387076, 1.000000000000000000, 0.8660254037844387076, 1.000000000000000000, 0.8660254037844387076, 1.000000000000000000, 0.8660254037844387076, 1.000000000000000000, 0.8660254037844387076, 1.000000000000000000, 0.8660254037844387076, 1.000000000000000000, 0.8660254037844387076, 1.000000000000000000, 0.8660254037844387076, 1.000000000000000000, 0.8660254037844387076, 1.000000000000000000, 0.8660254037844387076, 1.000000000000000000, 0.8660254037844387076, 1.000000000000000000, 0.8660254037844387076, 1.000000000000000000, 0.8660254037844387076, 1.000000000000000000, 0.8660254037844387076, 1.000000000000000000, 0.8660254037844387076, 1.000000000000000000, 0.8660254037844387076, 1.000000000000000000, 0.8660254037844387076, 1.000000000000000000, 0.8660254037844387076, 1.000000000000000000, 0.8660254037844387076, 1.000000000000000000, 0.8660254037844387076, 1.000000000000000000, 0.8660254037844387076, 1.000000000000000000, 0.8660254037844387076, 1.000000000000000000, 0.8660254037844387076, 1.000000000000000000, 0.8660254037844387076, 1.000000000000000000, 0.8660254037844387076, 1.000000000000000000, 0.8660254037844387076, 1.000000000000000000, 0.8660254037844387076, 1.000000000000000000, 0.8660254037844387076, 1.000000000000000000, 0.8660254037844387076, 1.000000000000000000, 0.8660254037844387076, 1.000000000000000000, 0.8660254037844387076, 1.000000000000000000, 0.8660254037844387076, 1.000000000000000000, 0.8660254037844387076, 1.000000000000000000, 0.8660254037844387076, 1.000000000000000000, 0.8660254037844387076, 1.000000000000000000, 0.8660254037844387076, 1.000000000000000000, 0.8660254037844387076, 1.000000000000000000, 0.8660254037844387076, 1.000000000000000000),
 ( 1.000000000000000000, 0.8660254037844387076, 1.000000000000000000, 0.8660254037844387076, 1.000000000000000000, 0.8660254037844387076, 1.000000000000000000, 0.8660254037844387076, 1.000000000000000000, 0.8660254037844387076, 1.000000000000000000, 0.8660254037844387076, 1.000000000000000000, 0.8660254037844387076, 1.000000000000000000, 0.8660254037844387076, 1.000000000000000000, 0.8660254037844387076, 1.000000000000000000, 0.8660254037844387076, 1.000000000000000000, 0.8660254037844387076, 1.000000000000000000, 0.8660254037844387076, 1.000000000000000000, 0.8660254037844387076, 1.000000000000000000, 0.8660254037844387076, 1.000000000000000000, 0.8660254037844387076, 1.000000000000000000, 0.8660254037844387076, 1.000000000000000000, 0.8660254037844387076, 1.000000000000000000, 0.8660254037844387076, 1.000000000000000000, 0.8660254037844387076, 1.000000000000000000, 0.8660254037844387076, 1.000000000000000000, 0.8660254037844387076, 1.000000000000000000, 0.8660254037844387076, 1.000000000000000000, 0.8660254037844387076, 1.000000000000000000, 0.8660254037844387076, 1.000000000000000000, 0.8660254037844387076, 1.000000000000000000, 0.8660254037844387076, 1.000000000000000000, 0.8660254037844387076, 1.000000000000000000, 0.8660254037844387076, 1.000000000000000000, 0.8660254037844387076, 1.000000000000000000, 0.8660254037844387076, 1.000000000000000000, 0.8660254037844387076, 1.000000000000000000, 0.8660254037844387076, 1.000000000000000000, 0.8660254037844387076, 1.000000000000000000, 0.8660254037844387076, 1.000000000000000000, 0.8660254037844387076, 1.000000000000000000, 0.8660254037844387076, 1.000000000000000000, 0.8660254037844387076, 1.000000000000000000, 0.8660254037844387076, 1.000000000000000000, 0.8660254037844387076, 1.000000000000000000, 0.8660254037844387076, 1.000000000000000000, 0.8660254037844387076, 1.000000000000000000, 0.8660254037844387076, 1.000000000000000000, 0.8660254037844387076, 1.000000000000000000, 0.8660254037844387076, 1.000000000000000000, 0.8660254037844387076, 1.000000000000000000, 0.8660254037844387076, 1.000000000000000000, 0.8660254037844387076, 1.000000000000000000, 0.8660254037844387076, 1.000000000000000000, 0.8660254037844387076, 1.000000000000000000, 0.8660254037844387076, 1.000000000000000000, 0.8660254037844387076, 1.000000000000000000, 0.8660254037844387076, 1.000000000000000000, 0.8660254037844387076, 1.000000000000000000, 0.8660254037844387076, 1.000000000000000000, 0.8660254037844387076, 1.000000000000000000, 0.8660254037844387076, 1.000000000000000000, 0.8660254037844387076, 1.000000000000000000, 0.8660254037844387076, 1.000000000000000000, 0.8660254037844387076, 1.000000000000000000, 0.8660254037844387076, 1.000000000000000000, 0.8660254037844387076, 1.000000000000000000, 0.8660254037844387076, 1.000000000000000000, 0.8660254037844387076, 1.000000000000000000, 0.8660254037844387076, 1.000000000000000000, 0.8660254037844387076, 1.000000000000000000, 0.8660254037844387076, 1.000000000000000000, 0.8660254037844387076, 1.000000000000000000, 0.8660254037844387076, 1.000000000000000000, 0.8660254037844387076, 1.000000000000000000, 0.8660254037844387076, 1.000000000000000000, 0.8660254037844387076, 1.000000000000000000, 0.8660254037844387076, 1.000000000000000000, 0.8660254037844387076, 1.000000000000000000, 0.8660254037844387076, 1.000000000000000000, 0.8660254037844387076, 1.000000000000000000, 0.8660254037844387076, 1.000000000000000000, 0.8660254037844387076, 1.000000000000000000, 0.8660254037844387076, 1.000000000000000000, 0.8660254037844387076, 1.000000000000000000, 0.8660254037844387076, 1.000000000000000000, 0.8660254037844387076, 1.000000000000000000, 0.8660254037844387076, 1.000000000000000000, 0.8660254037844387076, 1.000000000000000000, 0.8660254037844387076, 1.000000000000000000, 0.8660254037844387076, 1.000000000000000000, 0.8660254037844387076, 1.000000000000000000, 0.8660254037844387076, 1.000000000000000000, 0.8660254037844387076, 1.000000000000000000, 0.8660254037844387076, 1.000000000000000000, 0.8660254037844387076, 1.000000000000000000, 0.8660254037844387076, 1.000000000000000000, 0.8660254037844387076, 1.000000000000000000, 0.8660254037844387076, 1.000000000000000000, 0.8660254037844387076, 1.000000000000000000, 0.8660254037844387076, 1.000000000000000000, 0.8660254037844387076, 1.000000000000000000) ) ) 
 REPRESENTATION_ITEM ( '' )  SURFACE ( )  );
#2432=VECTOR ( 'NONE', #111770, 1000.000000000000000 ) ;
#2438=CARTESIAN_POINT ( 'NONE',  ( -1.225000000000048050, 2.791666667349441688, -0.7072540797572957061 ) ) ;
#2444=CARTESIAN_POINT ( 'NONE',  ( -1.992711204631002198E-15, 2.999999999999989342, 1.224999999999989875 ) ) ;
#2523=CARTESIAN_POINT ( 'NONE',  ( -0.6125000000000314637, 0.9583333333333388104, -1.060881119635965764 ) ) ;
#2530=CARTESIAN_POINT ( 'NONE',  ( -1.225000000000016076, 1.812500000682795598, -2.081668171172168513E-14 ) ) ;
#2540=ORIENTED_EDGE ( 'NONE', *, *, #181210, .T. ) ;
#2572=ADVANCED_FACE ( 'NONE', ( #9393 ), #208641, .F. ) ;
#2616=ORIENTED_EDGE ( 'NONE', *, *, #192096, .F. ) ;
#2664=CARTESIAN_POINT ( 'NONE',  ( -1.992711204631002198E-15, 2.999999999999989342, 1.224999999999989875 ) ) ;
#2681=ADVANCED_FACE ( 'NONE', ( #110168 ), #108034, .T. ) ;
#2712=CIRCLE ( 'NONE', #189522, 0.04999999999999985706 ) ;
#2741=CARTESIAN_POINT ( 'NONE',  ( -1.814759087649598923, 3.975067388632297138, -0.4606438099578613055 ) ) ;
#2744=CARTESIAN_POINT ( 'NONE',  ( -1.752700365193352367E-14, 1.609375000341425777, -1.570758158831794260 ) ) ;
#2745=SHAPE_DEFINITION_REPRESENTATION ( #178641, #121983 ) ;
#2766=CARTESIAN_POINT ( 'NONE',  ( -4.156403723172807449E-14, 0.3125000000000094924, 1.414508159514557439 ) ) ;
#2805=CARTESIAN_POINT ( 'NONE',  ( 3.602337597214539753E-15, 1.000000000682806034, -1.225000000000015410 ) ) ;
#2900=EDGE_LOOP ( 'NONE', ( #47457, #196132, #160277, #122236 ) ) ;
#2912=CARTESIAN_POINT ( 'NONE',  ( 0.6801582343749865700, 0.08854166700808518975, -1.178068619123869398 ) ) ;
#2927=EDGE_CURVE ( 'NONE', #104013, #15383, #204212, .T. ) ;
#3061=CARTESIAN_POINT ( 'NONE',  ( 1.360316468749966257, 1.765625000341414230, -3.642919299551294898E-14 ) ) ;
#3133=CARTESIAN_POINT ( 'NONE',  ( 1.224999999999979217, 2.604166666666692276, 0.7072540797572558491 ) ) ;
#3166=CARTESIAN_POINT ( 'NONE',  ( -1.162044386198238837E-16, 1.437500000000019540, -1.225000000000020739 ) ) ;
#3187=CARTESIAN_POINT ( 'NONE',  ( 0.4336004510535496626, 3.058108253035741964, -0.4198436715061193980 ) ) ;
#3221=DIRECTION ( 'NONE',  ( -1.276756478318932585E-15, 1.000000000000000000, -1.665334536937738262E-16 ) ) ;
#3227=CARTESIAN_POINT ( 'NONE',  ( -1.225000000000040057, -0.4583333326505021343, -0.7072540797573018123 ) ) ;
#3262=CARTESIAN_POINT ( 'NONE',  ( 0.6801582343749796866, -0.9114583329919088150, -1.178068619123886718 ) ) ;
#3304=CARTESIAN_POINT ( 'NONE',  ( -0.6801582343750403048, 1.598958333674738164, -1.178068619123869398 ) ) ;
#3320=VERTEX_POINT ( 'NONE', #191033 ) ;
#3343=CIRCLE ( 'NONE', #148711, 0.04999999999999991257 ) ;
#3373=CARTESIAN_POINT ( 'NONE',  ( -0.4000000000000322742, -2.775557561562891351E-14, 0.4999999999999535927 ) ) ;
#3409=ORIENTED_EDGE ( 'NONE', *, *, #85916, .F. ) ;
#3438=ORIENTED_EDGE ( 'NONE', *, *, #195789, .T. ) ;
#3475=LINE ( 'NONE', #4532, #47724 ) ;
#3503=ORIENTED_EDGE ( 'NONE', *, *, #34131, .T. ) ;
#3513=CARTESIAN_POINT ( 'NONE',  ( -0.6125000000000192513, 1.958333333333318826, -1.060881119635962211 ) ) ;
#3594=CARTESIAN_POINT ( 'NONE',  ( -0.6125000000000158096, 2.270833334016133964, -1.060881119635972647 ) ) ;
#3668=CARTESIAN_POINT ( 'NONE',  ( 0.4499999999999747535, 4.000000000000003553, -5.377642775528101993E-14 ) ) ;
#3696=CARTESIAN_POINT ( 'NONE',  ( -0.6125000000000037081, 2.458333333333319271, -1.060881119635955327 ) ) ;
#3802=CARTESIAN_POINT ( 'NONE',  ( 1.360316468749957597, 1.776041667008106506, 0.7853790794158801436 ) ) ;
#3825=CARTESIAN_POINT ( 'NONE',  ( 1.224999999999947020, 0.8958333333333401427, -0.7072540797573197979 ) ) ;
#3963=ORIENTED_EDGE ( 'NONE', *, *, #75861, .T. ) ;
#3980=CARTESIAN_POINT ( 'NONE',  ( 1.360316468749955598, 0.5260416670081086155, 0.7853790794158820310 ) ) ;
#3986=CIRCLE ( 'NONE', #152759, 1.962502847949850526 ) ;
#4048=ORIENTED_EDGE ( 'NONE', *, *, #197756, .F. ) ;
#4098=CYLINDRICAL_SURFACE ( 'NONE', #203756, 1.224999999999996980 ) ;
#4127=ORIENTED_EDGE ( 'NONE', *, *, #163291, .T. ) ;
#4129=CARTESIAN_POINT ( 'NONE',  ( -1.360316468750044860, 1.411458333674720622, 0.7853790794158801436 ) ) ;
#4199=CARTESIAN_POINT ( 'NONE',  ( 1.224999999999995204, 2.875000000000002665, 0.000000000000000000 ) ) ;
#4244=CARTESIAN_POINT ( 'NONE',  ( 1.284915497622363123, -5.970188836749928864E-15, -0.3104282545687488959 ) ) ;
#4283=CARTESIAN_POINT ( 'NONE',  ( 8.134310703387671364E-16, 2.000000000682804924, -1.225000000000021849 ) ) ;
#4288=CARTESIAN_POINT ( 'NONE',  ( -1.225000000000014078, -0.2083333326505250049, -0.7072540797572977045 ) ) ;
#4291=EDGE_CURVE ( 'NONE', #12260, #30915, #53572, .T. ) ;
#4323=CARTESIAN_POINT ( 'NONE',  ( 0.6801582343749900117, -0.4114583329919083154, -1.178068619123855409 ) ) ;
#4353=VERTEX_POINT ( 'NONE', #200857 ) ;
#4364=CARTESIAN_POINT ( 'NONE',  ( -0.6801582343750161019, 0.6822916670080614310, 1.178068619123810334 ) ) ;
#4374=ORIENTED_EDGE ( 'NONE', *, *, #96704, .T. ) ;
#4457=EDGE_LOOP ( 'NONE', ( #92481, #97816, #3438, #190730, #136190, #88897 ) ) ;
#4508=CARTESIAN_POINT ( 'NONE',  ( -1.734723475976807094E-15, 2.999999999999988898, -6.938893903907228378E-15 ) ) ;
#4532=CARTESIAN_POINT ( 'NONE',  ( 0.4499999999999747535, 4.000000000000003553, -5.377642775528101993E-14 ) ) ;
#4560=CARTESIAN_POINT ( 'NONE',  ( 0.6125000000000037081, 0.3333333333333590720, 1.060881119635903147 ) ) ;
#4659=CARTESIAN_POINT ( 'NONE',  ( 1.224999999999959233, 1.916666667349501196, 0.7072540797572717253 ) ) ;
#4745=EDGE_CURVE ( 'NONE', #42265, #62112, #156421, .T. ) ;
#4866=CARTESIAN_POINT ( 'NONE',  ( -0.6801582343750438575, 1.630208333674734611, -1.178068619123879834 ) ) ;
#4883=( BOUNDED_CURVE ( )  B_SPLINE_CURVE ( 3, ( #122582, #187475, #188544, #172308 ),
 .UNSPECIFIED., .F., .T. ) 
 B_SPLINE_CURVE_WITH_KNOTS ( ( 4, 4 ),
 ( 3.141592653589828643, 4.712388980384858428 ),
 .UNSPECIFIED. ) 
 CURVE ( )  GEOMETRIC_REPRESENTATION_ITEM ( )  RATIONAL_B_SPLINE_CURVE ( ( 1.000000000000000000, 0.8047378541243335182, 0.8047378541243335182, 1.000000000000000000 ) ) 
 REPRESENTATION_ITEM ( '' )  );
#4889=CARTESIAN_POINT ( 'NONE',  ( -1.151774525698488676E-14, 0.6875000000000193179, -1.414508159514585417 ) ) ;
#4902=LINE ( 'NONE', #206335, #160144 ) ;
#4972=DIRECTION ( 'NONE',  ( 1.276756478318932585E-15, -1.000000000000000000, 1.665334536937738262E-16 ) ) ;
#4984=EDGE_CURVE ( 'NONE', #179126, #141384, #144052, .T. ) ;
#5047=DIRECTION ( 'NONE',  ( -1.276756478318932585E-15, 1.000000000000000000, -1.665334536937738262E-16 ) ) ;
#5066=EDGE_CURVE ( 'NONE', #139477, #45585, #136576, .T. ) ;
#5076=CARTESIAN_POINT ( 'NONE',  ( -1.992711204631002198E-15, 2.999999999999989342, 1.224999999999989875 ) ) ;
#5098=VERTEX_POINT ( 'NONE', #149389 ) ;
#5109=ORIENTED_EDGE ( 'NONE', *, *, #29662, .T. ) ;
#5160=CARTESIAN_POINT ( 'NONE',  ( -0.3282377607281405374, 1.801335450315361131, 1.224999999999994982 ) ) ;
#5192=CARTESIAN_POINT ( 'NONE',  ( -1.360316468750046859, 0.6197916670081009549, -0.7853790794159322131 ) ) ;
#5194=FACE_BOUND ( 'NONE', #61549, .T. ) ;
#5260=CARTESIAN_POINT ( 'NONE',  ( -0.6125000000000175859, 2.541666666666664298, 1.060881119635903147 ) ) ;
#5303=CARTESIAN_POINT ( 'NONE',  ( 2.007420792093927986E-08, -6.938893903907228378E-15, -1.225000000000033396 ) ) ;
#5341=CARTESIAN_POINT ( 'NONE',  ( -0.5000000000000143219, 3.949999999999981526, 0.4999999999999553690 ) ) ;
#5349=CARTESIAN_POINT ( 'NONE',  ( 1.224999999999979661, -0.8124999993172135060, -2.602085213965210642E-14 ) ) ;
#5422=CARTESIAN_POINT ( 'NONE',  ( 0.6801582343749987825, 1.557291667008103841, -1.178068619123876282 ) ) ;
#5429=CARTESIAN_POINT ( 'NONE',  ( -0.6801582343750247617, 0.09895833367471601472, -1.178068619123872729 ) ) ;
#5725=CARTESIAN_POINT ( 'NONE',  ( -1.225000000000038058, 1.333333334016162386, 0.7072540797572777205 ) ) ;
#5802=DIRECTION ( 'NONE',  ( -3.330669073875479482E-16, 3.330669073875479482E-16, 1.000000000000000000 ) ) ;
#5847=CARTESIAN_POINT ( 'NONE',  ( -0.3788956605886329987, 3.049042541176487209, 0.4283520265745272004 ) ) ;
#5943=CARTESIAN_POINT ( 'NONE',  ( -1.360316468750018659, 2.401041667008069425, -0.7853790794159061228 ) ) ;
#5966=CARTESIAN_POINT ( 'NONE',  ( -1.151774525698488676E-14, 0.4375000000000101030, -1.414508159514601626 ) ) ;
#6013=EDGE_CURVE ( 'NONE', #130707, #106774, #129254, .T. ) ;
#6081=LINE ( 'NONE', #137195, #51417 ) ;
#6089=VERTEX_POINT ( 'NONE', #101980 ) ;
#6118=AXIS2_PLACEMENT_3D ( 'NONE', #74804, #144113, #58547 ) ;
#6181=CARTESIAN_POINT ( 'NONE',  ( 0.6124999999999880540, 0.1666666666666899443, -1.060881119635979530 ) ) ;
#6267=VERTEX_POINT ( 'NONE', #36970 ) ;
#6269=CARTESIAN_POINT ( 'NONE',  ( -0.6801582343750282034, 0.8489583336747236197, -1.178068619123876282 ) ) ;
#6287=CARTESIAN_POINT ( 'NONE',  ( -0.4170821662629227156, 3.033599471985643170, 0.4170821662629036752 ) ) ;
#6342=CARTESIAN_POINT ( 'NONE',  ( -1.225000000000042277, 2.479166666666715368, -0.7072540797573197979 ) ) ;
#6383=B_SPLINE_CURVE_WITH_KNOTS ( 'NONE', 3,
 ( #38914, #73536, #152662, #203513, #4244, #70315, #54102, #21555, #138561, #69250, #120238, #204582, #87665, #153735, #22636, #5303 ),
 .UNSPECIFIED., .F., .F.,
 ( 4, 2, 2, 2, 2, 2, 2, 4 ),
 ( 0.000000000000000000, 0.0006374118625136481224, 0.0009561177937704720209, 0.001274823725027296028, 0.001593529656284120143, 0.001912235587540944042, 0.002230941518797768374, 0.002549647450054592056 ),
 .UNSPECIFIED. ) ;
#6388=CARTESIAN_POINT ( 'NONE',  ( 1.872228381520312013, 3.299999999999997158, -0.4000000000000131783 ) ) ;
#6433=CARTESIAN_POINT ( 'NONE',  ( -5.508486862036250636E-15, -0.7499999993172156154, -1.414508159514623609 ) ) ;
#6448=LINE ( 'NONE', #188415, #192774 ) ;
#6466=AXIS2_PLACEMENT_3D ( 'NONE', #127068, #146460, #15339 ) ;
#6501=CARTESIAN_POINT ( 'NONE',  ( -0.6801582343750143256, 1.848958333674724397, -1.178068619123862515 ) ) ;
#6509=CARTESIAN_POINT ( 'NONE',  ( 0.6801582343749813520, 0.2239583336747300035, 1.178068619123796568 ) ) ;
#6634=CARTESIAN_POINT ( 'NONE',  ( 0.4499999999999903522, 3.949999999999988187, -0.8338124244295659349 ) ) ;
#6673=ORIENTED_EDGE ( 'NONE', *, *, #72117, .T. ) ;
#6729=CARTESIAN_POINT ( 'NONE',  ( 1.360316468749978469, 2.296875000341369599, -4.857225732735059864E-14 ) ) ;
#6783=ORIENTED_EDGE ( 'NONE', *, *, #38562, .T. ) ;
#6805=CARTESIAN_POINT ( 'NONE',  ( -1.225000000000038058, 1.041666667349488984, -0.7072540797573257931 ) ) ;
#6835=( BOUNDED_CURVE ( )  B_SPLINE_CURVE ( 2, ( #201795, #198600, #383, #35039, #18785, #136837, #2523, #19858, #68599 ),
 .UNSPECIFIED., .F., .T. ) 
 B_SPLINE_CURVE_WITH_KNOTS ( ( 3, 2, 2, 2, 3 ),
 ( 0.4843749999999998335, 0.4895833333333333148, 0.5000000000000000000, 0.5104166666666666297, 0.5156250000000002220 ),
 .UNSPECIFIED. ) 
 CURVE ( )  GEOMETRIC_REPRESENTATION_ITEM ( )  RATIONAL_B_SPLINE_CURVE ( ( 0.9330127018922194093, 0.9330127018922171889, 1.000000000000000000, 0.8660254037844387076, 1.000000000000000000, 0.8660254037844387076, 1.000000000000000000, 0.9330127018922165227, 0.9330127018922194093 ) ) 
 REPRESENTATION_ITEM ( '' )  );
#6861=FACE_OUTER_BOUND ( 'NONE', #192849, .T. ) ;
#6885=ORIENTED_EDGE ( 'NONE', *, *, #205195, .F. ) ;
#6917=CARTESIAN_POINT ( 'NONE',  ( -0.3769810270648435990, 3.049942316455334090, 0.4288785890452350702 ) ) ;
#6935=VECTOR ( 'NONE', #48280, 1000.000000000000000 ) ;
#7014=CARTESIAN_POINT ( 'NONE',  ( 1.360316468749973140, 0.5468750003413819227, -2.081668171172168513E-14 ) ) ;
#7034=CARTESIAN_POINT ( 'NONE',  ( 1.224999999999971001, -0.6458333333332910708, 0.7072540797572737237 ) ) ;
#7159=LINE ( 'NONE', #125290, #43171 ) ;
#7193=CARTESIAN_POINT ( 'NONE',  ( 0.4999999999999779066, 3.999999999999989786, 0.4999999999999640288 ) ) ;
#7248=DIRECTION ( 'NONE',  ( 1.276756478318932585E-15, -1.000000000000000000, 1.665334536937738262E-16 ) ) ;
#7339=CARTESIAN_POINT ( 'NONE',  ( -0.6801582343750074422, 0.5989583336747372755, -1.178068619123841643 ) ) ;
#7357=CARTESIAN_POINT ( 'NONE',  ( -0.5000000000000022204, 3.300000000000004263, 0.4000000000000010214 ) ) ;
#7410=CARTESIAN_POINT ( 'NONE',  ( 0.6124999999999637401, 2.416666666666629659, -1.060881119635962211 ) ) ;
#7424=CARTESIAN_POINT ( 'NONE',  ( -1.992711204631002198E-15, 2.999999999999989342, 1.224999999999989875 ) ) ;
#7444=CARTESIAN_POINT ( 'NONE',  ( -1.910130646976150981, 3.278792710263227050, 0.4195261609910668210 ) ) ;
#7459=CARTESIAN_POINT ( 'NONE',  ( -1.734723475976807094E-15, 2.999999999999988898, -6.938893903907228378E-15 ) ) ;
#7570=CARTESIAN_POINT ( 'NONE',  ( 0.6801582343749987825, 2.557291667008069869, -1.178068619123886718 ) ) ;
#7576=EDGE_CURVE ( 'NONE', #105749, #160775, #119719, .T. ) ;
#7578=CARTESIAN_POINT ( 'NONE',  ( -0.6801582343750143256, 0.3489583336747370534, -1.178068619123865846 ) ) ;
#7641=CARTESIAN_POINT ( 'NONE',  ( 1.224999999999989875, 0.4375000006828014265, -4.510281037539698445E-14 ) ) ;
#7645=CARTESIAN_POINT ( 'NONE',  ( 1.930984528693787894, 3.480873151563967927, 0.3999999999999849232 ) ) ;
#7664=ORIENTED_EDGE ( 'NONE', *, *, #100518, .T. ) ;
#7801=CARTESIAN_POINT ( 'NONE',  ( 1.360316468749975582, 2.317708333674725285, -0.7853790794158961308 ) ) ;
#7811=ORIENTED_EDGE ( 'NONE', *, *, #40880, .F. ) ;
#7812=CARTESIAN_POINT ( 'NONE',  ( 0.6125000000000071498, 2.395833334016134408, 1.060881119635924019 ) ) ;
#7882=CARTESIAN_POINT ( 'NONE',  ( -0.6125000000000019318, 0.2708333340161322988, -1.060881119635941339 ) ) ;
#7962=ORIENTED_EDGE ( 'NONE', *, *, #121327, .T. ) ;
#8023=( BOUNDED_SURFACE ( )  B_SPLINE_SURFACE ( 3, 2, ( 
 ( #117061, #31505, #14145 ),
 ( #163637, #178826, #15219 ),
 ( #162571, #80239, #212351 ),
 ( #183059, #52006, #148449 ) ),
 .UNSPECIFIED., .F., .F., .T. ) 
 B_SPLINE_SURFACE_WITH_KNOTS ( ( 4, 4 ),
 ( 3, 3 ),
 ( 4.712388980384689674, 6.283185307179586232 ),
 ( 0.000000000000000000, 1.000000000000000000 ),
 .UNSPECIFIED. ) 
 GEOMETRIC_REPRESENTATION_ITEM ( )  RATIONAL_B_SPLINE_SURFACE ( (
 ( 1.000000000000000000, 0.7071067811865294761, 1.000000000000000000),
 ( 1.000000000000000000, 0.8014503788335076706, 1.000000000000000000),
 ( 1.000000000000000000, 0.8676977444974025566, 1.000000000000000000),
 ( 1.000000000000000000, 0.8661919058288510831, 1.000000000000000000) ) ) 
 REPRESENTATION_ITEM ( '' )  SURFACE ( )  );
#8045=CARTESIAN_POINT ( 'NONE',  ( -1.225000000000042277, 2.229166666666690499, -0.7072540797573217963 ) ) ;
#8101=CARTESIAN_POINT ( 'NONE',  ( -1.360316468750012886, -0.05729166632526227348, 0.7853790794158901356 ) ) ;
#8125=CARTESIAN_POINT ( 'NONE',  ( -0.6125000000000001554, -0.4583333333332967330, 1.060881119635912029 ) ) ;
#8216=DIRECTION ( 'NONE',  ( 3.330669073875479482E-16, -3.330669073875479482E-16, -1.000000000000000000 ) ) ;
#8235=ORIENTED_EDGE ( 'NONE', *, *, #138098, .F. ) ;
#8275=FACE_OUTER_BOUND ( 'NONE', #127862, .T. ) ;
#8407=ORIENTED_EDGE ( 'NONE', *, *, #80469, .T. ) ;
#8417=CARTESIAN_POINT ( 'NONE',  ( 1.360316468750000896, 0.7656250003413994643, 0.000000000000000000 ) ) ;
#8489=CARTESIAN_POINT ( 'NONE',  ( -3.956095110007852622E-14, 1.437500000000030864, -1.414508159514597407 ) ) ;
#8648=CARTESIAN_POINT ( 'NONE',  ( -0.6801582343750403048, 1.598958333674738164, -1.178068619123869398 ) ) ;
#8673=ORIENTED_EDGE ( 'NONE', *, *, #183782, .T. ) ;
#8717=CARTESIAN_POINT ( 'NONE',  ( 0.4214947629261721618, 3.038568440852233987, -0.4183962726263586451 ) ) ;
#8733=( BOUNDED_CURVE ( )  B_SPLINE_CURVE ( 2, ( #87070, #206147, #153140, #74030, #169388, #57775, #72940, #140121, #156355 ),
 .UNSPECIFIED., .F., .T. ) 
 B_SPLINE_CURVE_WITH_KNOTS ( ( 3, 2, 2, 2, 3 ),
 ( 0.3593749999999999445, 0.3645833333333333148, 0.3750000000000000000, 0.3854166666666666852, 0.3906250000000001665 ),
 .UNSPECIFIED. ) 
 CURVE ( )  GEOMETRIC_REPRESENTATION_ITEM ( )  RATIONAL_B_SPLINE_CURVE ( ( 0.9330127018922194093, 0.9330127018922186322, 1.000000000000000000, 0.8660254037844387076, 1.000000000000000000, 0.8660254037844387076, 1.000000000000000000, 0.9330127018922171889, 0.9330127018922194093 ) ) 
 REPRESENTATION_ITEM ( '' )  );
#8762=DIRECTION ( 'NONE',  ( -3.330669073875472579E-16, 1.665334536937734318E-16, 1.000000000000000000 ) ) ;
#8788=CARTESIAN_POINT ( 'NONE',  ( -0.5000000000000091038, 3.999999999999948042, -0.5000000000000368594 ) ) ;
#8819=EDGE_CURVE ( 'NONE', #78057, #12050, #73389, .T. ) ;
#8879=CARTESIAN_POINT ( 'NONE',  ( -1.360316468750004448, 1.671875000341424666, -8.673617379884035472E-15 ) ) ;
#8962=CARTESIAN_POINT ( 'NONE',  ( 1.224999999999961009, 0.9583333340161364067, -0.7072540797573237947 ) ) ;
#8974=ORIENTED_EDGE ( 'NONE', *, *, #170968, .F. ) ;
#9008=DIRECTION ( 'NONE',  ( 1.276756478318932585E-15, -1.000000000000000000, 1.665334536937738262E-16 ) ) ;
#9018=B_SPLINE_CURVE_WITH_KNOTS ( 'NONE', 3,
 ( #144578, #146697, #210592, #48129 ),
 .UNSPECIFIED., .F., .F.,
 ( 4, 4 ),
 ( 0.000000000000000000, 2.032232339058191815E-05 ),
 .UNSPECIFIED. ) ;
#9020=EDGE_CURVE ( 'NONE', #80420, #5098, #197284, .T. ) ;
#9021=CARTESIAN_POINT ( 'NONE',  ( -0.4465194593918104249, 3.080450244942127380, 0.4155024747329021939 ) ) ;
#9028=CARTESIAN_POINT ( 'NONE',  ( 0.2999999999999999334, 3.950000000000001954, -1.007084189318397938 ) ) ;
#9040=CARTESIAN_POINT ( 'NONE',  ( -0.4032277238576902900, 3.019957635004387075, 0.4115402804778086621 ) ) ;
#9127=B_SPLINE_CURVE_WITH_KNOTS ( 'NONE', 3,
 ( #10160, #28559, #94648, #126138 ),
 .UNSPECIFIED., .F., .F.,
 ( 4, 4 ),
 ( 0.000000000000000000, 0.0007717018656778090215 ),
 .UNSPECIFIED. ) ;
#9144=ORIENTED_EDGE ( 'NONE', *, *, #76230, .F. ) ;
#9176=CARTESIAN_POINT ( 'NONE',  ( -0.6801582343750334214, 0.3802083336747336118, -1.178068619123869398 ) ) ;
#9200=CARTESIAN_POINT ( 'NONE',  ( -1.225000000000038058, -0.7291666666666354324, 0.7072540797572717253 ) ) ;
#9393=FACE_OUTER_BOUND ( 'NONE', #101495, .T. ) ;
#9407=CARTESIAN_POINT ( 'NONE',  ( 1.224999999999995204, 0.1249999999999862332, -6.938893903907228378E-15 ) ) ;
#9452=ORIENTED_EDGE ( 'NONE', *, *, #128228, .T. ) ;
#9463=CARTESIAN_POINT ( 'NONE',  ( -1.772826578343107640, 3.949999999999974420, 0.4499999999999487188 ) ) ;
#9494=CARTESIAN_POINT ( 'NONE',  ( -1.360316468750032870, 0.6614583336747411613, 0.7853790794158620470 ) ) ;
#9530=DIRECTION ( 'NONE',  ( -1.000000000000000000, 7.771561172376097755E-16, 4.440892098500627148E-16 ) ) ;
#9562=CARTESIAN_POINT ( 'NONE',  ( 1.224999999999947020, 2.354166666666675400, 0.7072540797573036997 ) ) ;
#9598=ORIENTED_EDGE ( 'NONE', *, *, #62818, .F. ) ;
#9619=CARTESIAN_POINT ( 'NONE',  ( -2.440293211016301606E-15, 1.187499999999993117, -1.225000000000025624 ) ) ;
#9639=DIRECTION ( 'NONE',  ( 1.276756478318932585E-15, -1.000000000000000000, 1.665334536937738262E-16 ) ) ;
#9706=CARTESIAN_POINT ( 'NONE',  ( 0.3999999999999889200, 3.372708439410121439, -0.5000000000000368594 ) ) ;
#9716=CARTESIAN_POINT ( 'NONE',  ( -1.360316468749999119, 0.3906250003414130090, -8.673617379884035472E-15 ) ) ;
#9748=ORIENTED_EDGE ( 'NONE', *, *, #70626, .T. ) ;
#9817=FACE_OUTER_BOUND ( 'NONE', #2900, .T. ) ;
#9946=CARTESIAN_POINT ( 'NONE',  ( 1.360316468749957597, 1.776041667008106506, 0.7853790794158801436 ) ) ;
#9981=DIRECTION ( 'NONE',  ( -1.276756478318932191E-15, 1.000000000000000000, -3.330669073875483426E-16 ) ) ;
#10022=ADVANCED_FACE ( 'NONE', ( #42888 ), #108997, .T. ) ;
#10024=CARTESIAN_POINT ( 'NONE',  ( -1.225000000000038058, 0.08333333401614038960, 0.7072540797572558491 ) ) ;
#10058=AXIS2_PLACEMENT_3D ( 'NONE', #199237, #133233, #99634 ) ;
#10108=DIRECTION ( 'NONE',  ( -1.276756478318932585E-15, 1.000000000000000000, -1.665334536937738262E-16 ) ) ;
#10142=VECTOR ( 'NONE', #195719, 1000.000000000000000 ) ;
#10160=CARTESIAN_POINT ( 'NONE',  ( 1.814759087649916003, 3.975067388631702059, -0.4606438099578838985 ) ) ;
#10180=( BOUNDED_CURVE ( )  B_SPLINE_CURVE ( 2, ( #213393, #68202, #50917, #65017, #165735, #162554, #67133, #33594, #17322 ),
 .UNSPECIFIED., .F., .T. ) 
 B_SPLINE_CURVE_WITH_KNOTS ( ( 3, 2, 2, 2, 3 ),
 ( 0.1093749999999998473, 0.1145833333333333287, 0.1250000000000000000, 0.1354166666666666574, 0.1406250000000001943 ),
 .UNSPECIFIED. ) 
 CURVE ( )  GEOMETRIC_REPRESENTATION_ITEM ( )  RATIONAL_B_SPLINE_CURVE ( ( 0.9330127018922194093, 0.9330127018922174109, 1.000000000000000000, 0.8660254037844387076, 1.000000000000000000, 0.8660254037844387076, 1.000000000000000000, 0.9330127018922168558, 0.9330127018922194093 ) ) 
 REPRESENTATION_ITEM ( '' )  );
#10237=CARTESIAN_POINT ( 'NONE',  ( 0.6801582343749970061, 0.8385416670080649837, -1.178068619123841643 ) ) ;
#10259=CARTESIAN_POINT ( 'NONE',  ( -3.355169270512988773E-14, -0.8124999999999558131, -1.414508159514601626 ) ) ;
#10354=ORIENTED_EDGE ( 'NONE', *, *, #144993, .T. ) ;
#10436=CARTESIAN_POINT ( 'NONE',  ( 0.3978093821460239599, 3.011896635411783318, -0.3978093821461178292 ) ) ;
#10460=CARTESIAN_POINT ( 'NONE',  ( -5.229199737892074420E-15, 0.06250000000001598721, 1.224999999999961009 ) ) ;
#10545=CARTESIAN_POINT ( 'NONE',  ( -1.225000000000024736, 2.562500000682817358, -1.908195823574487804E-14 ) ) ;
#10614=MECHANICAL_DESIGN_GEOMETRIC_PRESENTATION_REPRESENTATION('',(#239),#138667);
#10636=ORIENTED_EDGE ( 'NONE', *, *, #5066, .T. ) ;
#10646=CARTESIAN_POINT ( 'NONE',  ( -0.6801582343750403048, 2.463541667008038782, 1.178068619123829430 ) ) ;
#10669=CARTESIAN_POINT ( 'NONE',  ( -0.6311622855796981124, 3.299999999999983391, 0.3999999999999715450 ) ) ;
#10675=CARTESIAN_POINT ( 'NONE',  ( -0.6125000000000262457, 1.208333333333311277, -1.060881119635962211 ) ) ;
#10768=EDGE_CURVE ( 'NONE', #125996, #182627, #104485, .T. ) ;
#10771=CARTESIAN_POINT ( 'NONE',  ( -1.360316468750013108, 1.140625000341413564, -2.081668171172168513E-14 ) ) ;
#10804=CARTESIAN_POINT ( 'NONE',  ( 1.896367326442722989, 3.293421909012314686, -0.4056650308922483128 ) ) ;
#10815=CARTESIAN_POINT ( 'NONE',  ( 0.6124999999999862776, 2.333333333333325932, 1.060881119635898040 ) ) ;
#10862=ORIENTED_EDGE ( 'NONE', *, *, #211148, .T. ) ;
#10905=DIRECTION ( 'NONE',  ( 0.000000000000000000, 0.000000000000000000, 1.000000000000000000 ) ) ;
#10938=ORIENTED_EDGE ( 'NONE', *, *, #88956, .T. ) ;
#10962=EDGE_CURVE ( 'NONE', #38441, #175466, #186729, .T. ) ;
#11001=CARTESIAN_POINT ( 'NONE',  ( 1.360316468749941610, 2.276041667008116942, 0.7853790794158921340 ) ) ;
#11037=CARTESIAN_POINT ( 'NONE',  ( -0.6801582343750316451, 2.098958333674738608, -1.178068619123862515 ) ) ;
#11181=ORIENTED_EDGE ( 'NONE', *, *, #81383, .T. ) ;
#11214=CARTESIAN_POINT ( 'NONE',  ( -1.045839947578414805E-15, 1.812499999999992673, 1.224999999999988987 ) ) ;
#11221=CARTESIAN_POINT ( 'NONE',  ( 1.772826578343079884, 3.999999999999976019, 0.4499999999999729772 ) ) ;
#11224=VECTOR ( 'NONE', #73435, 1000.000000000000000 ) ;
#11293=CARTESIAN_POINT ( 'NONE',  ( 0.2999999999999877764, 3.322650755865456773, -0.5865692111442898371 ) ) ;
#11299=CARTESIAN_POINT ( 'NONE',  ( 1.360316468749989793, 0.8177083336747339448, -0.7853790794159001276 ) ) ;
#11320=CARTESIAN_POINT ( 'NONE',  ( -1.225000000000004086, -0.2708333333333212689, -0.7072540797572958171 ) ) ;
#11341=DIRECTION ( 'NONE',  ( 0.000000000000000000, 0.000000000000000000, 1.000000000000000000 ) ) ;
#11362=CARTESIAN_POINT ( 'NONE',  ( 0.4288785890452541105, 3.049942316455306113, 0.4196807566830256797 ) ) ;
#11427=EDGE_LOOP ( 'NONE', ( #37506, #127124, #157490, #49976 ) ) ;
#11493=EDGE_CURVE ( 'NONE', #16624, #13808, #3343, .T. ) ;
#11537=AXIS2_PLACEMENT_3D ( 'NONE', #9463, #141646, #207655 ) ;
#11615=CARTESIAN_POINT ( 'NONE',  ( -1.225000000000048050, 2.791666667349440800, -0.7072540797572958171 ) ) ;
#11617=CARTESIAN_POINT ( 'NONE',  ( -5.229199737892074420E-15, 0.06250000000001598721, 1.224999999999961009 ) ) ;
#11718=CARTESIAN_POINT ( 'NONE',  ( 0.6801582343749883464, 2.588541667008101399, -1.178068619123865846 ) ) ;
#11840=CARTESIAN_POINT ( 'NONE',  ( 0.6801582343750038895, 0.3072916670080680368, -1.178068619123848526 ) ) ;
#11854=CARTESIAN_POINT ( 'NONE',  ( 0.4041367621137400001, 3.038026290190015022, -0.4210133165200654615 ) ) ;
#11875=( BOUNDED_SURFACE ( )  B_SPLINE_SURFACE ( 3, 2, ( 
 ( #892, #180740, #181790 ),
 ( #194858, #16082, #64852 ),
 ( #95256, #148259, #66959 ),
 ( #130999, #114742, #48626 ) ),
 .UNSPECIFIED., .F., .F., .F. ) 
 B_SPLINE_SURFACE_WITH_KNOTS ( ( 4, 4 ),
 ( 3, 3 ),
 ( 1.570796326794896558, 2.636531018672050752 ),
 ( 0.000000000000000000, 1.000000000000000000 ),
 .UNSPECIFIED. ) 
 GEOMETRIC_REPRESENTATION_ITEM ( )  RATIONAL_B_SPLINE_SURFACE ( (
 ( 1.000000000000000000, 0.7071067811865960895, 1.000000000000000000),
 ( 1.000000000000000000, 0.8161930835858371980, 1.000000000000000000),
 ( 1.000000000000000000, 0.8980788380693774942, 1.000000000000000000),
 ( 1.000000000000000000, 0.9374448844494288613, 1.000000000000000000) ) ) 
 REPRESENTATION_ITEM ( '' )  SURFACE ( )  );
#11925=CARTESIAN_POINT ( 'NONE',  ( -0.6311622855796981124, 3.199999999999959766, 0.3999999999999542255 ) ) ;
#11955=CARTESIAN_POINT ( 'NONE',  ( -2.255140518769849223E-14, 3.249999999999988898, -4.336808689942017736E-14 ) ) ;
#11974=ORIENTED_EDGE ( 'NONE', *, *, #22906, .T. ) ;
#11995=AXIS2_PLACEMENT_3D ( 'NONE', #121616, #84759, #200617 ) ;
#11998=CARTESIAN_POINT ( 'NONE',  ( 2.207884333776653740E-15, 1.500000000682816914, -1.225000000000019851 ) ) ;
#12050=VERTEX_POINT ( 'NONE', #156507 ) ;
#12079=CARTESIAN_POINT ( 'NONE',  ( -2.353626204688216217E-14, 0.9843750003414547534, 1.570758158831764062 ) ) ;
#12109=CARTESIAN_POINT ( 'NONE',  ( -1.907519672996902838, 3.236073672982390903, -0.4612874649730039911 ) ) ;
#12112=CARTESIAN_POINT ( 'NONE',  ( 1.360316468749992236, 2.765625000341414896, -4.683753385137379155E-14 ) ) ;
#12179=CARTESIAN_POINT ( 'NONE',  ( 0.2999999999999981570, 4.050057683544640241, 0.8916696671245876171 ) ) ;
#12260=VERTEX_POINT ( 'NONE', #11293 ) ;
#12364=CARTESIAN_POINT ( 'NONE',  ( -1.360316468750048635, -0.5989583329919208055, -0.7853790794159082322 ) ) ;
#12368=EDGE_LOOP ( 'NONE', ( #184683, #94107, #112603, #60116 ) ) ;
#12407=DIRECTION ( 'NONE',  ( 1.276756478318932585E-15, -1.000000000000000000, 1.665334536937738262E-16 ) ) ;
#12430=B_SPLINE_CURVE_WITH_KNOTS ( 'NONE', 3,
 ( #41626, #71936, #172680, #106653 ),
 .UNSPECIFIED., .F., .F.,
 ( 4, 4 ),
 ( -3.662496629072134259E-08, 0.0006801242851315174049 ),
 .UNSPECIFIED. ) ;
#12487=VECTOR ( 'NONE', #136922, 1000.000000000000000 ) ;
#12529=ORIENTED_EDGE ( 'NONE', *, *, #76048, .T. ) ;
#12577=CARTESIAN_POINT ( 'NONE',  ( -6.972266317189433020E-16, 1.750000000682810475, -1.225000000000013634 ) ) ;
#12611=PRESENTATION_STYLE_ASSIGNMENT (( #180461 ) ) ;
#12659=ORIENTED_EDGE ( 'NONE', *, *, #199415, .T. ) ;
#12673=CARTESIAN_POINT ( 'NONE',  ( -1.360316468750034868, -0.8802083329919301313, -0.7853790794159242195 ) ) ;
#12773=CARTESIAN_POINT ( 'NONE',  ( 1.360316468749961594, 2.026041667008099623, 0.7853790794158520550 ) ) ;
#12817=CARTESIAN_POINT ( 'NONE',  ( 1.874158809982156670, 3.299964346911599122, 0.3999999999999681033 ) ) ;
#12899=CARTESIAN_POINT ( 'NONE',  ( -1.360316468750032870, 0.6614583336747411613, 0.7853790794158620470 ) ) ;
#12920=VERTEX_POINT ( 'NONE', #196213 ) ;
#12983=ORIENTED_EDGE ( 'NONE', *, *, #167761, .F. ) ;
#12999=ORIENTED_EDGE ( 'NONE', *, *, #158482, .F. ) ;
#13036=CARTESIAN_POINT ( 'NONE',  ( 0.4465194593917843902, 3.080450244942134486, 0.4155024747329351120 ) ) ;
#13041=EDGE_CURVE ( 'NONE', #78057, #62036, #180828, .T. ) ;
#13047=EDGE_LOOP ( 'NONE', ( #78155, #136377, #87269, #184872 ) ) ;
#13122=ADVANCED_FACE ( 'NONE', ( #210308 ), #111832, .T. ) ;
#13125=DIRECTION ( 'NONE',  ( -1.276756478318932585E-15, 1.000000000000000000, -1.665334536937738262E-16 ) ) ;
#13141=CARTESIAN_POINT ( 'NONE',  ( 1.360316468749939833, 0.02604166700813021276, 0.7853790794158660438 ) ) ;
#13151=ORIENTED_EDGE ( 'NONE', *, *, #240, .T. ) ;
#13182=CARTESIAN_POINT ( 'NONE',  ( 0.6801582343749883464, 2.473958333674766585, 1.178068619123824323 ) ) ;
#13202=ORIENTED_EDGE ( 'NONE', *, *, #124581, .T. ) ;
#13323=CARTESIAN_POINT ( 'NONE',  ( -0.4000000000000045186, 3.099999999999991651, -0.3423093779010097926 ) ) ;
#13404=ORIENTED_EDGE ( 'NONE', *, *, #158984, .F. ) ;
#13439=CARTESIAN_POINT ( 'NONE',  ( -1.360316468750028651, -0.5781249996585913209, -4.510281037539698445E-14 ) ) ;
#13569=ORIENTED_EDGE ( 'NONE', *, *, #183782, .F. ) ;
#13575=CARTESIAN_POINT ( 'NONE',  ( 0.4499999999999747535, 3.949999999999988187, 0.4999999999999674705 ) ) ;
#13745=CARTESIAN_POINT ( 'NONE',  ( -1.225000000000005640, 2.812500000682796486, -1.734723475976807094E-15 ) ) ;
#13747=CARTESIAN_POINT ( 'NONE',  ( -0.5236421425768283955, -3.124072594479749216E-14, 1.213415396354516673 ) ) ;
#13758=CARTESIAN_POINT ( 'NONE',  ( -5.810221930991193690E-16, 2.125000000682803147, 1.224999999999976774 ) ) ;
#13808=VERTEX_POINT ( 'NONE', #154457 ) ;
#13841=CARTESIAN_POINT ( 'NONE',  ( 1.360316468749955598, 1.526041667008097402, 0.7853790794158861388 ) ) ;
#13891=FACE_OUTER_BOUND ( 'NONE', #80347, .T. ) ;
#13964=CARTESIAN_POINT ( 'NONE',  ( -1.360316468750002894, 0.4114583336747319464, 0.7853790794158961308 ) ) ;
#14096=ORIENTED_EDGE ( 'NONE', *, *, #76230, .T. ) ;
#14145=CARTESIAN_POINT ( 'NONE',  ( 0.3999999999999922506, 3.949999999999971756, -0.8338124244296082344 ) ) ;
#14169=DIRECTION ( 'NONE',  ( 1.000000000000000000, 0.000000000000000000, 0.000000000000000000 ) ) ;
#14191=CARTESIAN_POINT ( 'NONE',  ( -1.360316468750042862, 0.9010416670080622081, -0.7853790794159041244 ) ) ;
#14252=ADVANCED_FACE ( 'NONE', ( #103316 ), #157417, .T. ) ;
#14326=AXIS2_PLACEMENT_3D ( 'NONE', #208233, #59865, #126017 ) ;
#14388=ORIENTED_EDGE ( 'NONE', *, *, #212165, .T. ) ;
#14483=CARTESIAN_POINT ( 'NONE',  ( -0.3544712801349463871, 3.975028838742713511, 0.9637995819943760978 ) ) ;
#14494=CARTESIAN_POINT ( 'NONE',  ( 0.6801582343749987825, 2.723958333674732391, 1.178068619123836314 ) ) ;
#14510=DIRECTION ( 'NONE',  ( 3.330669073875478989E-16, -3.540251991789410786E-16, -1.000000000000000000 ) ) ;
#14656=EDGE_LOOP ( 'NONE', ( #210394, #166395, #203395, #156257, #149531, #1371, #5109, #8407 ) ) ;
#14684=ADVANCED_FACE ( 'NONE', ( #193899 ), #192822, .T. ) ;
#14741=( NAMED_UNIT ( * ) SI_UNIT ( $, .STERADIAN. ) SOLID_ANGLE_UNIT ( ) );
#14804=ORIENTED_EDGE ( 'NONE', *, *, #199216, .F. ) ;
#14805=CARTESIAN_POINT ( 'NONE',  ( 1.360316468749994012, -0.9843749996586090845, -5.204170427930421283E-15 ) ) ;
#14834=DIRECTION ( 'NONE',  ( 1.276756478318932585E-15, -1.000000000000000000, 1.665334536937738262E-16 ) ) ;
#14900=CARTESIAN_POINT ( 'NONE',  ( -0.6801582343750438575, 1.630208333674734611, -1.178068619123879834 ) ) ;
#14984=( BOUNDED_CURVE ( )  B_SPLINE_CURVE ( 2, ( #213662, #65287, #197436, #131434, #212615, #30700, #64255, #129346, #29627 ),
 .UNSPECIFIED., .F., .T. ) 
 B_SPLINE_CURVE_WITH_KNOTS ( ( 3, 2, 2, 2, 3 ),
 ( 0.2968749999999997780, 0.3020833333333333148, 0.3125000000000000000, 0.3229166666666666852, 0.3281250000000001665 ),
 .UNSPECIFIED. ) 
 CURVE ( )  GEOMETRIC_REPRESENTATION_ITEM ( )  RATIONAL_B_SPLINE_CURVE ( ( 0.9330127018922194093, 0.9330127018922165227, 1.000000000000000000, 0.8660254037844387076, 1.000000000000000000, 0.8660254037844387076, 1.000000000000000000, 0.9330127018922171889, 0.9330127018922194093 ) ) 
 REPRESENTATION_ITEM ( '' )  );
#15006=ORIENTED_EDGE ( 'NONE', *, *, #116999, .F. ) ;
#15030=CARTESIAN_POINT ( 'NONE',  ( 0.6801582343749883464, -0.6927083329919120347, -1.178068619123862515 ) ) ;
#15144=ADVANCED_FACE ( 'NONE', ( #114845 ), #134267, .T. ) ;
#15150=CARTESIAN_POINT ( 'NONE',  ( -1.878188943807104661, 3.299815425349231557, -0.4000000000000339395 ) ) ;
#15219=CARTESIAN_POINT ( 'NONE',  ( 0.3999999999999977462, 3.963633530850342090, -0.9046180958551371942 ) ) ;
#15263=CARTESIAN_POINT ( 'NONE',  ( -1.360316468750038643, 0.4427083336747321130, 0.7853790794158701516 ) ) ;
#15300=CARTESIAN_POINT ( 'NONE',  ( 0.6801582343749987825, 2.723958333674732391, 1.178068619123836314 ) ) ;
#15339=DIRECTION ( 'NONE',  ( 0.000000000000000000, -0.5005768354468319581, 0.8656921114426510133 ) ) ;
#15383=VERTEX_POINT ( 'NONE', #32468 ) ;
#15389=AXIS2_PLACEMENT_3D ( 'NONE', #125071, #142336, #110930 ) ;
#15430=AXIS2_PLACEMENT_3D ( 'NONE', #164391, #149202, #213116 ) ;
#15441=DIRECTION ( 'NONE',  ( -1.276756478318932585E-15, 1.000000000000000000, -1.665334536937738262E-16 ) ) ;
#15476=CARTESIAN_POINT ( 'NONE',  ( -0.3645075752536049429, 3.999999999999980904, -0.9782388703847658684 ) ) ;
#15489=CARTESIAN_POINT ( 'NONE',  ( 0.3769810270647828698, 3.049942316455306113, 0.4288785890452298522 ) ) ;
#15555=CARTESIAN_POINT ( 'NONE',  ( -2.954552044183079750E-14, 2.578125000341414452, -1.570758158831808249 ) ) ;
#15625=DIRECTION ( 'NONE',  ( -1.000000000000000000, 7.771561172376097755E-16, 4.440892098500627148E-16 ) ) ;
#15653=EDGE_CURVE ( 'NONE', #190021, #127784, #160437, .T. ) ;
#15810=CARTESIAN_POINT ( 'NONE',  ( 1.360316468749961816, 2.817708333674743493, -0.7853790794159141164 ) ) ;
#15849=DIRECTION ( 'NONE',  ( 1.276756478318932585E-15, -1.000000000000000000, 1.665334536937738262E-16 ) ) ;
#15850=ORIENTED_EDGE ( 'NONE', *, *, #100912, .T. ) ;
#15925=ORIENTED_EDGE ( 'NONE', *, *, #152973, .F. ) ;
#15965=CARTESIAN_POINT ( 'NONE',  ( -4.957638175832625493E-14, 1.734375000341442208, 1.570758158831756068 ) ) ;
#15992=ORIENTED_EDGE ( 'NONE', *, *, #129225, .F. ) ;
#16024=AXIS2_PLACEMENT_3D ( 'NONE', #62734, #29185, #193800 ) ;
#16028=DIRECTION ( 'NONE',  ( 0.000000000000000000, 0.000000000000000000, -1.000000000000000000 ) ) ;
#16082=CARTESIAN_POINT ( 'NONE',  ( -0.3728825314829133375, 3.227879828479718327, -0.5317689764002342390 ) ) ;
#16092=CARTESIAN_POINT ( 'NONE',  ( -1.360316468750024876, -0.5885416663252728275, 0.7853790794158701516 ) ) ;
#16115=CARTESIAN_POINT ( 'NONE',  ( -1.360316468750013108, 1.390625000341414008, -3.469446951953614189E-15 ) ) ;
#16249=B_SPLINE_CURVE_WITH_KNOTS ( 'NONE', 3,
 ( #178446, #75603, #127646, #207724 ),
 .UNSPECIFIED., .F., .F.,
 ( 4, 4 ),
 ( 0.000000000000000000, 0.0007717018656778088046 ),
 .UNSPECIFIED. ) ;
#16316=SURFACE_SIDE_STYLE ('',( #84538 ) ) ;
#16318=CARTESIAN_POINT ( 'NONE',  ( -1.360316468750021768, 0.1718750003414371008, -3.295974604355933479E-14 ) ) ;
#16362=CARTESIAN_POINT ( 'NONE',  ( 1.360316468749963592, 1.286458333674703969, -0.7853790794158961308 ) ) ;
#16370=CARTESIAN_POINT ( 'NONE',  ( -6.972266317189433020E-16, 1.750000000682810475, -1.225000000000013634 ) ) ;
#16388=DIRECTION ( 'NONE',  ( -3.330669073875478989E-16, 3.330669073875478989E-16, 1.000000000000000000 ) ) ;
#16389=ORIENTED_EDGE ( 'NONE', *, *, #15653, .F. ) ;
#16466=ORIENTED_EDGE ( 'NONE', *, *, #199193, .F. ) ;
#16477=CARTESIAN_POINT ( 'NONE',  ( 0.3999999999999681033, 3.372708439410100567, 0.4999999999999501510 ) ) ;
#16523=DIRECTION ( 'NONE',  ( -1.276756478318932585E-15, 1.000000000000000000, -1.665334536937738262E-16 ) ) ;
#16554=DIRECTION ( 'NONE',  ( 3.330669073875478989E-16, -3.540251991789410786E-16, -1.000000000000000000 ) ) ;
#16620=CARTESIAN_POINT ( 'NONE',  ( 0.6801582343749970061, -0.4947916663252532876, 1.178068619123832983 ) ) ;
#16624=VERTEX_POINT ( 'NONE', #202952 ) ;
#16664=ORIENTED_EDGE ( 'NONE', *, *, #27793, .T. ) ;
#16670=CARTESIAN_POINT ( 'NONE',  ( 0.4499999999999712563, 3.949999999999981526, -6.938893903907228378E-15 ) ) ;
#16754=LINE ( 'NONE', #101215, #176720 ) ;
#16763=CARTESIAN_POINT ( 'NONE',  ( 3.486133158594716510E-16, 2.437499999999986677, -1.225000000000021849 ) ) ;
#16767=DIRECTION ( 'NONE',  ( 1.276756478318932585E-15, -1.000000000000000000, 1.665334536937738262E-16 ) ) ;
#16784=LINE ( 'NONE', #99141, #93936 ) ;
#16912=CARTESIAN_POINT ( 'NONE',  ( -1.326716514427061987E-15, 2.999999999999988454, -1.225000000000003864 ) ) ;
#16958=DIRECTION ( 'NONE',  ( 3.330669073875478989E-16, -4.632576442341012461E-16, -1.000000000000000000 ) ) ;
#17035=CARTESIAN_POINT ( 'NONE',  ( 1.360316468749992236, 1.546875000341396689, -1.040834085586084257E-14 ) ) ;
#17164=CARTESIAN_POINT ( 'NONE',  ( -0.6801582343750438575, -0.5677083329919535570, 1.178068619123803451 ) ) ;
#17185=CARTESIAN_POINT ( 'NONE',  ( -1.360316468750040642, 1.911458333674787236, 0.7853790794158660438 ) ) ;
#17286=ORIENTED_EDGE ( 'NONE', *, *, #152973, .T. ) ;
#17310=CARTESIAN_POINT ( 'NONE',  ( -1.510657702057710340E-15, 1.375000000682792267, 1.224999999999963229 ) ) ;
#17322=CARTESIAN_POINT ( 'NONE',  ( -1.743066579297358008E-15, 2.250000000682787160, -1.225000000000020739 ) ) ;
#17325=ORIENTED_EDGE ( 'NONE', *, *, #31532, .F. ) ;
#17367=VERTEX_POINT ( 'NONE', #170222 ) ;
#17385=CARTESIAN_POINT ( 'NONE',  ( 0.6801582343749883464, -0.7447916663252535097, 1.178068619123796568 ) ) ;
#17424=CARTESIAN_POINT ( 'NONE',  ( -0.6801582343750368631, 1.682291667008048552, 1.178068619123803451 ) ) ;
#17432=CARTESIAN_POINT ( 'NONE',  ( -1.225000000000016076, 1.812500000682795598, -2.081668171172168513E-14 ) ) ;
#17490=DIRECTION ( 'NONE',  ( -1.276756478318932585E-15, 1.000000000000000000, -1.665334536937738262E-16 ) ) ;
#17504=CARTESIAN_POINT ( 'NONE',  ( -1.326716514427061987E-15, 2.999999999999988454, -1.225000000000003864 ) ) ;
#17515=DIRECTION ( 'NONE',  ( -3.330669073875479482E-16, 3.330669073875479482E-16, 1.000000000000000000 ) ) ;
#17550=ORIENTED_EDGE ( 'NONE', *, *, #204483, .T. ) ;
#17681=CARTESIAN_POINT ( 'NONE',  ( -1.360316468750040642, 2.161458333674780352, 0.7853790794158861388 ) ) ;
#17842=CARTESIAN_POINT ( 'NONE',  ( 0.3999999999999825362, 3.248764396332278981, -0.4641653677813217804 ) ) ;
#17932=CARTESIAN_POINT ( 'NONE',  ( -3.755786496842897795E-14, 2.109375000341444206, -1.570758158831810247 ) ) ;
#17955=CARTESIAN_POINT ( 'NONE',  ( 1.224999999999971001, 1.354166666666710483, 0.7072540797572898219 ) ) ;
#17976=ORIENTED_EDGE ( 'NONE', *, *, #188508, .F. ) ;
#17995=CARTESIAN_POINT ( 'NONE',  ( 0.4205683736966560615, 3.129384673317399113, 0.4296503687815094175 ) ) ;
#18007=CARTESIAN_POINT ( 'NONE',  ( -1.162044386198238935E-15, 2.625000000682799151, 1.224999999999985656 ) ) ;
#18028=DIRECTION ( 'NONE',  ( 0.5005768354468328463, -0.8656921114426504582, 6.106226635438361958E-16 ) ) ;
#18104=CARTESIAN_POINT ( 'NONE',  ( -1.360316468750038865, 0.4427083336747321130, 0.7853790794158700406 ) ) ;
#18136=CARTESIAN_POINT ( 'NONE',  ( -0.4000000000000322742, 3.950000000000009059, 1.007084189318363077 ) ) ;
#18149=CARTESIAN_POINT ( 'NONE',  ( 1.278248824818062671E-15, 1.062499999999996003, 1.224999999999968781 ) ) ;
#18160=EDGE_LOOP ( 'NONE', ( #178324, #187270, #20793, #194947 ) ) ;
#18213=ORIENTED_EDGE ( 'NONE', *, *, #202175, .T. ) ;
#18233=CARTESIAN_POINT ( 'NONE',  ( 0.6801582343749744686, -0.7760416663252778235, 1.178068619123799898 ) ) ;
#18256=CARTESIAN_POINT ( 'NONE',  ( 1.360316468749953600, 1.786458333674746601, -0.7853790794159161148 ) ) ;
#18275=LINE ( 'NONE', #120136, #687 ) ;
#18425=DIRECTION ( 'NONE',  ( -1.000000000000000000, 0.000000000000000000, 0.000000000000000000 ) ) ;
#18426=CARTESIAN_POINT ( 'NONE',  ( -1.225000000000042277, 0.2291666666666811181, -0.7072540797573237947 ) ) ;
#18444=CARTESIAN_POINT ( 'NONE',  ( 0.6125000000000071498, 1.583333333333325488, 1.060881119635915359 ) ) ;
#18462=CARTESIAN_POINT ( 'NONE',  ( -1.151774525698488676E-14, -0.7656249996585936524, 1.570758158831776052 ) ) ;
#18504=CARTESIAN_POINT ( 'NONE',  ( -1.360316468750042862, 1.869791667008058544, -0.7853790794158961308 ) ) ;
#18785=CARTESIAN_POINT ( 'NONE',  ( -1.225000000000033396, 1.000000000000021760, -2.775557561562891351E-14 ) ) ;
#18793=CARTESIAN_POINT ( 'NONE',  ( 0.6124999999999707345, 1.895833334016133742, 1.060881119635880721 ) ) ;
#18803=CARTESIAN_POINT ( 'NONE',  ( -1.626862140677534470E-15, 1.125000000682806034, 1.224999999999975886 ) ) ;
#18823=CARTESIAN_POINT ( 'NONE',  ( -1.772826578343107640, 3.949999999999974420, 0.4499999999999487188 ) ) ;
#18926=CARTESIAN_POINT ( 'NONE',  ( -1.225000000000044276, 1.083333334016145066, 0.7072540797572517413 ) ) ;
#19005=CARTESIAN_POINT ( 'NONE',  ( -1.997444822565112910, 3.480956003829108081, -0.4000000000000817901 ) ) ;
#19008=CARTESIAN_POINT ( 'NONE',  ( 0.6801582343749761339, 1.838541667008058988, -1.178068619123876282 ) ) ;
#19029=CARTESIAN_POINT ( 'NONE',  ( -0.6125000000000089262, 1.041666666666662966, 1.060881119635898040 ) ) ;
#19043=CARTESIAN_POINT ( 'NONE',  ( -0.4170821662629279336, 3.033599471985628959, -0.4170821662629279336 ) ) ;
#19046=ADVANCED_FACE ( 'NONE', ( #100279 ), #144822, .T. ) ;
#19071=CARTESIAN_POINT ( 'NONE',  ( 0.3000000002817697631, 3.198312376128888967, 0.5146719259195579044 ) ) ;
#19180=CARTESIAN_POINT ( 'NONE',  ( 1.360316468749987573, 0.2760416670081234369, 0.7853790794158700406 ) ) ;
#19296=CARTESIAN_POINT ( 'NONE',  ( -0.4423565646247712979, 3.073250980203129146, 0.4181372721655218783 ) ) ;
#19301=TOROIDAL_SURFACE ( 'NONE', #119576, 0.05000000000000000278, 0.05000000000000000278 ) ;
#19312=VECTOR ( 'NONE', #139927, 1000.000000000000114 ) ;
#19329=CARTESIAN_POINT ( 'NONE',  ( -1.360316468749990459, 1.890625000341386475, -2.428612866367529932E-14 ) ) ;
#19345=DIRECTION ( 'NONE',  ( 3.330669073875478989E-16, -3.540251991789410786E-16, -1.000000000000000000 ) ) ;
#19399=CARTESIAN_POINT ( 'NONE',  ( -1.752700365193352367E-14, 2.687499999999996447, -1.414508159514589636 ) ) ;
#19415=CARTESIAN_POINT ( 'NONE',  ( -1.908029163539614492, 3.237038651130966116, -0.4603255239806567367 ) ) ;
#19528=CARTESIAN_POINT ( 'NONE',  ( 1.360316468749955598, -0.9739583329918906074, 0.7853790794158580502 ) ) ;
#19574=CARTESIAN_POINT ( 'NONE',  ( 1.360316468749957597, 1.265625000341379147, -5.030698080332740574E-14 ) ) ;
#19796=ORIENTED_EDGE ( 'NONE', *, *, #135923, .F. ) ;
#19817=ADVANCED_FACE ( 'NONE', ( #46526 ), #2408, .F. ) ;
#19858=CARTESIAN_POINT ( 'NONE',  ( -0.3282377607281401488, 0.9486645496846495274, -1.225000000000020961 ) ) ;
#19866=CARTESIAN_POINT ( 'NONE',  ( 1.224999999999961009, 1.708333334016139959, -0.7072540797573118043 ) ) ;
#19889=DIRECTION ( 'NONE',  ( 1.276756478318932585E-15, -1.000000000000000000, 1.665334536937738262E-16 ) ) ;
#20071=CARTESIAN_POINT ( 'NONE',  ( -0.6801582343750403048, 2.463541667008038782, 1.178068619123829430 ) ) ;
#20089=( BOUNDED_SURFACE ( )  B_SPLINE_SURFACE ( 3, 2, ( 
 ( #135548, #100893, #50021 ),
 ( #53218, #103040, #55352 ),
 ( #138750, #58549, #7645 ),
 ( #153927, #204768, #203705 ) ),
 .UNSPECIFIED., .F., .F., .T. ) 
 B_SPLINE_SURFACE_WITH_KNOTS ( ( 4, 4 ),
 ( 3, 3 ),
 ( 0.0002736160683302337414, 0.001000278046670503461 ),
 ( 0.000000000000000000, 1.000000000000000000 ),
 .UNSPECIFIED. ) 
 GEOMETRIC_REPRESENTATION_ITEM ( )  RATIONAL_B_SPLINE_SURFACE ( (
 ( 1.000000000000000000, 0.6273451206645834777, 1.000000000000000000),
 ( 1.000000000000000000, 0.6198151287834121614, 1.000000000000000000),
 ( 1.000000000000000000, 0.6183718462547956873, 1.000000000000000000),
 ( 1.000000000000000000, 0.6222643257228424041, 1.000000000000000000) ) ) 
 REPRESENTATION_ITEM ( '' )  SURFACE ( )  );
#20095=CARTESIAN_POINT ( 'NONE',  ( 1.224999999999967004, 0.3958333333333378667, -0.7072540797573018123 ) ) ;
#20133=ORIENTED_EDGE ( 'NONE', *, *, #117402, .T. ) ;
#20201=ORIENTED_EDGE ( 'NONE', *, *, #190484, .F. ) ;
#20244=CARTESIAN_POINT ( 'NONE',  ( -0.6801582343750316451, 0.2135416670080853008, 1.178068619123807004 ) ) ;
#20315=ORIENTED_EDGE ( 'NONE', *, *, #145048, .T. ) ;
#20360=CARTESIAN_POINT ( 'NONE',  ( 1.224999999999998757, 0.9375000006827949317, -8.673617379884035472E-15 ) ) ;
#20364=CARTESIAN_POINT ( 'NONE',  ( -0.4320269763655096851, 3.055387103097219281, 0.4199383792806183902 ) ) ;
#20395=CARTESIAN_POINT ( 'NONE',  ( 0.6801582343749796866, 1.473958333674751930, 1.178068619123789462 ) ) ;
#20478=DIRECTION ( 'NONE',  ( 0.9692622846690300831, 0.000000000000000000, 0.2460297208025325477 ) ) ;
#20498=CARTESIAN_POINT ( 'NONE',  ( -1.907692715643321657, 3.236394383240515982, 0.4609675857477188998 ) ) ;
#20555=CARTESIAN_POINT ( 'NONE',  ( -1.352083138863443345E-14, -0.6249999993171989621, 1.414508159514555441 ) ) ;
#20572=DIRECTION ( 'NONE',  ( 1.276756478318932585E-15, -1.000000000000000000, 1.665334536937738262E-16 ) ) ;
#20589=CARTESIAN_POINT ( 'NONE',  ( -1.752700365193352367E-14, -0.2656249996585993145, 1.570758158831780271 ) ) ;
#20626=CARTESIAN_POINT ( 'NONE',  ( 0.6801582343749831283, 1.057291667008075642, -1.178068619123862515 ) ) ;
#20664=EDGE_CURVE ( 'NONE', #143294, #38441, #64824, .T. ) ;
#20769=FACE_OUTER_BOUND ( 'NONE', #70562, .T. ) ;
#20785=CARTESIAN_POINT ( 'NONE',  ( -0.4000000000000080158, 4.050057683544674880, -0.8916696671246466810 ) ) ;
#20793=ORIENTED_EDGE ( 'NONE', *, *, #43786, .F. ) ;
#20916=CARTESIAN_POINT ( 'NONE',  ( 1.224999999999979661, 1.437500000682781387, -2.602085213965210642E-14 ) ) ;
#20944=DIRECTION ( 'NONE',  ( -1.000000000000000000, 7.771561172376097755E-16, 4.440892098500627148E-16 ) ) ;
#21017=EDGE_CURVE ( 'NONE', #22696, #198538, #31552, .T. ) ;
#21021=ORIENTED_EDGE ( 'NONE', *, *, #149834, .F. ) ;
#21034=CARTESIAN_POINT ( 'NONE',  ( 0.3405876332337732237, 3.079852035184926784, -0.4461735512528454684 ) ) ;
#21120=CARTESIAN_POINT ( 'NONE',  ( 1.360316468749992236, 1.546875000341396689, -1.040834085586084257E-14 ) ) ;
#21145=CARTESIAN_POINT ( 'NONE',  ( 1.224999999999982991, 1.395833333333318382, -0.7072540797572817173 ) ) ;
#21240=CARTESIAN_POINT ( 'NONE',  ( -9.296355089585910693E-16, 2.750000000682797818, -1.225000000000007860 ) ) ;
#21289=CARTESIAN_POINT ( 'NONE',  ( 0.3000000000000009881, 3.214163249644255593, -0.5238375172407520042 ) ) ;
#21300=CARTESIAN_POINT ( 'NONE',  ( 0.5980308150947402090, 0.002692760363722866267, 1.225484906753091519 ) ) ;
#21405=ORIENTED_EDGE ( 'NONE', *, *, #183143, .T. ) ;
#21415=CARTESIAN_POINT ( 'NONE',  ( -0.4304495291404314417, 3.052659083096569415, 0.4198826858263652873 ) ) ;
#21440=FACE_OUTER_BOUND ( 'NONE', #84457, .T. ) ;
#21444=CARTESIAN_POINT ( 'NONE',  ( -0.6801582343750247617, 0.09895833367471601472, -1.178068619123872729 ) ) ;
#21497=VECTOR ( 'NONE', #182075, 1000.000000000000000 ) ;
#21534=ADVANCED_FACE ( 'NONE', ( #203399 ), #163745, .T. ) ;
#21555=CARTESIAN_POINT ( 'NONE',  ( 1.034320804586478904, -6.966782166145887105E-15, -0.7758101520237091764 ) ) ;
#21556=AXIS2_PLACEMENT_3D ( 'NONE', #178138, #147771, #132607 ) ;
#21557=AXIS2_PLACEMENT_3D ( 'NONE', #32804, #16523, #113060 ) ;
#21594=CARTESIAN_POINT ( 'NONE',  ( 1.224999999999958789, 1.916666667349501196, 0.7072540797572717253 ) ) ;
#21601=CARTESIAN_POINT ( 'NONE',  ( -3.755786496842897795E-14, -0.2499999993171491686, -1.414508159514577423 ) ) ;
#21634=CARTESIAN_POINT ( 'NONE',  ( 1.360316468749981800, -0.4739583329918962695, 0.7853790794158760358 ) ) ;
#21669=CARTESIAN_POINT ( 'NONE',  ( 1.360316468749985575, 2.036458333674739940, -0.7853790794159022370 ) ) ;
#21708=DIRECTION ( 'NONE',  ( 0.000000000000000000, 0.000000000000000000, 1.000000000000000000 ) ) ;
#21731=ADVANCED_FACE ( 'NONE', ( #5194, #186100 ), #181044, .F. ) ;
#21743=CARTESIAN_POINT ( 'NONE',  ( 1.224999999999965006, 0.4166666673494940354, 0.7072540797572456350 ) ) ;
#21814=AXIS2_PLACEMENT_3D ( 'NONE', #11955, #92185, #8762 ) ;
#21883=VERTEX_POINT ( 'NONE', #205547 ) ;
#21891=FACE_OUTER_BOUND ( 'NONE', #204676, .T. ) ;
#21941=EDGE_LOOP ( 'NONE', ( #147627, #127454, #39084, #9598 ) ) ;
#21976=CARTESIAN_POINT ( 'NONE',  ( 0.6124999999999932720, 1.979166667349464781, -1.060881119635938008 ) ) ;
#22001=CARTESIAN_POINT ( 'NONE',  ( -1.734723475976807094E-15, 2.999999999999988898, -6.938893903907228378E-15 ) ) ;
#22081=VERTEX_POINT ( 'NONE', #73418 ) ;
#22092=ADVANCED_FACE ( 'NONE', ( #154687 ), #74505, .F. ) ;
#22133=CARTESIAN_POINT ( 'NONE',  ( -0.6125000000000349054, 2.208333333333325932, -1.060881119635983083 ) ) ;
#22188=CARTESIAN_POINT ( 'NONE',  ( 0.6801582343749917881, 1.255208333674727506, 1.178068619123834759 ) ) ;
#22206=EDGE_CURVE ( 'NONE', #211791, #63320, #93168, .T. ) ;
#22211=CARTESIAN_POINT ( 'NONE',  ( -1.225000000000042277, 0.9791666666666765106, -0.7072540797572898219 ) ) ;
#22225=CIRCLE ( 'NONE', #119114, 1.224999999999996980 ) ;
#22308=CARTESIAN_POINT ( 'NONE',  ( 1.224999999999971223, 2.708333334016145066, -0.7072540797573039217 ) ) ;
#22369=CARTESIAN_POINT ( 'NONE',  ( 1.360316468749957597, 0.3177083336747154596, -0.7853790794158961308 ) ) ;
#22376=PLANE ( 'NONE',  #58063 ) ;
#22494=AXIS2_PLACEMENT_3D ( 'NONE', #123476, #201400, #90896 ) ;
#22518=CARTESIAN_POINT ( 'NONE',  ( 0.6801582343749900117, 0.05729166700808169255, -1.178068619123848526 ) ) ;
#22519=EDGE_CURVE ( 'NONE', #101381, #30345, #145932, .T. ) ;
#22541=ADVANCED_FACE ( 'NONE', ( #132874 ), #53679, .F. ) ;
#22543=VECTOR ( 'NONE', #24749, 1000.000000000000000 ) ;
#22593=CARTESIAN_POINT ( 'NONE',  ( 0.6125000000000071498, 1.583333333333325488, 1.060881119635915359 ) ) ;
#22636=CARTESIAN_POINT ( 'NONE',  ( 0.1071175833137206629, -7.075894077951318707E-15, -1.231310646603006376 ) ) ;
#22672=DIRECTION ( 'NONE',  ( 3.330669073875479482E-16, -3.330669073875479482E-16, -1.000000000000000000 ) ) ;
#22679=CARTESIAN_POINT ( 'NONE',  ( 1.224999999999971001, -0.08333333265048434302, 0.7072540797572797189 ) ) ;
#22696=VERTEX_POINT ( 'NONE', #2805 ) ;
#22744=CARTESIAN_POINT ( 'NONE',  ( 0.6801582343749796866, 1.723958333674766141, 1.178068619123784355 ) ) ;
#22752=CARTESIAN_POINT ( 'NONE',  ( -3.956095110007851991E-14, 0.3281250003414356020, -1.570758158831788265 ) ) ;
#22846=CARTESIAN_POINT ( 'NONE',  ( -1.874158809982213958, 3.299964346911606228, -0.4000000000000374922 ) ) ;
#22906=EDGE_CURVE ( 'NONE', #53788, #47983, #27465, .T. ) ;
#22975=CARTESIAN_POINT ( 'NONE',  ( 0.6801582343749952297, 2.255208333674735499, 1.178068619123839866 ) ) ;
#23033=VERTEX_POINT ( 'NONE', #54790 ) ;
#23055=CARTESIAN_POINT ( 'NONE',  ( 0.6124999999999723999, 1.145833334016146843, 1.060881119635889380 ) ) ;
#23067=ORIENTED_EDGE ( 'NONE', *, *, #84896, .F. ) ;
#23083=FACE_OUTER_BOUND ( 'NONE', #61280, .T. ) ;
#23166=VERTEX_POINT ( 'NONE', #102216 ) ;
#23267=CARTESIAN_POINT ( 'NONE',  ( -0.6801582343750438575, 0.6302083336747199560, -1.178068619123869398 ) ) ;
#23292=CARTESIAN_POINT ( 'NONE',  ( 0.6124999999999846123, -0.08333333333329639991, -1.060881119635962211 ) ) ;
#23311=ORIENTED_EDGE ( 'NONE', *, *, #85916, .T. ) ;
#23329=ORIENTED_EDGE ( 'NONE', *, *, #117424, .T. ) ;
#23595=CARTESIAN_POINT ( 'NONE',  ( 0.6801582343749917881, 0.7239583336747443809, 1.178068619123793015 ) ) ;
#23669=CARTESIAN_POINT ( 'NONE',  ( 0.6124999999999898304, 1.916666666666677621, -1.060881119635962211 ) ) ;
#23683=CARTESIAN_POINT ( 'NONE',  ( -1.772826578343107640, 3.949999999999974420, 0.4499999999999487188 ) ) ;
#23703=CARTESIAN_POINT ( 'NONE',  ( -1.911686719268548496, 3.274494700676831904, 0.4236673858377323909 ) ) ;
#23761=CARTESIAN_POINT ( 'NONE',  ( 0.6124999999999637401, -0.3541666659838821341, 1.060881119635891157 ) ) ;
#23768=DIRECTION ( 'NONE',  ( -1.084202172485508576E-15, 0.5005768354468290715, 0.8656921114426525676 ) ) ;
#23826=CARTESIAN_POINT ( 'NONE',  ( 1.360316468749992236, 2.015625000341400685, -1.040834085586084257E-14 ) ) ;
#23857=AXIS2_PLACEMENT_3D ( 'NONE', #77589, #176177, #29921 ) ;
#23896=DIRECTION ( 'NONE',  ( -1.000000000000000000, 7.771561172376097755E-16, 4.440892098500627148E-16 ) ) ;
#23916=ORIENTED_EDGE ( 'NONE', *, *, #28302, .F. ) ;
#23953=VERTEX_POINT ( 'NONE', #11362 ) ;
#24004=CARTESIAN_POINT ( 'NONE',  ( 2.207884333776653740E-15, 1.500000000682816914, -1.225000000000019851 ) ) ;
#24011=CIRCLE ( 'NONE', #145132, 1.914481421317578258 ) ;
#24045=CARTESIAN_POINT ( 'NONE',  ( -1.326716514427061987E-15, 2.999999999999988454, -1.225000000000003864 ) ) ;
#24055=CARTESIAN_POINT ( 'NONE',  ( -1.360316468750011332, 2.421875000341397577, -1.387778780781445676E-14 ) ) ;
#24065=ORIENTED_EDGE ( 'NONE', *, *, #158984, .T. ) ;
#24131=CARTESIAN_POINT ( 'NONE',  ( -0.6125000000000383471, 0.6041666673494219264, 1.060881119635901593 ) ) ;
#24220=CARTESIAN_POINT ( 'NONE',  ( 0.3282377607281200538, 0.5736645496846195513, 1.224999999999978995 ) ) ;
#24336=CARTESIAN_POINT ( 'NONE',  ( -0.6801582343750177673, 0.9635416670080582113, 1.178068619123796568 ) ) ;
#24357=CARTESIAN_POINT ( 'NONE',  ( -0.6125000000000314637, -0.2916666666666761776, -1.060881119635948444 ) ) ;
#24558=AXIS2_PLACEMENT_3D ( 'NONE', #13575, #28774, #211765 ) ;
#24662=CARTESIAN_POINT ( 'NONE',  ( -1.360316468750040642, 1.161458333674751486, 0.7853790794158861388 ) ) ;
#24737=CARTESIAN_POINT ( 'NONE',  ( -1.225000000000010747, 1.500000000000008216, -8.673617379884035472E-15 ) ) ;
#24749=DIRECTION ( 'NONE',  ( 1.276756478318932585E-15, -1.000000000000000000, 1.665334536937738262E-16 ) ) ;
#24773=CARTESIAN_POINT ( 'NONE',  ( 1.360316468749951602, 2.526041667008118274, 0.7853790794158560518 ) ) ;
#24876=LINE ( 'NONE', #58461, #149401 ) ;
#24891=CARTESIAN_POINT ( 'NONE',  ( -4.957638175832625493E-14, 2.078125000341435769, -1.570758158831802254 ) ) ;
#24971=CARTESIAN_POINT ( 'NONE',  ( -0.3000000000000157541, 3.214163249644056197, -0.5238375172406551927 ) ) ;
#25001=ORIENTED_EDGE ( 'NONE', *, *, #155697, .T. ) ;
#25124=CARTESIAN_POINT ( 'NONE',  ( 1.224999999999934808, 0.7083333340161593883, -0.7072540797573136917 ) ) ;
#25126=CARTESIAN_POINT ( 'NONE',  ( -4.156403723172807449E-14, 1.859375000341410678, -1.570758158831802254 ) ) ;
#25137=CARTESIAN_POINT ( 'NONE',  ( 1.224999999999991651, 2.437500000682837786, -4.336808689942017736E-14 ) ) ;
#25206=CARTESIAN_POINT ( 'NONE',  ( -4.957638175832625493E-14, 0.3750000006828378418, 1.414508159514567431 ) ) ;
#25285=CARTESIAN_POINT ( 'NONE',  ( -0.4205683736966763231, 3.129384673317354704, 0.4296503687815398376 ) ) ;
#25378=VECTOR ( 'NONE', #61416, 1000.000000000000000 ) ;
#25383=VECTOR ( 'NONE', #59680, 1000.000000000000000 ) ;
#25419=CARTESIAN_POINT ( 'NONE',  ( -1.360316468749996677, 0.4010416670080598767, -0.7853790794158941324 ) ) ;
#25440=CARTESIAN_POINT ( 'NONE',  ( 0.6124999999999707345, -0.5833333333332968440, -1.060881119635976200 ) ) ;
#25548=ORIENTED_EDGE ( 'NONE', *, *, #147413, .T. ) ;
#25609=EDGE_CURVE ( 'NONE', #102463, #142570, #114138, .T. ) ;
#25732=CARTESIAN_POINT ( 'NONE',  ( -3.956095110007852622E-14, 0.3281250003414356020, -1.570758158831788265 ) ) ;
#25760=AXIS2_PLACEMENT_3D ( 'NONE', #7193, #5047, #154542 ) ;
#25804=CARTESIAN_POINT ( 'NONE',  ( -0.6125000000000140332, 2.041666666666650087, 1.060881119635936232 ) ) ;
#25815=CARTESIAN_POINT ( 'NONE',  ( 0.4999999999999761302, 3.172938907704328404, 0.3999999999999750422 ) ) ;
#25958=ORIENTED_EDGE ( 'NONE', *, *, #1238, .T. ) ;
#25962=CARTESIAN_POINT ( 'NONE',  ( 0.6801582343749831283, 1.223958333674737720, 1.178068619123822547 ) ) ;
#25970=CARTESIAN_POINT ( 'NONE',  ( -5.758872628492442907E-14, 0.4531250003414521998, 1.570758158831760287 ) ) ;
#26035=CARTESIAN_POINT ( 'NONE',  ( 1.772826578343088544, 3.950000000000001954, -0.4500000000000284883 ) ) ;
#26100=DIRECTION ( 'NONE',  ( -1.276756478318932585E-15, 1.000000000000000000, -1.665334536937738262E-16 ) ) ;
#26194=CARTESIAN_POINT ( 'NONE',  ( 1.360316468749961816, 2.026041667008099179, 0.7853790794158520550 ) ) ;
#26229=PLANE ( 'NONE',  #46553 ) ;
#26271=CARTESIAN_POINT ( 'NONE',  ( 0.6124999999999741762, 0.1458333340161460656, 1.060881119635889380 ) ) ;
#26287=CYLINDRICAL_SURFACE ( 'NONE', #14326, 0.05000000000000002359 ) ;
#26366=( BOUNDED_CURVE ( )  B_SPLINE_CURVE ( 2, ( #213515, #113992, #182087, #100850, #48923, #65137, #197283, #134464, #115044 ),
 .UNSPECIFIED., .F., .T. ) 
 B_SPLINE_CURVE_WITH_KNOTS ( ( 3, 2, 2, 2, 3 ),
 ( 0.6093749999999996669, 0.6145833333333333703, 0.6250000000000000000, 0.6354166666666666297, 0.6406250000000002220 ),
 .UNSPECIFIED. ) 
 CURVE ( )  GEOMETRIC_REPRESENTATION_ITEM ( )  RATIONAL_B_SPLINE_CURVE ( ( 0.9330127018922194093, 0.9330127018922150794, 1.000000000000000000, 0.8660254037844387076, 1.000000000000000000, 0.8660254037844387076, 1.000000000000000000, 0.9330127018922165227, 0.9330127018922194093 ) ) 
 REPRESENTATION_ITEM ( '' )  );
#26423=CYLINDRICAL_SURFACE ( 'NONE', #56395, 1.224999999999996980 ) ;
#26460=DIRECTION ( 'NONE',  ( -3.330669073875481947E-16, 4.742150360713068815E-16, 1.000000000000000000 ) ) ;
#26488=CARTESIAN_POINT ( 'NONE',  ( -1.360316468750032870, 0.9427083336747503761, 0.7853790794158641564 ) ) ;
#26510=CARTESIAN_POINT ( 'NONE',  ( -1.225000000000028066, -0.2499999999999724665, -4.510281037539698445E-14 ) ) ;
#26664=CARTESIAN_POINT ( 'NONE',  ( 0.4379653042624709336, 3.065656782498147770, -0.4195809500674644865 ) ) ;
#26802=CARTESIAN_POINT ( 'NONE',  ( 0.6801582343749883464, -0.6927083329919120347, -1.178068619123862515 ) ) ;
#26904=CARTESIAN_POINT ( 'NONE',  ( 1.360316468749971586, 2.567708333674758148, -0.7853790794159302147 ) ) ;
#26930=ORIENTED_EDGE ( 'NONE', *, *, #183143, .F. ) ;
#27009=DIRECTION ( 'NONE',  ( -1.000000000000000000, -8.104628079763641167E-15, 0.000000000000000000 ) ) ;
#27024=CARTESIAN_POINT ( 'NONE',  ( -0.6801582343750161019, 0.6822916670080614310, 1.178068619123810334 ) ) ;
#27061=CYLINDRICAL_SURFACE ( 'NONE', #201019, 1.224999999999996980 ) ;
#27112=AXIS2_PLACEMENT_3D ( 'NONE', #104778, #91743, #205446 ) ;
#27131=DIRECTION ( 'NONE',  ( -1.000000000000000000, 0.000000000000000000, 4.440892098500751393E-16 ) ) ;
#27258=CARTESIAN_POINT ( 'NONE',  ( 0.6801582343749883464, 2.588541667008101399, -1.178068619123865846 ) ) ;
#27283=ORIENTED_EDGE ( 'NONE', *, *, #66555, .T. ) ;
#27295=CARTESIAN_POINT ( 'NONE',  ( -1.360316468750040642, 2.161458333674780352, 0.7853790794158861388 ) ) ;
#27339=ORIENTED_EDGE ( 'NONE', *, *, #205468, .F. ) ;
#27344=CARTESIAN_POINT ( 'NONE',  ( -1.225000000000022293, 0.2916666673494853756, -0.7072540797573118043 ) ) ;
#27358=ORIENTED_EDGE ( 'NONE', *, *, #43686, .T. ) ;
#27429=DIRECTION ( 'NONE',  ( -3.330669073875485398E-16, 1.665334536937734071E-16, 1.000000000000000000 ) ) ;
#27465=CIRCLE ( 'NONE', #183007, 0.9475805310473219834 ) ;
#27474=CARTESIAN_POINT ( 'NONE',  ( 1.225000000000000311, 1.874999999999994671, -1.734723475976807094E-15 ) ) ;
#27561=CARTESIAN_POINT ( 'NONE',  ( -0.6801582343750334214, 1.213541667008023683, 1.178068619123810334 ) ) ;
#27576=CYLINDRICAL_SURFACE ( 'NONE', #164598, 1.224999999999996980 ) ;
#27582=CARTESIAN_POINT ( 'NONE',  ( -1.360316468750013108, 2.921875000341411788, -1.734723475976807094E-14 ) ) ;
#27738=EDGE_LOOP ( 'NONE', ( #82038, #130191, #36784, #207268 ) ) ;
#27793=EDGE_CURVE ( 'NONE', #141010, #68973, #45732, .T. ) ;
#27877=CARTESIAN_POINT ( 'NONE',  ( 0.6801582343749952297, -0.9427083329919122567, -1.178068619123855409 ) ) ;
#27958=DIRECTION ( 'NONE',  ( 0.000000000000000000, 0.000000000000000000, 1.000000000000000000 ) ) ;
#27970=CARTESIAN_POINT ( 'NONE',  ( -0.5445930744354052777, 3.250057683544617326, 0.3999999999999455103 ) ) ;
#27990=CARTESIAN_POINT ( 'NONE',  ( -0.4000000000000131783, 3.372708439410149417, -0.5000000000000160982 ) ) ;
#28039=VECTOR ( 'NONE', #108177, 1000.000000000000000 ) ;
#28105=CARTESIAN_POINT ( 'NONE',  ( -0.6801582343750143256, 0.3489583336747370534, -1.178068619123865846 ) ) ;
#28139=ORIENTED_EDGE ( 'NONE', *, *, #138594, .F. ) ;
#28152=CARTESIAN_POINT ( 'NONE',  ( 1.224999999999974332, 2.374999999999988454, -3.295974604355933479E-14 ) ) ;
#28207=DIRECTION ( 'NONE',  ( 0.2460297208025344073, -9.436895709313838482E-16, 0.9692622846690297500 ) ) ;
#28302=EDGE_CURVE ( 'NONE', #154544, #150426, #199787, .T. ) ;
#28319=VERTEX_POINT ( 'NONE', #133780 ) ;
#28336=CARTESIAN_POINT ( 'NONE',  ( -0.6801582343750022241, 1.130208333674734167, -1.178068619123841643 ) ) ;
#28443=CIRCLE ( 'NONE', #38950, 1.857347330825974252 ) ;
#28537=CARTESIAN_POINT ( 'NONE',  ( -0.6125000000000019318, 1.270833334016133076, -1.060881119635938008 ) ) ;
#28552=CARTESIAN_POINT ( 'NONE',  ( -0.3282377607281340426, 2.113835450998172050, 1.224999999999984768 ) ) ;
#28559=CARTESIAN_POINT ( 'NONE',  ( 1.946706258587953764, 3.753940929402488358, -0.4616008842494966902 ) ) ;
#28569=CARTESIAN_POINT ( 'NONE',  ( 0.3999999999999698241, 3.999999999999968914, -0.5000000000000368594 ) ) ;
#28639=CARTESIAN_POINT ( 'NONE',  ( 1.360316468749957597, -0.2239583329919110355, 0.7853790794158921340 ) ) ;
#28766=ADVANCED_FACE ( 'NONE', ( #155327 ), #68833, .T. ) ;
#28774=DIRECTION ( 'NONE',  ( 3.330669073875479482E-16, -3.330669073875479482E-16, -1.000000000000000000 ) ) ;
#28862=CARTESIAN_POINT ( 'NONE',  ( 1.874158809982156670, 3.299964346911599122, 0.3999999999999681033 ) ) ;
#28904=CARTESIAN_POINT ( 'NONE',  ( -0.3585786437627347389, 3.975028841772314969, 0.9637995837462216553 ) ) ;
#28921=CARTESIAN_POINT ( 'NONE',  ( 0.4999999999999900080, 3.949999999999974420, 0.4999999999999640288 ) ) ;
#28948=VERTEX_POINT ( 'NONE', #98605 ) ;
#28949=CARTESIAN_POINT ( 'NONE',  ( -1.360316468750040642, -0.3802083329919277999, -0.7853790794159161148 ) ) ;
#29007=( BOUNDED_CURVE ( )  B_SPLINE_CURVE ( 3, ( #19043, #637, #85122, #68850 ),
 .UNSPECIFIED., .F., .T. ) 
 B_SPLINE_CURVE_WITH_KNOTS ( ( 4, 4 ),
 ( 0.7261627075366219319, 1.570796326795131259 ),
 .UNSPECIFIED. ) 
 CURVE ( )  GEOMETRIC_REPRESENTATION_ITEM ( )  RATIONAL_B_SPLINE_CURVE ( ( 1.000000000000000000, 0.9414278581754867981, 0.9414278581754867981, 1.000000000000000000 ) ) 
 REPRESENTATION_ITEM ( '' )  );
#29103=CARTESIAN_POINT ( 'NONE',  ( 1.907692715643283243, 3.236394383240550621, 0.4609675857477184557 ) ) ;
#29178=CARTESIAN_POINT ( 'NONE',  ( 1.360316468749977581, 0.5364583336746844289, -0.7853790794159001276 ) ) ;
#29185=DIRECTION ( 'NONE',  ( -1.276756478318932191E-15, 1.000000000000000000, -3.330669073875483426E-16 ) ) ;
#29281=CARTESIAN_POINT ( 'NONE',  ( -2.449742653233043743, 3.949999999999981526, -0.4500000000000354272 ) ) ;
#29315=CARTESIAN_POINT ( 'NONE',  ( -1.992711204631002198E-15, 2.999999999999989342, 1.224999999999989875 ) ) ;
#29392=DIRECTION ( 'NONE',  ( 1.000000000000000000, -7.771561172376097755E-16, -4.440892098500627148E-16 ) ) ;
#29413=CARTESIAN_POINT ( 'NONE',  ( 0.2999999999999565237, 3.372708439410121439, 0.4999999999999553690 ) ) ;
#29415=CARTESIAN_POINT ( 'NONE',  ( 0.6801582343749865700, 0.08854166700808518975, -1.178068619123869398 ) ) ;
#29452=CARTESIAN_POINT ( 'NONE',  ( 0.6801582343749987825, 2.557291667008069869, -1.178068619123886718 ) ) ;
#29574=ORIENTED_EDGE ( 'NONE', *, *, #92378, .T. ) ;
#29627=CARTESIAN_POINT ( 'NONE',  ( 2.207884333776653740E-15, 1.500000000682816914, -1.225000000000019851 ) ) ;
#29643=LINE ( 'NONE', #28569, #111790 ) ;
#29662=EDGE_CURVE ( 'NONE', #101381, #74826, #134050, .T. ) ;
#29713=CARTESIAN_POINT ( 'NONE',  ( -1.752700365193352367E-14, -0.3906249996585918205, -1.570758158831796258 ) ) ;
#29742=EDGE_CURVE ( 'NONE', #108528, #45585, #32097, .T. ) ;
#29753=CARTESIAN_POINT ( 'NONE',  ( 0.4999999999999761302, 3.999999999999948042, -0.5000000000000299760 ) ) ;
#29839=EDGE_LOOP ( 'NONE', ( #25548, #127192, #133783, #173581 ) ) ;
#29921=DIRECTION ( 'NONE',  ( -1.000000000000000000, 0.000000000000000000, 5.421010862427519212E-16 ) ) ;
#29922=CARTESIAN_POINT ( 'NONE',  ( 0.4999999999999553690, -1.387778780781445676E-14, -0.5000000000000507372 ) ) ;
#29989=CARTESIAN_POINT ( 'NONE',  ( -1.992711204631002198E-15, 2.999999999999989342, 1.224999999999989875 ) ) ;
#30018=CARTESIAN_POINT ( 'NONE',  ( 0.6801582343749744686, -0.7760416663252778235, 1.178068619123799898 ) ) ;
#30056=DIRECTION ( 'NONE',  ( -2.253752739989063359E-14, 4.419671232041788924E-16, 1.000000000000000000 ) ) ;
#30115=CARTESIAN_POINT ( 'NONE',  ( -4.156403723172807449E-14, 1.859375000341410900, -1.570758158831802254 ) ) ;
#30200=( BOUNDED_CURVE ( )  B_SPLINE_CURVE ( 2, ( #1095, #84499, #166830, #133292, #199298, #101819, #50943, #150589, #86635 ),
 .UNSPECIFIED., .F., .T. ) 
 B_SPLINE_CURVE_WITH_KNOTS ( ( 3, 2, 2, 2, 3 ),
 ( 0.04687499999999977796, 0.05208333333333333565, 0.06250000000000000000, 0.07291666666666667129, 0.07812500000000006939 ),
 .UNSPECIFIED. ) 
 CURVE ( )  GEOMETRIC_REPRESENTATION_ITEM ( )  RATIONAL_B_SPLINE_CURVE ( ( 0.9330127018922194093, 0.9330127018922165227, 1.000000000000000000, 0.8660254037844387076, 1.000000000000000000, 0.8660254037844387076, 1.000000000000000000, 0.9330127018922185211, 0.9330127018922194093 ) ) 
 REPRESENTATION_ITEM ( '' )  );
#30247=CARTESIAN_POINT ( 'NONE',  ( -3.956095110007852622E-14, 0.3281250003414356020, -1.570758158831788265 ) ) ;
#30268=CARTESIAN_POINT ( 'NONE',  ( -1.360316468750006225, 2.640625000341401130, 3.469446951953614189E-15 ) ) ;
#30345=VERTEX_POINT ( 'NONE', #152419 ) ;
#30407=CIRCLE ( 'NONE', #54513, 1.872309607372811158 ) ;
#30458=VERTEX_POINT ( 'NONE', #73281 ) ;
#30483=CARTESIAN_POINT ( 'NONE',  ( 0.6801582343749935644, 0.2552083336747196229, 1.178068619123780802 ) ) ;
#30523=CARTESIAN_POINT ( 'NONE',  ( -1.360316468750052854, 2.661458333674782573, 0.7853790794158581612 ) ) ;
#30589=CYLINDRICAL_SURFACE ( 'NONE', #146562, 0.09999999999999961697 ) ;
#30700=CARTESIAN_POINT ( 'NONE',  ( -1.225000000000030065, 1.541666667349459230, -0.7072540797573017013 ) ) ;
#30713=CARTESIAN_POINT ( 'NONE',  ( 0.4041367621137377242, 3.038026290190030121, 0.4210133165199971828 ) ) ;
#30785=CARTESIAN_POINT ( 'NONE',  ( -1.360316468750024876, -1.057291666325259172, 0.7853790794158601596 ) ) ;
#30829=DIRECTION ( 'NONE',  ( -1.276756478318932585E-15, 1.000000000000000000, -1.665334536937738262E-16 ) ) ;
#30915=VERTEX_POINT ( 'NONE', #174034 ) ;
#31042=DIRECTION ( 'NONE',  ( 1.276756478318932585E-15, -1.000000000000000000, 1.665334536937738262E-16 ) ) ;
#31089=( BOUNDED_SURFACE ( )  B_SPLINE_SURFACE ( 1, 2, ( 
 ( #48360, #114471, #128613, #146933, #100275, #15810, #162102, #210825, #62450, #195663, #194580, #213992, #131762, #96049, #197767, #115524, #145877, #119790, #37404, #68814, #39542, #150108, #20071, #117662, #101335, #5943, #55789, #85089, #67734, #187912, #151173, #72014, #152231, #199891, #120874, #84017, #51537, #105643, #170601, #17932, #201999, #169540, #87226, #133884, #183654, #1680, #86160, #35259, #200942, #53658, #167417, #69876, #19008, #121946, #138127, #3802, #135985, #185771, #134936, #88303, #52591, #118718, #4866, #2744, #184705, #103478, #21120, #203080, #153290, #36327, #102405, #154364, #168473, #70944, #137055, #54725, #186848, #38480, #204136, #104557, #22188, #175967, #27561, #126218, #158640, #75251, #58997, #159700, #173842, #107817, #205220, #174910, #172761, #93657, #24336, #26488, #188987, #77378, #192179, #92598, #10237, #11299, #139190, #190055, #143494, #76312, #209490, #91525, #140283, #142419, #23267, #41707, #108887, #57927, #7014, #56862, #157583, #125153, #89379, #191112, #43840, #25419, #9176, #141364, #155428, #206303, #109956, #73089, #207377, #127291, #171670, #124092, #208428, #61131, #42779, #60062, #123036, #44909, #193262, #40631, #106734, #90444, #156512, #8101, #74191, #210573, #112094, #144563, #32896, #97922, #96864, #28639, #81642, #114225, #65367, #165026, #180223, #98974, #63265, #29713, #94726, #147727, #129427, #198568, #16620, #196471, #95794, #211630, #13439, #12364, #178096, #113156, #111017, #161851, #62207, #78443, #79516, #131514, #197517, #82702, #177022, #146682, #213744, #128364, #45973, #145634, #31845, #115278, #64339, #160771, #179161, #30785, #195411 ),
 ( #49161, #163980, #194331, #47040, #148781, #351, #48113, #162912, #14494, #80584, #181270, #66424, #212698, #130481, #132567, #15555, #7570, #40100, #171154, #154917, #41183, #55280, #203628, #83767, #56346, #54214, #57407, #120352, #122508, #67492, #173312, #73655, #188468, #106212, #107290, #17681, #71501, #189535, #172238, #24891, #187398, #21669, #23826, #116336, #137612, #204696, #153851, #100031, #149860, #39030, #6501, #182326, #72576, #139755, #121428, #105114, #22744, #33955, #87777, #205779, #166093, #88862, #8648, #50217, #5422, #89931, #157060, #138677, #155982, #1428, #140832, #74727, #133637, #202562, #123573, #90997, #186329, #37963, #104036, #170082, #25962, #128887, #193793, #174384, #10771, #194868, #45442, #46502, #126758, #175439, #111556, #58477, #76845, #144036, #93132, #42247, #92067, #192718, #94200, #124632, #160240, #161315, #142964, #44372, #208967, #190590, #27024, #12899, #108360, #60599, #162387, #206845, #159171, #29178, #96331, #110495, #176494, #158125, #80048, #13964, #9716, #75792, #28105, #30247, #11840, #141900, #207910, #59531, #125691, #112625, #177565, #77917, #191650, #95267, #210033, #43315, #109433, #61673, #127841, #78979, #178635, #145098, #211102, #62726, #212167, #113697, #150403, #199106, #1970, #214269, #115815, #181802, #129959, #179701, #63801, #98444, #195947, #131009, #65902, #47583, #82176, #146151, #31317, #97394, #33435, #165569, #17164, #16092, #163450, #132048, #198058, #182879, #15030, #197001, #99512, #901, #18233, #116880, #32378, #164508, #81122, #147207, #34495, #148270, #49687, #83238, #213232, #64864, #149323, #100569, #48636, #114754, #180751 ) ),
 .UNSPECIFIED., .F., .F., .T. ) 
 B_SPLINE_SURFACE_WITH_KNOTS ( ( 2, 2 ),
 ( 3, 2, 2, 2, 2, 2, 2, 2, 2, 2, 2, 2, 2, 2, 2, 2, 2, 2, 2, 2, 2, 2, 2, 2, 2, 2, 2, 2, 2, 2, 2, 2, 2, 2, 2, 2, 2, 2, 2, 2, 2, 2, 2, 2, 2, 2, 2, 2, 2, 2, 2, 2, 2, 2, 2, 2, 2, 2, 2, 2, 2, 2, 2, 2, 2, 2, 2, 2, 2, 2, 2, 2, 2, 2, 2, 2, 2, 2, 2, 2, 2, 2, 2, 2, 2, 2, 2, 2, 2, 2, 2, 2, 2, 2, 2, 2, 3 ),
 ( 0.000000000000000000, 1.000000000000000000 ),
 ( 0.000000000000000000, 0.01041666666666666609, 0.02083333333333333218, 0.03125000000000000000, 0.04166666666666666435, 0.05208333333333333565, 0.06250000000000000000, 0.07291666666666667129, 0.08333333333333332871, 0.09375000000000000000, 0.1041666666666666713, 0.1145833333333333287, 0.1250000000000000000, 0.1354166666666666574, 0.1458333333333333426, 0.1562500000000000000, 0.1666666666666666574, 0.1770833333333333426, 0.1875000000000000000, 0.1979166666666666574, 0.2083333333333333426, 0.2187500000000000000, 0.2291666666666666574, 0.2395833333333333426, 0.2500000000000000000, 0.2604166666666666852, 0.2708333333333333148, 0.2812500000000000000, 0.2916666666666666852, 0.3020833333333333148, 0.3125000000000000000, 0.3229166666666666852, 0.3333333333333333148, 0.3437500000000000000, 0.3541666666666666852, 0.3645833333333333148, 0.3750000000000000000, 0.3854166666666666852, 0.3958333333333333148, 0.4062500000000000000, 0.4166666666666666852, 0.4270833333333333148, 0.4375000000000000000, 0.4479166666666666852, 0.4583333333333333148, 0.4687500000000000000, 0.4791666666666666852, 0.4895833333333333148, 0.5000000000000000000, 0.5104166666666666297, 0.5208333333333333703, 0.5312500000000000000, 0.5416666666666666297, 0.5520833333333333703, 0.5625000000000000000, 0.5729166666666666297, 0.5833333333333333703, 0.5937500000000000000, 0.6041666666666666297, 0.6145833333333333703, 0.6250000000000000000, 0.6354166666666666297, 0.6458333333333333703, 0.6562500000000000000, 0.6666666666666666297, 0.6770833333333333703, 0.6875000000000000000, 0.6979166666666666297, 0.7083333333333333703, 0.7187500000000000000, 0.7291666666666666297, 0.7395833333333333703, 0.7500000000000000000, 0.7604166666666666297, 0.7708333333333333703, 0.7812500000000000000, 0.7916666666666666297, 0.8020833333333333703, 0.8125000000000000000, 0.8229166666666666297, 0.8333333333333333703, 0.8437500000000000000, 0.8541666666666666297, 0.8645833333333333703, 0.8750000000000000000, 0.8854166666666666297, 0.8958333333333333703, 0.9062500000000000000, 0.9166666666666666297, 0.9270833333333333703, 0.9375000000000000000, 0.9479166666666666297, 0.9583333333333333703, 0.9687500000000000000, 0.9791666666666666297, 0.9895833333333333703, 1.000000000000000000 ),
 .UNSPECIFIED. ) 
 GEOMETRIC_REPRESENTATION_ITEM ( )  RATIONAL_B_SPLINE_SURFACE ( (
 ( 1.000000000000000000, 0.8660254037844387076, 1.000000000000000000, 0.8660254037844387076, 1.000000000000000000, 0.8660254037844387076, 1.000000000000000000, 0.8660254037844387076, 1.000000000000000000, 0.8660254037844387076, 1.000000000000000000, 0.8660254037844387076, 1.000000000000000000, 0.8660254037844387076, 1.000000000000000000, 0.8660254037844387076, 1.000000000000000000, 0.8660254037844387076, 1.000000000000000000, 0.8660254037844387076, 1.000000000000000000, 0.8660254037844387076, 1.000000000000000000, 0.8660254037844387076, 1.000000000000000000, 0.8660254037844387076, 1.000000000000000000, 0.8660254037844387076, 1.000000000000000000, 0.8660254037844387076, 1.000000000000000000, 0.8660254037844387076, 1.000000000000000000, 0.8660254037844387076, 1.000000000000000000, 0.8660254037844387076, 1.000000000000000000, 0.8660254037844387076, 1.000000000000000000, 0.8660254037844387076, 1.000000000000000000, 0.8660254037844387076, 1.000000000000000000, 0.8660254037844387076, 1.000000000000000000, 0.8660254037844387076, 1.000000000000000000, 0.8660254037844387076, 1.000000000000000000, 0.8660254037844387076, 1.000000000000000000, 0.8660254037844387076, 1.000000000000000000, 0.8660254037844387076, 1.000000000000000000, 0.8660254037844387076, 1.000000000000000000, 0.8660254037844387076, 1.000000000000000000, 0.8660254037844387076, 1.000000000000000000, 0.8660254037844387076, 1.000000000000000000, 0.8660254037844387076, 1.000000000000000000, 0.8660254037844387076, 1.000000000000000000, 0.8660254037844387076, 1.000000000000000000, 0.8660254037844387076, 1.000000000000000000, 0.8660254037844387076, 1.000000000000000000, 0.8660254037844387076, 1.000000000000000000, 0.8660254037844387076, 1.000000000000000000, 0.8660254037844387076, 1.000000000000000000, 0.8660254037844387076, 1.000000000000000000, 0.8660254037844387076, 1.000000000000000000, 0.8660254037844387076, 1.000000000000000000, 0.8660254037844387076, 1.000000000000000000, 0.8660254037844387076, 1.000000000000000000, 0.8660254037844387076, 1.000000000000000000, 0.8660254037844387076, 1.000000000000000000, 0.8660254037844387076, 1.000000000000000000, 0.8660254037844387076, 1.000000000000000000, 0.8660254037844387076, 1.000000000000000000, 0.8660254037844387076, 1.000000000000000000, 0.8660254037844387076, 1.000000000000000000, 0.8660254037844387076, 1.000000000000000000, 0.8660254037844387076, 1.000000000000000000, 0.8660254037844387076, 1.000000000000000000, 0.8660254037844387076, 1.000000000000000000, 0.8660254037844387076, 1.000000000000000000, 0.8660254037844387076, 1.000000000000000000, 0.8660254037844387076, 1.000000000000000000, 0.8660254037844387076, 1.000000000000000000, 0.8660254037844387076, 1.000000000000000000, 0.8660254037844387076, 1.000000000000000000, 0.8660254037844387076, 1.000000000000000000, 0.8660254037844387076, 1.000000000000000000, 0.8660254037844387076, 1.000000000000000000, 0.8660254037844387076, 1.000000000000000000, 0.8660254037844387076, 1.000000000000000000, 0.8660254037844387076, 1.000000000000000000, 0.8660254037844387076, 1.000000000000000000, 0.8660254037844387076, 1.000000000000000000, 0.8660254037844387076, 1.000000000000000000, 0.8660254037844387076, 1.000000000000000000, 0.8660254037844387076, 1.000000000000000000, 0.8660254037844387076, 1.000000000000000000, 0.8660254037844387076, 1.000000000000000000, 0.8660254037844387076, 1.000000000000000000, 0.8660254037844387076, 1.000000000000000000, 0.8660254037844387076, 1.000000000000000000, 0.8660254037844387076, 1.000000000000000000, 0.8660254037844387076, 1.000000000000000000, 0.8660254037844387076, 1.000000000000000000, 0.8660254037844387076, 1.000000000000000000, 0.8660254037844387076, 1.000000000000000000, 0.8660254037844387076, 1.000000000000000000, 0.8660254037844387076, 1.000000000000000000, 0.8660254037844387076, 1.000000000000000000, 0.8660254037844387076, 1.000000000000000000, 0.8660254037844387076, 1.000000000000000000, 0.8660254037844387076, 1.000000000000000000, 0.8660254037844387076, 1.000000000000000000, 0.8660254037844387076, 1.000000000000000000, 0.8660254037844387076, 1.000000000000000000, 0.8660254037844387076, 1.000000000000000000, 0.8660254037844387076, 1.000000000000000000, 0.8660254037844387076, 1.000000000000000000, 0.8660254037844387076, 1.000000000000000000, 0.8660254037844387076, 1.000000000000000000),
 ( 1.000000000000000000, 0.8660254037844387076, 1.000000000000000000, 0.8660254037844387076, 1.000000000000000000, 0.8660254037844387076, 1.000000000000000000, 0.8660254037844387076, 1.000000000000000000, 0.8660254037844387076, 1.000000000000000000, 0.8660254037844387076, 1.000000000000000000, 0.8660254037844387076, 1.000000000000000000, 0.8660254037844387076, 1.000000000000000000, 0.8660254037844387076, 1.000000000000000000, 0.8660254037844387076, 1.000000000000000000, 0.8660254037844387076, 1.000000000000000000, 0.8660254037844387076, 1.000000000000000000, 0.8660254037844387076, 1.000000000000000000, 0.8660254037844387076, 1.000000000000000000, 0.8660254037844387076, 1.000000000000000000, 0.8660254037844387076, 1.000000000000000000, 0.8660254037844387076, 1.000000000000000000, 0.8660254037844387076, 1.000000000000000000, 0.8660254037844387076, 1.000000000000000000, 0.8660254037844387076, 1.000000000000000000, 0.8660254037844387076, 1.000000000000000000, 0.8660254037844387076, 1.000000000000000000, 0.8660254037844387076, 1.000000000000000000, 0.8660254037844387076, 1.000000000000000000, 0.8660254037844387076, 1.000000000000000000, 0.8660254037844387076, 1.000000000000000000, 0.8660254037844387076, 1.000000000000000000, 0.8660254037844387076, 1.000000000000000000, 0.8660254037844387076, 1.000000000000000000, 0.8660254037844387076, 1.000000000000000000, 0.8660254037844387076, 1.000000000000000000, 0.8660254037844387076, 1.000000000000000000, 0.8660254037844387076, 1.000000000000000000, 0.8660254037844387076, 1.000000000000000000, 0.8660254037844387076, 1.000000000000000000, 0.8660254037844387076, 1.000000000000000000, 0.8660254037844387076, 1.000000000000000000, 0.8660254037844387076, 1.000000000000000000, 0.8660254037844387076, 1.000000000000000000, 0.8660254037844387076, 1.000000000000000000, 0.8660254037844387076, 1.000000000000000000, 0.8660254037844387076, 1.000000000000000000, 0.8660254037844387076, 1.000000000000000000, 0.8660254037844387076, 1.000000000000000000, 0.8660254037844387076, 1.000000000000000000, 0.8660254037844387076, 1.000000000000000000, 0.8660254037844387076, 1.000000000000000000, 0.8660254037844387076, 1.000000000000000000, 0.8660254037844387076, 1.000000000000000000, 0.8660254037844387076, 1.000000000000000000, 0.8660254037844387076, 1.000000000000000000, 0.8660254037844387076, 1.000000000000000000, 0.8660254037844387076, 1.000000000000000000, 0.8660254037844387076, 1.000000000000000000, 0.8660254037844387076, 1.000000000000000000, 0.8660254037844387076, 1.000000000000000000, 0.8660254037844387076, 1.000000000000000000, 0.8660254037844387076, 1.000000000000000000, 0.8660254037844387076, 1.000000000000000000, 0.8660254037844387076, 1.000000000000000000, 0.8660254037844387076, 1.000000000000000000, 0.8660254037844387076, 1.000000000000000000, 0.8660254037844387076, 1.000000000000000000, 0.8660254037844387076, 1.000000000000000000, 0.8660254037844387076, 1.000000000000000000, 0.8660254037844387076, 1.000000000000000000, 0.8660254037844387076, 1.000000000000000000, 0.8660254037844387076, 1.000000000000000000, 0.8660254037844387076, 1.000000000000000000, 0.8660254037844387076, 1.000000000000000000, 0.8660254037844387076, 1.000000000000000000, 0.8660254037844387076, 1.000000000000000000, 0.8660254037844387076, 1.000000000000000000, 0.8660254037844387076, 1.000000000000000000, 0.8660254037844387076, 1.000000000000000000, 0.8660254037844387076, 1.000000000000000000, 0.8660254037844387076, 1.000000000000000000, 0.8660254037844387076, 1.000000000000000000, 0.8660254037844387076, 1.000000000000000000, 0.8660254037844387076, 1.000000000000000000, 0.8660254037844387076, 1.000000000000000000, 0.8660254037844387076, 1.000000000000000000, 0.8660254037844387076, 1.000000000000000000, 0.8660254037844387076, 1.000000000000000000, 0.8660254037844387076, 1.000000000000000000, 0.8660254037844387076, 1.000000000000000000, 0.8660254037844387076, 1.000000000000000000, 0.8660254037844387076, 1.000000000000000000, 0.8660254037844387076, 1.000000000000000000, 0.8660254037844387076, 1.000000000000000000, 0.8660254037844387076, 1.000000000000000000, 0.8660254037844387076, 1.000000000000000000, 0.8660254037844387076, 1.000000000000000000, 0.8660254037844387076, 1.000000000000000000, 0.8660254037844387076, 1.000000000000000000, 0.8660254037844387076, 1.000000000000000000) ) ) 
 REPRESENTATION_ITEM ( '' )  SURFACE ( )  );
#31096=CARTESIAN_POINT ( 'NONE',  ( -0.6125000000000279110, 2.520833334016120197, -1.060881119635969094 ) ) ;
#31098=CARTESIAN_POINT ( 'NONE',  ( -1.225000000000005640, 1.387778780781445676E-14, -1.387778780781445676E-14 ) ) ;
#31109=CARTESIAN_POINT ( 'NONE',  ( -1.743066579297358008E-15, 2.250000000682787160, -1.225000000000020739 ) ) ;
#31125=CARTESIAN_POINT ( 'NONE',  ( -1.734723475976807094E-14, 4.000000000000003553, -1.734723475976807094E-14 ) ) ;
#31157=EDGE_CURVE ( 'NONE', #43349, #55688, #52417, .T. ) ;
#31191=CARTESIAN_POINT ( 'NONE',  ( 0.6801582343749900117, 2.005208333674748822, 1.178068619123818994 ) ) ;
#31236=CARTESIAN_POINT ( 'NONE',  ( -2.905110965495596944E-15, 1.687500000000013101, -1.225000000000019851 ) ) ;
#31240=CARTESIAN_POINT ( 'NONE',  ( 1.911686719268508527, 3.274494700676894077, 0.4236673858377237312 ) ) ;
#31317=CARTESIAN_POINT ( 'NONE',  ( 1.360316468749978469, -0.4843749996586016460, -3.816391647148975608E-14 ) ) ;
#31326=DIRECTION ( 'NONE',  ( -0.8583236685137333177, 0.5131086435338296781, -8.673617379884052827E-15 ) ) ;
#31337=CARTESIAN_POINT ( 'NONE',  ( 0.6125000000000001554, 2.166666666666670960, -1.060881119635941339 ) ) ;
#31372=CARTESIAN_POINT ( 'NONE',  ( 1.981527703613512825, 3.480048614628221681, -0.4617793045968336396 ) ) ;
#31432=CARTESIAN_POINT ( 'NONE',  ( -1.896367326442726542, 3.293421909012321347, -0.4056650308922968851 ) ) ;
#31466=EDGE_CURVE ( 'NONE', #108115, #76056, #29643, .T. ) ;
#31505=CARTESIAN_POINT ( 'NONE',  ( 0.3999999999999896416, 3.999999999999973799, -0.8338124244296082344 ) ) ;
#31528=CARTESIAN_POINT ( 'NONE',  ( 1.772826578343066117, 3.950000000000009059, 0.4499999999999590994 ) ) ;
#31530=VERTEX_POINT ( 'NONE', #163913 ) ;
#31532=EDGE_CURVE ( 'NONE', #17367, #55688, #107650, .T. ) ;
#31548=CARTESIAN_POINT ( 'NONE',  ( -0.6801582343750316451, 0.8802083336747270614, -1.178068619123876282 ) ) ;
#31552=( BOUNDED_CURVE ( )  B_SPLINE_CURVE ( 2, ( #214253, #115796, #102699, #181784, #20360, #150388, #149305, #84303, #86444 ),
 .UNSPECIFIED., .F., .T. ) 
 B_SPLINE_CURVE_WITH_KNOTS ( ( 3, 2, 2, 2, 3 ),
 ( 0.4531250000000002220, 0.4583333333333333148, 0.4687500000000000000, 0.4791666666666666852, 0.4843749999999997780 ),
 .UNSPECIFIED. ) 
 CURVE ( )  GEOMETRIC_REPRESENTATION_ITEM ( )  RATIONAL_B_SPLINE_CURVE ( ( 0.9330127018922194093, 0.9330127018922221849, 1.000000000000000000, 0.8660254037844387076, 1.000000000000000000, 0.8660254037844387076, 1.000000000000000000, 0.9330127018922221849, 0.9330127018922194093 ) ) 
 REPRESENTATION_ITEM ( '' )  );
#31712=EDGE_LOOP ( 'NONE', ( #39299, #105251, #95140, #159344 ) ) ;
#31812=ORIENTED_EDGE ( 'NONE', *, *, #86051, .F. ) ;
#31836=CARTESIAN_POINT ( 'NONE',  ( -0.4000000000000382694, 3.999999999999974243, 0.8338124244295226362 ) ) ;
#31845=CARTESIAN_POINT ( 'NONE',  ( 1.360316468749955821, -0.9531249996585916540, -5.204170427930421283E-14 ) ) ;
#31850=ORIENTED_EDGE ( 'NONE', *, *, #185099, .T. ) ;
#31906=CARTESIAN_POINT ( 'NONE',  ( -5.810221930991193690E-16, 2.500000000682804036, -1.225000000000023626 ) ) ;
#32097=CIRCLE ( 'NONE', #194589, 0.04999999999999991257 ) ;
#32134=ORIENTED_EDGE ( 'NONE', *, *, #115015, .F. ) ;
#32176=FACE_OUTER_BOUND ( 'NONE', #14656, .T. ) ;
#32245=CARTESIAN_POINT ( 'NONE',  ( -1.360316468750042862, 0.9010416670080623192, -0.7853790794159041244 ) ) ;
#32298=DIRECTION ( 'NONE',  ( 3.330669073875478989E-16, -3.540251991789410786E-16, -1.000000000000000000 ) ) ;
#32329=CARTESIAN_POINT ( 'NONE',  ( 0.2999999999999860556, 4.000000000000010658, 1.007084189318397938 ) ) ;
#32378=CARTESIAN_POINT ( 'NONE',  ( -0.6801582343750074422, -0.8177083329919260235, 1.178068619123834759 ) ) ;
#32396=CARTESIAN_POINT ( 'NONE',  ( 0.3282377607281235510, 2.176335450315365350, -1.225000000000017408 ) ) ;
#32399=CARTESIAN_POINT ( 'NONE',  ( 1.360316468749949825, 2.244791667008100511, 0.7853790794158780342 ) ) ;
#32468=CARTESIAN_POINT ( 'NONE',  ( 2.672702088255949078E-15, 1.625000000682787160, 1.224999999999980549 ) ) ;
#32484=CARTESIAN_POINT ( 'NONE',  ( -1.907519672996902838, 3.236073672982390903, -0.4612874649730039911 ) ) ;
#32499=CARTESIAN_POINT ( 'NONE',  ( 3.486133158594716510E-16, 2.437499999999986677, -1.225000000000021849 ) ) ;
#32504=CARTESIAN_POINT ( 'NONE',  ( -1.889772045536167067, 3.296949564223877083, 0.4024211290685098530 ) ) ;
#32520=CARTESIAN_POINT ( 'NONE',  ( 7.785697387528199762E-15, 0.5624999999999894529, 1.224999999999973443 ) ) ;
#32526=ADVANCED_FACE ( 'NONE', ( #184565 ), #153150, .F. ) ;
#32598=CARTESIAN_POINT ( 'NONE',  ( -7.511572993685796537E-15, 0.3593750003414036831, -1.570758158831792262 ) ) ;
#32636=CARTESIAN_POINT ( 'NONE',  ( 1.360316468749973584, 0.7864583336747016373, -0.7853790794159161148 ) ) ;
#32672=ORIENTED_EDGE ( 'NONE', *, *, #177588, .T. ) ;
#32794=ADVANCED_FACE ( 'NONE', ( #104368 ), #72908, .T. ) ;
#32804=CARTESIAN_POINT ( 'NONE',  ( -1.734723475976807094E-14, 4.000000000000003553, -1.734723475976807094E-14 ) ) ;
#32896=CARTESIAN_POINT ( 'NONE',  ( 0.6801582343749970061, -0.1614583329919219712, -1.178068619123852079 ) ) ;
#32939=VECTOR ( 'NONE', #76755, 1000.000000000000000 ) ;
#33044=ORIENTED_EDGE ( 'NONE', *, *, #87216, .T. ) ;
#33171=UNCERTAINTY_MEASURE_WITH_UNIT (LENGTH_MEASURE( 1.000000000000000082E-05 ), #177270, 'distance_accuracy_value', 'NONE');
#33301=CARTESIAN_POINT ( 'NONE',  ( -3.355169270512988773E-14, 1.234375000341463746, 1.570758158831764062 ) ) ;
#33406=( BOUNDED_CURVE ( )  B_SPLINE_CURVE ( 2, ( #168176, #2438, #116284, #1376, #67437 ),
 .UNSPECIFIED., .F., .T. ) 
 B_SPLINE_CURVE_WITH_KNOTS ( ( 3, 2, 3 ),
 ( 0.000000000000000000, 0.01041666666666666609, 0.01562500000000010061 ),
 .UNSPECIFIED. ) 
 CURVE ( )  GEOMETRIC_REPRESENTATION_ITEM ( )  RATIONAL_B_SPLINE_CURVE ( ( 1.000000000000000000, 0.8660254037844387076, 1.000000000000000000, 0.9330127018922180770, 0.9330127018922194093 ) ) 
 REPRESENTATION_ITEM ( '' )  );
#33435=CARTESIAN_POINT ( 'NONE',  ( 0.6801582343749692505, -0.5260416663252707181, 1.178068619123786132 ) ) ;
#33456=CARTESIAN_POINT ( 'NONE',  ( -5.358255402162534516E-14, 1.328125000341440431, -1.570758158831820239 ) ) ;
#33581=DIRECTION ( 'NONE',  ( 4.440892098500630106E-16, 3.330669073875473073E-16, 1.000000000000000000 ) ) ;
#33594=CARTESIAN_POINT ( 'NONE',  ( -0.3282377607281426468, 2.261164550367422255, -1.225000000000034062 ) ) ;
#33603=AXIS2_PLACEMENT_3D ( 'NONE', #210829, #31042, #97118 ) ;
#33653=( NAMED_UNIT ( * ) SI_UNIT ( $, .STERADIAN. ) SOLID_ANGLE_UNIT ( ) );
#33696=CARTESIAN_POINT ( 'NONE',  ( -1.360316468750006669, 1.119791667008071423, -0.7853790794158921340 ) ) ;
#33754=EDGE_LOOP ( 'NONE', ( #9452, #132370, #58261, #112498 ) ) ;
#33955=CARTESIAN_POINT ( 'NONE',  ( -3.755786496842897795E-14, 1.703125000341434214, 1.570758158831776052 ) ) ;
#34023=VERTEX_POINT ( 'NONE', #159246 ) ;
#34060=CARTESIAN_POINT ( 'NONE',  ( -0.4000000000000131783, 3.049942316455299451, 0.4288785890452472271 ) ) ;
#34076=ORIENTED_EDGE ( 'NONE', *, *, #25609, .T. ) ;
#34116=CARTESIAN_POINT ( 'NONE',  ( 0.3728825314828371762, 3.227879828479794710, -0.5317689764002981878 ) ) ;
#34131=EDGE_CURVE ( 'NONE', #30345, #160120, #96375, .T. ) ;
#34225=CARTESIAN_POINT ( 'NONE',  ( -1.225000000000028066, 1.229166666666677843, -0.7072540797573076965 ) ) ;
#34292=FACE_OUTER_BOUND ( 'NONE', #179164, .T. ) ;
#34367=CARTESIAN_POINT ( 'NONE',  ( 1.360316468749987573, 1.817708333674738608, -0.7853790794158981292 ) ) ;
#34383=CARTESIAN_POINT ( 'NONE',  ( -0.5000000000000247580, 3.172938907704287104, 0.3999999999999698241 ) ) ;
#34401=FACE_OUTER_BOUND ( 'NONE', #31712, .T. ) ;
#34413=CARTESIAN_POINT ( 'NONE',  ( 0.6125000000000001554, 1.166666666666656083, -1.060881119635941339 ) ) ;
#34419=CARTESIAN_POINT ( 'NONE',  ( -1.225000000000044276, 0.7916666673494797690, -0.7072540797572998139 ) ) ;
#34450=ORIENTED_EDGE ( 'NONE', *, *, #80889, .T. ) ;
#34486=CARTESIAN_POINT ( 'NONE',  ( -0.6124999999999967137, 1.708333333333339477, -1.060881119635938008 ) ) ;
#34495=CARTESIAN_POINT ( 'NONE',  ( -0.6801582343750161019, -0.9010416663252431846, -1.178068619123869398 ) ) ;
#34518=CARTESIAN_POINT ( 'NONE',  ( -0.6801582343750282034, 1.432291667008027458, 1.178068619123810334 ) ) ;
#34643=CARTESIAN_POINT ( 'NONE',  ( 0.3282377607281028453, 1.386164550367412929, 1.224999999999958566 ) ) ;
#34667=DIRECTION ( 'NONE',  ( 1.276756478318932585E-15, -1.000000000000000000, 1.665334536937738262E-16 ) ) ;
#34678=CARTESIAN_POINT ( 'NONE',  ( 1.224999999999969225, 1.937500000682795820, -2.081668171172168513E-14 ) ) ;
#34680=CARTESIAN_POINT ( 'NONE',  ( -1.162044386198238935E-15, 0.3125000000000180411, 1.224999999999967004 ) ) ;
#34700=LINE ( 'NONE', #183088, #163641 ) ;
#34715=CARTESIAN_POINT ( 'NONE',  ( -0.6801582343750074422, -0.1197916663252529546, -1.178068619123865846 ) ) ;
#34724=DIRECTION ( 'NONE',  ( 1.276756478318932585E-15, -1.000000000000000000, 1.665334536937738262E-16 ) ) ;
#34752=CARTESIAN_POINT ( 'NONE',  ( 1.360316468749969365, 0.7447916670080855228, 0.7853790794158739264 ) ) ;
#35016=CARTESIAN_POINT ( 'NONE',  ( -0.5000000000000229816, 3.999999999999976019, 0.4999999999999553690 ) ) ;
#35039=CARTESIAN_POINT ( 'NONE',  ( -1.225000000000026290, 1.020833333333308834, 0.7072540797572558491 ) ) ;
#35046=CARTESIAN_POINT ( 'NONE',  ( -1.752700365193352367E-14, 1.875000000682780943, 1.414508159514551444 ) ) ;
#35047=CARTESIAN_POINT ( 'NONE',  ( -0.4499999999999833578, 4.000000000000003553, -0.9353126743251295450 ) ) ;
#35051=ORIENTED_EDGE ( 'NONE', *, *, #153089, .F. ) ;
#35178=CARTESIAN_POINT ( 'NONE',  ( -0.6125000000000089262, 0.7083333333333317050, -1.060881119635948444 ) ) ;
#35195=EDGE_CURVE ( 'NONE', #201878, #212450, #109408, .T. ) ;
#35256=CARTESIAN_POINT ( 'NONE',  ( -1.981451431469474223, 3.479816182765814059, -0.4617787996151642149 ) ) ;
#35259=CARTESIAN_POINT ( 'NONE',  ( -1.360316468750048635, 1.942708333674827204, 0.7853790794158580502 ) ) ;
#35283=CARTESIAN_POINT ( 'NONE',  ( 0.6125000000000037081, 0.3333333333333590720, 1.060881119635903147 ) ) ;
#35303=LINE ( 'NONE', #16912, #84311 ) ;
#35323=CARTESIAN_POINT ( 'NONE',  ( 0.3868389748197148537, 3.100956225802592670, 0.4583768147622874212 ) ) ;
#35335=CARTESIAN_POINT ( 'NONE',  ( 1.224999999999929257, 2.208333334016110427, -0.7072540797573095839 ) ) ;
#35341=EDGE_CURVE ( 'NONE', #73414, #6089, #96532, .T. ) ;
#35368=DIRECTION ( 'NONE',  ( 1.276756478318932585E-15, -1.000000000000000000, 1.665334536937738262E-16 ) ) ;
#35387=ORIENTED_EDGE ( 'NONE', *, *, #192096, .T. ) ;
#35434=CARTESIAN_POINT ( 'NONE',  ( 0.5101186646354113341, -1.387778780781445676E-14, 1.261047121698059215 ) ) ;
#35454=EDGE_CURVE ( 'NONE', #43310, #95302, #110682, .T. ) ;
#35460=VERTEX_POINT ( 'NONE', #13036 ) ;
#35468=DIRECTION ( 'NONE',  ( 1.276756478318932585E-15, -1.000000000000000000, 1.665334536937738262E-16 ) ) ;
#35485=CARTESIAN_POINT ( 'NONE',  ( -0.6125000000000383471, 0.7708333340161397373, -1.060881119635972647 ) ) ;
#35577=CARTESIAN_POINT ( 'NONE',  ( 1.224999999999991651, 2.124999999999967137, -3.469446951953614189E-14 ) ) ;
#35580=CARTESIAN_POINT ( 'NONE',  ( -0.6801582343750004478, 2.348958333674739052, -1.178068619123869398 ) ) ;
#35646=ORIENTED_EDGE ( 'NONE', *, *, #197756, .T. ) ;
#35669=CARTESIAN_POINT ( 'NONE',  ( -1.913843478179648727, 3.256154753185184880, -0.4414708703500292430 ) ) ;
#35670=AXIS2_PLACEMENT_3D ( 'NONE', #156382, #76181, #192046 ) ;
#35714=EDGE_CURVE ( 'NONE', #99612, #192043, #172583, .T. ) ;
#35744=CARTESIAN_POINT ( 'NONE',  ( 1.224999999999955014, 1.958333334016109095, -0.7072540797573237947 ) ) ;
#35750=CARTESIAN_POINT ( 'NONE',  ( 0.6124999999999723999, -0.1041666659838680342, 1.060881119635899816 ) ) ;
#35769=DIRECTION ( 'NONE',  ( 1.276756478318932585E-15, -1.000000000000000000, 1.665334536937738262E-16 ) ) ;
#35785=CARTESIAN_POINT ( 'NONE',  ( -1.752700365193352367E-14, -0.3906249996585918205, -1.570758158831796258 ) ) ;
#35816=AXIS2_PLACEMENT_3D ( 'NONE', #26035, #141972, #207984 ) ;
#35825=CARTESIAN_POINT ( 'NONE',  ( -1.360316468750044638, 1.411458333674720622, 0.7853790794158801436 ) ) ;
#35863=EDGE_CURVE ( 'NONE', #59826, #169074, #79181, .T. ) ;
#35864=PRODUCT_DEFINITION ( 'UNKNOWN', '', #204417, #50390 ) ;
#36110=CIRCLE ( 'NONE', #202136, 1.857347330825974252 ) ;
#36116=CARTESIAN_POINT ( 'NONE',  ( -1.225000000000030065, 1.541666667349459230, -0.7072540797573018123 ) ) ;
#36290=CARTESIAN_POINT ( 'NONE',  ( 1.872228381520318896, 3.299999999999997158, 0.3999999999999958589 ) ) ;
#36327=CARTESIAN_POINT ( 'NONE',  ( -6.960724307482170605E-14, 1.484375000341481066, 1.570758158831758289 ) ) ;
#36349=CARTESIAN_POINT ( 'NONE',  ( -1.225000000000033396, 1.000000000000021760, -2.775557561562891351E-14 ) ) ;
#36393=CARTESIAN_POINT ( 'NONE',  ( -3.157554866538104066E-14, 3.499999999999961808, 1.052419468952637160 ) ) ;
#36503=CARTESIAN_POINT ( 'NONE',  ( -1.360316468750021768, 0.1718750003414371008, -3.295974604355933479E-14 ) ) ;
#36547=( BOUNDED_SURFACE ( )  B_SPLINE_SURFACE ( 1, 2, ( 
 ( #86550, #201337, #70269, #54055, #37801, #152615, #4199, #151566, #133203, #184037, #103876, #87620, #85480, #167802, #83334, #19399, #2064, #150504, #153691, #3133, #69203, #52977, #5260, #174230, #124476, #6342, #156901, #122349, #7410, #89779, #140675, #9562, #157971, #72414, #206690, #139593, #56188, #73492, #138515, #58319, #205616, #190433, #42092, #71336, #141746, #108207, #25804, #170994, #155826, #121268, #75638, #57256, #23669, #123416, #204539, #104954, #189380, #91913, #187243, #173155, #137453, #203467, #55122, #41023, #38869, #188304, #88699, #39946, #22593, #154758, #107132, #106053, #24737, #172077, #90838, #8489, #74573, #21145, #118741, #17955, #100297, #136009, #202022, #184725, #86183, #34225, #104580, #102427, #170625, #101359, #87249, #166364, #153314, #182601, #19029, #134957, #36349, #22211, #53682, #88324, #70967, #3825, #133908, #1703, #154388, #117686, #119813, #169563, #85109, #84042, #203102, #4889, #186870, #150130, #168496, #137077, #167437, #183678, #67757, #54747, #199914, #51561, #116608, #5966, #185793, #20095, #138149, #151195, #35283, #2766, #68837, #200965, #52612, #152252, #69898, #37426, #103503, #120897, #72036, #38502, #50487, #89402, #207397, #56883, #106756, #156534, #189012, #73111, #23292, #174930, #42799, #90467, #204158, #121968, #157604, #191133, #26510, #11320, #24357, #139211, #43862, #173865, #108907, #155451, #175988, #109978, #8125, #206324, #92619, #172784, #158661, #74211, #25440, #159722, #55813, #7034, #141387, #57949, #107838, #9200, #40655, #39564, #140306, #10259, #91546, #124114, #41729, #190077, #76334, #75272, #208448, #142441, #187934 ),
 ( #27582, #59016, #125172, #60081, #126238, #192200, #93680, #205242, #77399, #105666, #123058, #171693, #107522, #123803, #189763, #142125, #27258, #42481, #41415, #209196, #90158, #188702, #172467, #156224, #24055, #105347, #73893, #72808, #57643, #7801, #6729, #11001, #22975, #174618, #138909, #124856, #40338, #139987, #206008, #106444, #204929, #155147, #92309, #26194, #173552, #121659, #39254, #74958, #108590, #158353, #143206, #25126, #56580, #175670, #91229, #9946, #122739, #93366, #159402, #157289, #8879, #76022, #141068, #208138, #207075, #58706, #77078, #187627, #190820, #59768, #125927, #191885, #43546, #109668, #171384, #89093, #94433, #129131, #197220, #176724, #130183, #60836, #164729, #126997, #79217, #196176, #28336, #192956, #160472, #146382, #64038, #110724, #148493, #12079, #62961, #96567, #211337, #14191, #31548, #195107, #78146, #144277, #212395, #47817, #46743, #162614, #44608, #114975, #112856, #180976, #80283, #97623, #194026, #178872, #210270, #61908, #163681, #82403, #128070, #15263, #113929, #213454, #48861, #32598, #81350, #147430, #179925, #45676, #30483, #65077, #131232, #98673, #16318, #111793, #177798, #145336, #29415, #95506, #161553, #13141, #199337, #83469, #54179, #152742, #67196, #185222, #34715, #52050, #134400, #168990, #170049, #104005, #50983, #20589, #184164, #100786, #118177, #117105, #86675, #35785, #4323, #70393, #60, #21634, #136510, #202530, #165800, #68267, #49917, #37931, #101861, #2191, #200402, #201462, #183106, #166868, #17385, #18462, #198275, #133333, #84540, #135441, #150630, #69330, #3262, #167929, #87742, #19528, #66124, #85605, #132267, #36846, #116038 ) ),
 .UNSPECIFIED., .F., .F., .F. ) 
 B_SPLINE_SURFACE_WITH_KNOTS ( ( 2, 2 ),
 ( 3, 2, 2, 2, 2, 2, 2, 2, 2, 2, 2, 2, 2, 2, 2, 2, 2, 2, 2, 2, 2, 2, 2, 2, 2, 2, 2, 2, 2, 2, 2, 2, 2, 2, 2, 2, 2, 2, 2, 2, 2, 2, 2, 2, 2, 2, 2, 2, 2, 2, 2, 2, 2, 2, 2, 2, 2, 2, 2, 2, 2, 2, 2, 2, 2, 2, 2, 2, 2, 2, 2, 2, 2, 2, 2, 2, 2, 2, 2, 2, 2, 2, 2, 2, 2, 2, 2, 2, 2, 2, 2, 2, 2, 2, 2, 2, 3 ),
 ( 0.000000000000000000, 1.000000000000000000 ),
 ( 0.000000000000000000, 0.01041666666666666609, 0.02083333333333333218, 0.03125000000000000000, 0.04166666666666666435, 0.05208333333333333565, 0.06250000000000000000, 0.07291666666666667129, 0.08333333333333332871, 0.09375000000000000000, 0.1041666666666666713, 0.1145833333333333287, 0.1250000000000000000, 0.1354166666666666574, 0.1458333333333333426, 0.1562500000000000000, 0.1666666666666666574, 0.1770833333333333426, 0.1875000000000000000, 0.1979166666666666574, 0.2083333333333333426, 0.2187500000000000000, 0.2291666666666666574, 0.2395833333333333426, 0.2500000000000000000, 0.2604166666666666852, 0.2708333333333333148, 0.2812500000000000000, 0.2916666666666666852, 0.3020833333333333148, 0.3125000000000000000, 0.3229166666666666852, 0.3333333333333333148, 0.3437500000000000000, 0.3541666666666666852, 0.3645833333333333148, 0.3750000000000000000, 0.3854166666666666852, 0.3958333333333333148, 0.4062500000000000000, 0.4166666666666666852, 0.4270833333333333148, 0.4375000000000000000, 0.4479166666666666852, 0.4583333333333333148, 0.4687500000000000000, 0.4791666666666666852, 0.4895833333333333148, 0.5000000000000000000, 0.5104166666666666297, 0.5208333333333333703, 0.5312500000000000000, 0.5416666666666666297, 0.5520833333333333703, 0.5625000000000000000, 0.5729166666666666297, 0.5833333333333333703, 0.5937500000000000000, 0.6041666666666666297, 0.6145833333333333703, 0.6250000000000000000, 0.6354166666666666297, 0.6458333333333333703, 0.6562500000000000000, 0.6666666666666666297, 0.6770833333333333703, 0.6875000000000000000, 0.6979166666666666297, 0.7083333333333333703, 0.7187500000000000000, 0.7291666666666666297, 0.7395833333333333703, 0.7500000000000000000, 0.7604166666666666297, 0.7708333333333333703, 0.7812500000000000000, 0.7916666666666666297, 0.8020833333333333703, 0.8125000000000000000, 0.8229166666666666297, 0.8333333333333333703, 0.8437500000000000000, 0.8541666666666666297, 0.8645833333333333703, 0.8750000000000000000, 0.8854166666666666297, 0.8958333333333333703, 0.9062500000000000000, 0.9166666666666666297, 0.9270833333333333703, 0.9375000000000000000, 0.9479166666666666297, 0.9583333333333333703, 0.9687500000000000000, 0.9791666666666666297, 0.9895833333333333703, 1.000000000000000000 ),
 .UNSPECIFIED. ) 
 GEOMETRIC_REPRESENTATION_ITEM ( )  RATIONAL_B_SPLINE_SURFACE ( (
 ( 1.000000000000000000, 0.8660254037844387076, 1.000000000000000000, 0.8660254037844387076, 1.000000000000000000, 0.8660254037844387076, 1.000000000000000000, 0.8660254037844387076, 1.000000000000000000, 0.8660254037844387076, 1.000000000000000000, 0.8660254037844387076, 1.000000000000000000, 0.8660254037844387076, 1.000000000000000000, 0.8660254037844387076, 1.000000000000000000, 0.8660254037844387076, 1.000000000000000000, 0.8660254037844387076, 1.000000000000000000, 0.8660254037844387076, 1.000000000000000000, 0.8660254037844387076, 1.000000000000000000, 0.8660254037844387076, 1.000000000000000000, 0.8660254037844387076, 1.000000000000000000, 0.8660254037844387076, 1.000000000000000000, 0.8660254037844387076, 1.000000000000000000, 0.8660254037844387076, 1.000000000000000000, 0.8660254037844387076, 1.000000000000000000, 0.8660254037844387076, 1.000000000000000000, 0.8660254037844387076, 1.000000000000000000, 0.8660254037844387076, 1.000000000000000000, 0.8660254037844387076, 1.000000000000000000, 0.8660254037844387076, 1.000000000000000000, 0.8660254037844387076, 1.000000000000000000, 0.8660254037844387076, 1.000000000000000000, 0.8660254037844387076, 1.000000000000000000, 0.8660254037844387076, 1.000000000000000000, 0.8660254037844387076, 1.000000000000000000, 0.8660254037844387076, 1.000000000000000000, 0.8660254037844387076, 1.000000000000000000, 0.8660254037844387076, 1.000000000000000000, 0.8660254037844387076, 1.000000000000000000, 0.8660254037844387076, 1.000000000000000000, 0.8660254037844387076, 1.000000000000000000, 0.8660254037844387076, 1.000000000000000000, 0.8660254037844387076, 1.000000000000000000, 0.8660254037844387076, 1.000000000000000000, 0.8660254037844387076, 1.000000000000000000, 0.8660254037844387076, 1.000000000000000000, 0.8660254037844387076, 1.000000000000000000, 0.8660254037844387076, 1.000000000000000000, 0.8660254037844387076, 1.000000000000000000, 0.8660254037844387076, 1.000000000000000000, 0.8660254037844387076, 1.000000000000000000, 0.8660254037844387076, 1.000000000000000000, 0.8660254037844387076, 1.000000000000000000, 0.8660254037844387076, 1.000000000000000000, 0.8660254037844387076, 1.000000000000000000, 0.8660254037844387076, 1.000000000000000000, 0.8660254037844387076, 1.000000000000000000, 0.8660254037844387076, 1.000000000000000000, 0.8660254037844387076, 1.000000000000000000, 0.8660254037844387076, 1.000000000000000000, 0.8660254037844387076, 1.000000000000000000, 0.8660254037844387076, 1.000000000000000000, 0.8660254037844387076, 1.000000000000000000, 0.8660254037844387076, 1.000000000000000000, 0.8660254037844387076, 1.000000000000000000, 0.8660254037844387076, 1.000000000000000000, 0.8660254037844387076, 1.000000000000000000, 0.8660254037844387076, 1.000000000000000000, 0.8660254037844387076, 1.000000000000000000, 0.8660254037844387076, 1.000000000000000000, 0.8660254037844387076, 1.000000000000000000, 0.8660254037844387076, 1.000000000000000000, 0.8660254037844387076, 1.000000000000000000, 0.8660254037844387076, 1.000000000000000000, 0.8660254037844387076, 1.000000000000000000, 0.8660254037844387076, 1.000000000000000000, 0.8660254037844387076, 1.000000000000000000, 0.8660254037844387076, 1.000000000000000000, 0.8660254037844387076, 1.000000000000000000, 0.8660254037844387076, 1.000000000000000000, 0.8660254037844387076, 1.000000000000000000, 0.8660254037844387076, 1.000000000000000000, 0.8660254037844387076, 1.000000000000000000, 0.8660254037844387076, 1.000000000000000000, 0.8660254037844387076, 1.000000000000000000, 0.8660254037844387076, 1.000000000000000000, 0.8660254037844387076, 1.000000000000000000, 0.8660254037844387076, 1.000000000000000000, 0.8660254037844387076, 1.000000000000000000, 0.8660254037844387076, 1.000000000000000000, 0.8660254037844387076, 1.000000000000000000, 0.8660254037844387076, 1.000000000000000000, 0.8660254037844387076, 1.000000000000000000, 0.8660254037844387076, 1.000000000000000000, 0.8660254037844387076, 1.000000000000000000, 0.8660254037844387076, 1.000000000000000000, 0.8660254037844387076, 1.000000000000000000, 0.8660254037844387076, 1.000000000000000000, 0.8660254037844387076, 1.000000000000000000, 0.8660254037844387076, 1.000000000000000000, 0.8660254037844387076, 1.000000000000000000, 0.8660254037844387076, 1.000000000000000000, 0.8660254037844387076, 1.000000000000000000),
 ( 1.000000000000000000, 0.8660254037844387076, 1.000000000000000000, 0.8660254037844387076, 1.000000000000000000, 0.8660254037844387076, 1.000000000000000000, 0.8660254037844387076, 1.000000000000000000, 0.8660254037844387076, 1.000000000000000000, 0.8660254037844387076, 1.000000000000000000, 0.8660254037844387076, 1.000000000000000000, 0.8660254037844387076, 1.000000000000000000, 0.8660254037844387076, 1.000000000000000000, 0.8660254037844387076, 1.000000000000000000, 0.8660254037844387076, 1.000000000000000000, 0.8660254037844387076, 1.000000000000000000, 0.8660254037844387076, 1.000000000000000000, 0.8660254037844387076, 1.000000000000000000, 0.8660254037844387076, 1.000000000000000000, 0.8660254037844387076, 1.000000000000000000, 0.8660254037844387076, 1.000000000000000000, 0.8660254037844387076, 1.000000000000000000, 0.8660254037844387076, 1.000000000000000000, 0.8660254037844387076, 1.000000000000000000, 0.8660254037844387076, 1.000000000000000000, 0.8660254037844387076, 1.000000000000000000, 0.8660254037844387076, 1.000000000000000000, 0.8660254037844387076, 1.000000000000000000, 0.8660254037844387076, 1.000000000000000000, 0.8660254037844387076, 1.000000000000000000, 0.8660254037844387076, 1.000000000000000000, 0.8660254037844387076, 1.000000000000000000, 0.8660254037844387076, 1.000000000000000000, 0.8660254037844387076, 1.000000000000000000, 0.8660254037844387076, 1.000000000000000000, 0.8660254037844387076, 1.000000000000000000, 0.8660254037844387076, 1.000000000000000000, 0.8660254037844387076, 1.000000000000000000, 0.8660254037844387076, 1.000000000000000000, 0.8660254037844387076, 1.000000000000000000, 0.8660254037844387076, 1.000000000000000000, 0.8660254037844387076, 1.000000000000000000, 0.8660254037844387076, 1.000000000000000000, 0.8660254037844387076, 1.000000000000000000, 0.8660254037844387076, 1.000000000000000000, 0.8660254037844387076, 1.000000000000000000, 0.8660254037844387076, 1.000000000000000000, 0.8660254037844387076, 1.000000000000000000, 0.8660254037844387076, 1.000000000000000000, 0.8660254037844387076, 1.000000000000000000, 0.8660254037844387076, 1.000000000000000000, 0.8660254037844387076, 1.000000000000000000, 0.8660254037844387076, 1.000000000000000000, 0.8660254037844387076, 1.000000000000000000, 0.8660254037844387076, 1.000000000000000000, 0.8660254037844387076, 1.000000000000000000, 0.8660254037844387076, 1.000000000000000000, 0.8660254037844387076, 1.000000000000000000, 0.8660254037844387076, 1.000000000000000000, 0.8660254037844387076, 1.000000000000000000, 0.8660254037844387076, 1.000000000000000000, 0.8660254037844387076, 1.000000000000000000, 0.8660254037844387076, 1.000000000000000000, 0.8660254037844387076, 1.000000000000000000, 0.8660254037844387076, 1.000000000000000000, 0.8660254037844387076, 1.000000000000000000, 0.8660254037844387076, 1.000000000000000000, 0.8660254037844387076, 1.000000000000000000, 0.8660254037844387076, 1.000000000000000000, 0.8660254037844387076, 1.000000000000000000, 0.8660254037844387076, 1.000000000000000000, 0.8660254037844387076, 1.000000000000000000, 0.8660254037844387076, 1.000000000000000000, 0.8660254037844387076, 1.000000000000000000, 0.8660254037844387076, 1.000000000000000000, 0.8660254037844387076, 1.000000000000000000, 0.8660254037844387076, 1.000000000000000000, 0.8660254037844387076, 1.000000000000000000, 0.8660254037844387076, 1.000000000000000000, 0.8660254037844387076, 1.000000000000000000, 0.8660254037844387076, 1.000000000000000000, 0.8660254037844387076, 1.000000000000000000, 0.8660254037844387076, 1.000000000000000000, 0.8660254037844387076, 1.000000000000000000, 0.8660254037844387076, 1.000000000000000000, 0.8660254037844387076, 1.000000000000000000, 0.8660254037844387076, 1.000000000000000000, 0.8660254037844387076, 1.000000000000000000, 0.8660254037844387076, 1.000000000000000000, 0.8660254037844387076, 1.000000000000000000, 0.8660254037844387076, 1.000000000000000000, 0.8660254037844387076, 1.000000000000000000, 0.8660254037844387076, 1.000000000000000000, 0.8660254037844387076, 1.000000000000000000, 0.8660254037844387076, 1.000000000000000000, 0.8660254037844387076, 1.000000000000000000, 0.8660254037844387076, 1.000000000000000000, 0.8660254037844387076, 1.000000000000000000, 0.8660254037844387076, 1.000000000000000000, 0.8660254037844387076, 1.000000000000000000) ) ) 
 REPRESENTATION_ITEM ( '' )  SURFACE ( )  );
#36649=CARTESIAN_POINT ( 'NONE',  ( 1.360316468749983576, 1.515625000341386253, -4.163336342344337027E-14 ) ) ;
#36768=DIRECTION ( 'NONE',  ( 1.000000000000000000, -7.771561172376096769E-16, -4.440892098500627148E-16 ) ) ;
#36784=ORIENTED_EDGE ( 'NONE', *, *, #204783, .T. ) ;
#36811=CARTESIAN_POINT ( 'NONE',  ( -3.355169270512988773E-14, -0.4999999993171823642, -1.414508159514593411 ) ) ;
#36846=CARTESIAN_POINT ( 'NONE',  ( -1.360316468750024876, -1.057291666325259172, 0.7853790794158601596 ) ) ;
#36889=CARTESIAN_POINT ( 'NONE',  ( -1.360316468750054630, 0.9114583336747262843, 0.7853790794158721500 ) ) ;
#36970=CARTESIAN_POINT ( 'NONE',  ( -1.792021045695255545E-15, 2.999999999999988898, 1.224999999999993427 ) ) ;
#36976=ORIENTED_EDGE ( 'NONE', *, *, #109534, .T. ) ;
#37018=CARTESIAN_POINT ( 'NONE',  ( -0.3585786437627170309, 3.975028841772325627, -0.9637995837463111393 ) ) ;
#37038=CARTESIAN_POINT ( 'NONE',  ( -3.469446951953614189E-15, 3.236073672982384242, -5.377642775528101993E-14 ) ) ;
#37097=ORIENTED_EDGE ( 'NONE', *, *, #92378, .F. ) ;
#37152=( BOUNDED_SURFACE ( )  B_SPLINE_SURFACE ( 3, 2, ( 
 ( #272, #1347, #182246 ),
 ( #145549, #15476, #166013 ),
 ( #114145, #46955, #81560 ),
 ( #161765, #99949, #147644 ) ),
 .UNSPECIFIED., .F., .F., .T. ) 
 B_SPLINE_SURFACE_WITH_KNOTS ( ( 4, 4 ),
 ( 3, 3 ),
 ( 3.141592653589793116, 4.712388980384689674 ),
 ( 0.000000000000000000, 1.000000000000000000 ),
 .UNSPECIFIED. ) 
 GEOMETRIC_REPRESENTATION_ITEM ( )  RATIONAL_B_SPLINE_SURFACE ( (
 ( 1.000000000000000000, 0.8661919058288115592, 1.000000000000000000),
 ( 1.000000000000000000, 0.8676977444973651421, 1.000000000000000000),
 ( 1.000000000000000000, 0.8014503788334911283, 1.000000000000000000),
 ( 1.000000000000000000, 0.7071067811865225927, 1.000000000000000000) ) ) 
 REPRESENTATION_ITEM ( '' )  SURFACE ( )  );
#37161=CARTESIAN_POINT ( 'NONE',  ( -0.3000000000000241918, 4.000000000000003553, -1.007084189318394385 ) ) ;
#37194=CARTESIAN_POINT ( 'NONE',  ( 0.6124999999999707345, 2.145833334016141070, 1.060881119635899816 ) ) ;
#37214=EDGE_CURVE ( 'NONE', #132173, #144032, #173215, .T. ) ;
#37311=ORIENTED_EDGE ( 'NONE', *, *, #181736, .T. ) ;
#37400=CARTESIAN_POINT ( 'NONE',  ( -0.4000000000000496492, 3.372708439410135206, 0.4999999999999483746 ) ) ;
#37404=CARTESIAN_POINT ( 'NONE',  ( 1.360316468750004448, 2.546875000341383810, -3.295974604355933479E-14 ) ) ;
#37426=CARTESIAN_POINT ( 'NONE',  ( -2.553934817853170728E-14, 0.1875000000000329459, -1.414508159514617391 ) ) ;
#37506=ORIENTED_EDGE ( 'NONE', *, *, #188015, .T. ) ;
#37541=DIRECTION ( 'NONE',  ( 9.436895709313856232E-16, -0.8656921114426506803, -0.5005768354468324022 ) ) ;
#37636=EDGE_LOOP ( 'NONE', ( #208577, #163984, #101568, #185543 ) ) ;
#37714=ORIENTED_EDGE ( 'NONE', *, *, #45494, .T. ) ;
#37728=CARTESIAN_POINT ( 'NONE',  ( 1.360316468749955598, -0.005208332991877948244, 0.7853790794158660438 ) ) ;
#37747=CARTESIAN_POINT ( 'NONE',  ( -5.270602541814852086E-14, 4.000000000000003553, 1.829047314007930636 ) ) ;
#37801=CARTESIAN_POINT ( 'NONE',  ( 0.6125000000000123679, 2.916666666666671404, -1.060881119635948444 ) ) ;
#37835=CARTESIAN_POINT ( 'NONE',  ( -1.913843478179667823, 3.256154753185136475, 0.4414708703499633513 ) ) ;
#37876=DIRECTION ( 'NONE',  ( -0.9692622846690300831, 1.734723475976804255E-14, -0.2460297208025325477 ) ) ;
#37893=CARTESIAN_POINT ( 'NONE',  ( -1.225000000000042055, -1.187499999317158439, -4.857225732735059864E-14 ) ) ;
#37910=EDGE_CURVE ( 'NONE', #12050, #65799, #189671, .T. ) ;
#37931=CARTESIAN_POINT ( 'NONE',  ( -1.360316468750048635, -0.5989583329919208055, -0.7853790794159082322 ) ) ;
#37963=CARTESIAN_POINT ( 'NONE',  ( 1.360316468749963592, 1.286458333674704191, -0.7853790794158961308 ) ) ;
#37971=CARTESIAN_POINT ( 'NONE',  ( 1.360316468749983576, 0.5156250003414062366, -5.204170427930421283E-15 ) ) ;
#37981=ORIENTED_EDGE ( 'NONE', *, *, #119819, .T. ) ;
#38266=CARTESIAN_POINT ( 'NONE',  ( -4.957638175832625493E-14, 1.375000000682762291, 1.414508159514551444 ) ) ;
#38332=DIRECTION ( 'NONE',  ( 1.000000000000000000, -7.771561172376096769E-16, -4.440892098500627148E-16 ) ) ;
#38357=CARTESIAN_POINT ( 'NONE',  ( 0.2999999999999860556, 3.999999999999996447, 0.9782388782688545836 ) ) ;
#38377=CARTESIAN_POINT ( 'NONE',  ( -0.3914079065635818755, 3.043201908700303715, 0.4248930002254263094 ) ) ;
#38441=VERTEX_POINT ( 'NONE', #43369 ) ;
#38480=CARTESIAN_POINT ( 'NONE',  ( 1.360316468749963592, 1.317708333674712184, -0.7853790794158981292 ) ) ;
#38502=CARTESIAN_POINT ( 'NONE',  ( 1.224999999999967004, 0.1041666666667366015, 0.7072540797572677285 ) ) ;
#38556=CIRCLE ( 'NONE', #159620, 0.09999999999999976963 ) ;
#38562=EDGE_CURVE ( 'NONE', #132409, #17367, #42943, .T. ) ;
#38586=CARTESIAN_POINT ( 'NONE',  ( -1.326716514427061987E-15, 2.999999999999988454, -1.225000000000003864 ) ) ;
#38590=CARTESIAN_POINT ( 'NONE',  ( -0.4000000000000236144, -3.469446951953614189E-14, -3.989863994746656317E-14 ) ) ;
#38660=CARTESIAN_POINT ( 'NONE',  ( 0.3999999999999889200, 0.000000000000000000, -5.204170427930421283E-15 ) ) ;
#38768=CARTESIAN_POINT ( 'NONE',  ( -1.225000000000044276, 1.770833333333392545, 0.7072540797572737237 ) ) ;
#38798=CARTESIAN_POINT ( 'NONE',  ( -1.552391752028397856E-14, -0.04687499965855816686, 1.570758158831750295 ) ) ;
#38814=ADVANCED_FACE ( 'NONE', ( #113751 ), #65039, .T. ) ;
#38849=CARTESIAN_POINT ( 'NONE',  ( -1.874158809982179319, 3.299964346911585356, 0.3999999999999993006 ) ) ;
#38869=CARTESIAN_POINT ( 'NONE',  ( 0.6124999999999932720, 1.666666666666712038, -1.060881119635983083 ) ) ;
#38914=CARTESIAN_POINT ( 'NONE',  ( 1.253848497529134409, -2.775557561562891351E-14, 0.5275650105875644424 ) ) ;
#38950=AXIS2_PLACEMENT_3D ( 'NONE', #50550, #199982, #51629 ) ;
#38963=CARTESIAN_POINT ( 'NONE',  ( 0.6124999999999793943, -0.8541666659838200726, 1.060881119635887604 ) ) ;
#39030=CARTESIAN_POINT ( 'NONE',  ( -1.360316468750042862, 1.869791667008058988, -0.7853790794158961308 ) ) ;
#39038=CARTESIAN_POINT ( 'NONE',  ( -1.360316468750008667, 0.1197916670080665519, -0.7853790794159001276 ) ) ;
#39060=ORIENTED_EDGE ( 'NONE', *, *, #82886, .F. ) ;
#39064=ORIENTED_EDGE ( 'NONE', *, *, #187251, .T. ) ;
#39084=ORIENTED_EDGE ( 'NONE', *, *, #170552, .F. ) ;
#39123=ORIENTED_EDGE ( 'NONE', *, *, #191685, .F. ) ;
#39233=CARTESIAN_POINT ( 'NONE',  ( 1.224999999999967004, 0.3958333333333378667, -0.7072540797573017013 ) ) ;
#39254=CARTESIAN_POINT ( 'NONE',  ( -0.6801582343750282034, 1.963541667008045222, 1.178068619123803451 ) ) ;
#39264=DIRECTION ( 'NONE',  ( -1.000000000000000000, 7.771561172376096769E-16, 4.440892098500627148E-16 ) ) ;
#39288=VERTEX_POINT ( 'NONE', #45247 ) ;
#39299=ORIENTED_EDGE ( 'NONE', *, *, #29742, .F. ) ;
#39333=CARTESIAN_POINT ( 'NONE',  ( 1.224999999999976108, 1.187500000682802037, -3.469446951953614189E-14 ) ) ;
#39362=ORIENTED_EDGE ( 'NONE', *, *, #212165, .F. ) ;
#39492=ADVANCED_FACE ( 'NONE', ( #32176 ), #114562, .F. ) ;
#39539=CARTESIAN_POINT ( 'NONE',  ( -1.919777701841220319, 3.227564709615637462, -0.4000000000000281664 ) ) ;
#39542=CARTESIAN_POINT ( 'NONE',  ( 0.6801582343749970061, 2.505208333674749266, 1.178068619123801675 ) ) ;
#39564=CARTESIAN_POINT ( 'NONE',  ( -1.225000000000034284, -0.7708333333333156068, -0.7072540797573237947 ) ) ;
#39595=ORIENTED_EDGE ( 'NONE', *, *, #171411, .F. ) ;
#39607=ORIENTED_EDGE ( 'NONE', *, *, #40880, .T. ) ;
#39632=CYLINDRICAL_SURFACE ( 'NONE', #42440, 0.1000000000000000472 ) ;
#39778=ORIENTED_EDGE ( 'NONE', *, *, #153901, .F. ) ;
#39783=EDGE_CURVE ( 'NONE', #41218, #176198, #85972, .T. ) ;
#39850=AXIS2_PLACEMENT_3D ( 'NONE', #62622, #194762, #112515 ) ;
#39873=CARTESIAN_POINT ( 'NONE',  ( 1.360316468749969809, 1.036458333674743049, -0.7853790794158820310 ) ) ;
#39939=ORIENTED_EDGE ( 'NONE', *, *, #161766, .F. ) ;
#39946=CARTESIAN_POINT ( 'NONE',  ( 1.224999999999989209, 1.604166666666679619, 0.7072540797572898219 ) ) ;
#39990=CARTESIAN_POINT ( 'NONE',  ( 1.874158809982179319, 3.299964346911585356, -0.3999999999999993006 ) ) ;
#40100=CARTESIAN_POINT ( 'NONE',  ( 1.360316468749947605, 2.536458333674726173, -0.7853790794159141164 ) ) ;
#40109=CARTESIAN_POINT ( 'NONE',  ( 1.253848497529134409, -2.775557561562891351E-14, 0.5275650105875644424 ) ) ;
#40211=CARTESIAN_POINT ( 'NONE',  ( -2.353344407399531160E-15, 2.999999999999989342, 1.857347330825967369 ) ) ;
#40248=DIRECTION ( 'NONE',  ( -3.330669073875477510E-16, 2.265265487380573707E-16, 1.000000000000000000 ) ) ;
#40304=CARTESIAN_POINT ( 'NONE',  ( -1.225000000000005640, 0.5625000006828015930, -1.734723475976807094E-15 ) ) ;
#40331=DIRECTION ( 'NONE',  ( 3.330669073875478989E-16, -3.540251991789410786E-16, -1.000000000000000000 ) ) ;
#40336=CARTESIAN_POINT ( 'NONE',  ( 0.3282377607281209420, 0.6361645503674333568, 1.224999999999965894 ) ) ;
#40338=CARTESIAN_POINT ( 'NONE',  ( -1.360316468750007779, 2.171875000341411344, -4.336808689942017736E-14 ) ) ;
#40349=CARTESIAN_POINT ( 'NONE',  ( -2.449742653233043743, 3.299999999999976730, -0.4000000000000339950 ) ) ;
#40417=CARTESIAN_POINT ( 'NONE',  ( 0.6124999999999828360, 0.9791666673494778816, -1.060881119635955327 ) ) ;
#40492=CARTESIAN_POINT ( 'NONE',  ( -0.4000000000000393241, 3.248764396332298965, 0.4641653677812256906 ) ) ;
#40528=VERTEX_POINT ( 'NONE', #60956 ) ;
#40531=CARTESIAN_POINT ( 'NONE',  ( -1.225000000000038058, 1.333333334016162386, 0.7072540797572777205 ) ) ;
#40628=CARTESIAN_POINT ( 'NONE',  ( -1.859593142679977218, 3.245846270153701418, -0.4000000000000284439 ) ) ;
#40631=CARTESIAN_POINT ( 'NONE',  ( 1.360316468749939833, 0.02604166700813021276, 0.7853790794158660438 ) ) ;
#40655=CARTESIAN_POINT ( 'NONE',  ( -1.225000000000008971, -0.7499999999999867883, -8.673617379884035472E-15 ) ) ;
#40667=FACE_OUTER_BOUND ( 'NONE', #158391, .T. ) ;
#40678=CARTESIAN_POINT ( 'NONE',  ( -0.4288785890452732064, 3.049942316455313218, 0.4196807566830707548 ) ) ;
#40763=ORIENTED_EDGE ( 'NONE', *, *, #195142, .F. ) ;
#40796=ORIENTED_EDGE ( 'NONE', *, *, #92773, .T. ) ;
#40880=EDGE_CURVE ( 'NONE', #195414, #126635, #165919, .T. ) ;
#40939=ORIENTED_EDGE ( 'NONE', *, *, #77201, .F. ) ;
#40949=CARTESIAN_POINT ( 'NONE',  ( -3.355169270512988773E-14, 0.9531250003414385441, 1.570758158831740303 ) ) ;
#41023=CARTESIAN_POINT ( 'NONE',  ( -4.957638175832625493E-14, 1.687500000000000000, -1.414508159514599628 ) ) ;
#41035=CARTESIAN_POINT ( 'NONE',  ( -1.743066579297358008E-15, 2.187499999999992006, -1.225000000000032951 ) ) ;
#41060=CARTESIAN_POINT ( 'NONE',  ( -1.360316468750011332, 2.421875000341397577, -1.387778780781445676E-14 ) ) ;
#41144=EDGE_CURVE ( 'NONE', #127784, #140828, #29007, .T. ) ;
#41183=CARTESIAN_POINT ( 'NONE',  ( 0.6801582343749883464, 2.473958333674766585, 1.178068619123824323 ) ) ;
#41191=CARTESIAN_POINT ( 'NONE',  ( 0.3282377607281215526, 2.926335450315382225, -1.225000000000001421 ) ) ;
#41218=VERTEX_POINT ( 'NONE', #53696 ) ;
#41415=CARTESIAN_POINT ( 'NONE',  ( 1.360316468750004448, 2.546875000341383810, -3.295974604355933479E-14 ) ) ;
#41426=FACE_OUTER_BOUND ( 'NONE', #188070, .T. ) ;
#41485=CARTESIAN_POINT ( 'NONE',  ( -0.4500000000000215494, 3.999999999999989786, -0.5000000000000160982 ) ) ;
#41492=CARTESIAN_POINT ( 'NONE',  ( 0.6124999999999793943, 0.4791666673494773820, -1.060881119635969094 ) ) ;
#41501=EDGE_LOOP ( 'NONE', ( #4048, #192765, #190260, #96327 ) ) ;
#41584=LINE ( 'NONE', #38357, #176883 ) ;
#41609=CARTESIAN_POINT ( 'NONE',  ( -0.3282377607281434240, 1.363835450998170051, 1.224999999999967892 ) ) ;
#41612=ORIENTED_EDGE ( 'NONE', *, *, #86559, .T. ) ;
#41626=CARTESIAN_POINT ( 'NONE',  ( 1.874158809982179319, 3.299964346911585356, -0.3999999999999993006 ) ) ;
#41654=CARTESIAN_POINT ( 'NONE',  ( -1.743066579297358008E-15, 2.187499999999992006, -1.225000000000032951 ) ) ;
#41673=ORIENTED_EDGE ( 'NONE', *, *, #82844, .F. ) ;
#41707=CARTESIAN_POINT ( 'NONE',  ( -5.558564015327489343E-14, 0.6093750003414449834, -1.570758158831798257 ) ) ;
#41729=CARTESIAN_POINT ( 'NONE',  ( 1.224999999999993427, -0.8750000000000077716, -3.989863994746656317E-14 ) ) ;
#41904=ORIENTED_EDGE ( 'NONE', *, *, #166426, .F. ) ;
#41921=VECTOR ( 'NONE', #47178, 1000.000000000000000 ) ;
#41993=EDGE_CURVE ( 'NONE', #67541, #43310, #6835, .T. ) ;
#42024=CARTESIAN_POINT ( 'NONE',  ( -1.360316468750046859, 0.3697916670080757529, -0.7853790794159101196 ) ) ;
#42092=CARTESIAN_POINT ( 'NONE',  ( 1.224999999999991651, 2.124999999999967137, -3.469446951953614189E-14 ) ) ;
#42152=CARTESIAN_POINT ( 'NONE',  ( -2.440293211016301606E-15, 1.312499999999991118, 1.224999999999973888 ) ) ;
#42230=DIRECTION ( 'NONE',  ( 1.276756478318932585E-15, -1.000000000000000000, 1.665334536937738262E-16 ) ) ;
#42242=LINE ( 'NONE', #74722, #191702 ) ;
#42247=CARTESIAN_POINT ( 'NONE',  ( -1.360316468750054852, 0.9114583336747262843, 0.7853790794158720390 ) ) ;
#42265=VERTEX_POINT ( 'NONE', #41485 ) ;
#42280=CARTESIAN_POINT ( 'NONE',  ( 1.911686719268467005, 3.274494700676901182, -0.4236673858377861812 ) ) ;
#42295=CARTESIAN_POINT ( 'NONE',  ( 3.486133158594716510E-16, 2.437499999999986677, -1.225000000000021849 ) ) ;
#42318=CARTESIAN_POINT ( 'NONE',  ( 0.4170821662628897974, 3.033599471985628959, -0.4170821662629418114 ) ) ;
#42362=EDGE_CURVE ( 'NONE', #210405, #65799, #99892, .T. ) ;
#42398=CYLINDRICAL_SURFACE ( 'NONE', #62604, 0.09999999999999982514 ) ;
#42411=DIRECTION ( 'NONE',  ( 3.330669073875478989E-16, -3.540251991789410786E-16, -1.000000000000000000 ) ) ;
#42440=AXIS2_PLACEMENT_3D ( 'NONE', #156604, #120971, #59081 ) ;
#42481=CARTESIAN_POINT ( 'NONE',  ( 1.360316468749971808, 2.567708333674758148, -0.7853790794159301036 ) ) ;
#42565=CARTESIAN_POINT ( 'NONE',  ( -1.225000000000003864, 0.8125000006827948207, -3.469446951953614189E-15 ) ) ;
#42580=FACE_OUTER_BOUND ( 'NONE', #56307, .T. ) ;
#42593=VECTOR ( 'NONE', #178493, 1000.000000000000000 ) ;
#42654=AXIS2_PLACEMENT_3D ( 'NONE', #82400, #84537, #132264 ) ;
#42660=VERTEX_POINT ( 'NONE', #64119 ) ;
#42779=CARTESIAN_POINT ( 'NONE',  ( -0.6801582343750438575, 0.1302083336747333897, -1.178068619123883165 ) ) ;
#42799=CARTESIAN_POINT ( 'NONE',  ( 1.224999999999984768, -0.1250000000000139888, -4.857225732735059864E-14 ) ) ;
#42864=( BOUNDED_CURVE ( )  B_SPLINE_CURVE ( 2, ( #21240, #155554, #87346, #22308, #172880, #73206, #153413, #138244, #54847 ),
 .UNSPECIFIED., .F., .T. ) 
 B_SPLINE_CURVE_WITH_KNOTS ( ( 3, 2, 2, 2, 3 ),
 ( 0.01562500000000010061, 0.02083333333333333218, 0.03125000000000000000, 0.04166666666666666435, 0.04687499999999993755 ),
 .UNSPECIFIED. ) 
 CURVE ( )  GEOMETRIC_REPRESENTATION_ITEM ( )  RATIONAL_B_SPLINE_CURVE ( ( 0.9330127018922194093, 0.9330127018922207416, 1.000000000000000000, 0.8660254037844387076, 1.000000000000000000, 0.8660254037844387076, 1.000000000000000000, 0.9330127018922200755, 0.9330127018922192983 ) ) 
 REPRESENTATION_ITEM ( '' )  );
#42888=FACE_OUTER_BOUND ( 'NONE', #80257, .T. ) ;
#42943=( BOUNDED_CURVE ( )  B_SPLINE_CURVE ( 3, ( #140890, #206901, #93194, #174442 ),
 .UNSPECIFIED., .F., .T. ) 
 B_SPLINE_CURVE_WITH_KNOTS ( ( 4, 4 ),
 ( 1.570796326794846154, 2.479086375273363618 ),
 .UNSPECIFIED. ) 
 CURVE ( )  GEOMETRIC_REPRESENTATION_ITEM ( )  RATIONAL_B_SPLINE_CURVE ( ( 1.000000000000000000, 0.9324242863012337512, 0.9324242863012337512, 1.000000000000000000 ) ) 
 REPRESENTATION_ITEM ( '' )  );
#43092=CARTESIAN_POINT ( 'NONE',  ( -1.360316468750014884, -0.8593749996585950957, -6.938893903907228378E-15 ) ) ;
#43116=CIRCLE ( 'NONE', #88079, 0.05000000000000002359 ) ;
#43171=VECTOR ( 'NONE', #93798, 1000.000000000000000 ) ;
#43195=CARTESIAN_POINT ( 'NONE',  ( 1.360316468749964480, 2.796875000341370043, -3.989863994746656317E-14 ) ) ;
#43291=AXIS2_PLACEMENT_3D ( 'NONE', #145994, #47419, #209874 ) ;
#43310=VERTEX_POINT ( 'NONE', #202611 ) ;
#43315=CARTESIAN_POINT ( 'NONE',  ( -1.752700365193352367E-14, 0.07812500034142640104, -1.570758158831804474 ) ) ;
#43346=FACE_OUTER_BOUND ( 'NONE', #197298, .T. ) ;
#43349=VERTEX_POINT ( 'NONE', #44156 ) ;
#43369=CARTESIAN_POINT ( 'NONE',  ( -1.772826578343123405, 4.000000000000045297, -0.4500000000000354272 ) ) ;
#43454=VECTOR ( 'NONE', #193167, 1000.000000000000000 ) ;
#43502=CARTESIAN_POINT ( 'NONE',  ( -5.810221930991193690E-16, 2.500000000682804036, -1.225000000000023626 ) ) ;
#43546=CARTESIAN_POINT ( 'NONE',  ( -1.360316468750021768, 1.421875000341424222, -4.510281037539698445E-14 ) ) ;
#43584=CARTESIAN_POINT ( 'NONE',  ( 0.6801582343749970061, 2.223958333674731946, 1.178068619123799898 ) ) ;
#43627=CARTESIAN_POINT ( 'NONE',  ( -2.553934817853170728E-14, 1.000000000682808698, -1.414508159514595409 ) ) ;
#43686=EDGE_CURVE ( 'NONE', #76056, #6089, #165344, .T. ) ;
#43786=EDGE_CURVE ( 'NONE', #63320, #107948, #187262, .T. ) ;
#43794=CARTESIAN_POINT ( 'NONE',  ( -0.6125000000000089262, 0.02083333401611819902, -1.060881119635969094 ) ) ;
#43840=CARTESIAN_POINT ( 'NONE',  ( -1.360316468750019991, 0.4218750003414165062, -4.336808689942017736E-14 ) ) ;
#43862=CARTESIAN_POINT ( 'NONE',  ( 0.6124999999999793943, -0.3333333333333243775, -1.060881119635979530 ) ) ;
#43998=CARTESIAN_POINT ( 'NONE',  ( -0.5000000000000403011, 3.949999999999953548, 0.4499999999999556577 ) ) ;
#44092=ADVANCED_FACE ( 'NONE', ( #70168 ), #4098, .T. ) ;
#44142=LINE ( 'NONE', #90765, #99540 ) ;
#44145=CARTESIAN_POINT ( 'NONE',  ( -7.561650146977034455E-14, -0.5468749996585524631, 1.570758158831754070 ) ) ;
#44156=CARTESIAN_POINT ( 'NONE',  ( 0.3423093779010028537, 2.999999999999988898, 0.3423093779009768189 ) ) ;
#44311=AXIS2_PLACEMENT_3D ( 'NONE', #29922, #96005, #75465 ) ;
#44372=CARTESIAN_POINT ( 'NONE',  ( 1.360316468749969809, 0.7447916670080856338, 0.7853790794158741484 ) ) ;
#44422=ORIENTED_EDGE ( 'NONE', *, *, #138594, .T. ) ;
#44423=LINE ( 'NONE', #56392, #49293 ) ;
#44452=CARTESIAN_POINT ( 'NONE',  ( 1.224999999999947020, 0.1666666673495328932, 0.7072540797572737237 ) ) ;
#44479=DIRECTION ( 'NONE',  ( 3.330669073875479482E-16, -3.330669073875479482E-16, -1.000000000000000000 ) ) ;
#44491=EDGE_CURVE ( 'NONE', #194227, #3320, #125205, .T. ) ;
#44544=ADVANCED_FACE ( 'NONE', ( #94531 ), #160570, .T. ) ;
#44608=CARTESIAN_POINT ( 'NONE',  ( -0.6801582343750438575, 0.7135416670080579893, 1.178068619123810334 ) ) ;
#44645=CARTESIAN_POINT ( 'NONE',  ( 1.360316468749973584, 2.786458333674735499, -0.7853790794159101196 ) ) ;
#44750=VERTEX_POINT ( 'NONE', #87854 ) ;
#44784=ORIENTED_EDGE ( 'NONE', *, *, #45494, .F. ) ;
#44805=ORIENTED_EDGE ( 'NONE', *, *, #76744, .T. ) ;
#44909=CARTESIAN_POINT ( 'NONE',  ( 1.360316468749945606, 0.06770833367471427999, -0.7853790794159161148 ) ) ;
#44956=FACE_OUTER_BOUND ( 'NONE', #175712, .T. ) ;
#44967=CARTESIAN_POINT ( 'NONE',  ( -1.225000000000042277, 0.5208333333333544646, 0.7072540797572777205 ) ) ;
#45017=DIRECTION ( 'NONE',  ( 0.000000000000000000, 1.000000000000000000, -3.330669073875479482E-16 ) ) ;
#45112=DIRECTION ( 'NONE',  ( -3.330669073875478989E-16, 3.330669073875478989E-16, 1.000000000000000000 ) ) ;
#45189=FACE_OUTER_BOUND ( 'NONE', #202558, .T. ) ;
#45217=CARTESIAN_POINT ( 'NONE',  ( 1.224999999999971001, 2.708333334016145066, -0.7072540797573036997 ) ) ;
#45247=CARTESIAN_POINT ( 'NONE',  ( -1.743066579297358008E-15, 2.250000000682787160, -1.225000000000020739 ) ) ;
#45279=CIRCLE ( 'NONE', #207754, 0.09999999999999982514 ) ;
#45314=CARTESIAN_POINT ( 'NONE',  ( 1.360316468749941832, 2.276041667008116942, 0.7853790794158921340 ) ) ;
#45323=DIRECTION ( 'NONE',  ( -0.8583236685137344280, -0.5131086435338277907, 3.252606517456507780E-15 ) ) ;
#45365=CARTESIAN_POINT ( 'NONE',  ( 1.878188943807060696, 3.299815425349224451, 0.3999999999999645506 ) ) ;
#45442=CARTESIAN_POINT ( 'NONE',  ( -0.6801582343750125492, 1.098958333674737720, -1.178068619123855409 ) ) ;
#45448=DIRECTION ( 'NONE',  ( -1.000000000000000000, 7.771561172376096769E-16, 4.440892098500627148E-16 ) ) ;
#45475=DIRECTION ( 'NONE',  ( 1.276756478318932585E-15, -1.000000000000000000, 1.665334536937738262E-16 ) ) ;
#45494=EDGE_CURVE ( 'NONE', #134733, #81519, #33406, .T. ) ;
#45585=VERTEX_POINT ( 'NONE', #32329 ) ;
#45598=DIRECTION ( 'NONE',  ( 1.276756478318932585E-15, -1.000000000000000000, 1.665334536937738262E-16 ) ) ;
#45676=CARTESIAN_POINT ( 'NONE',  ( 1.360316468749987573, 0.2760416670081234369, 0.7853790794158701516 ) ) ;
#45677=CARTESIAN_POINT ( 'NONE',  ( -0.4214947629262029150, 3.038568440852209562, 0.4183962726263074638 ) ) ;
#45716=CARTESIAN_POINT ( 'NONE',  ( -0.6801582343750282034, 2.432291667008048996, 1.178068619123807004 ) ) ;
#45729=ORIENTED_EDGE ( 'NONE', *, *, #119819, .F. ) ;
#45732=CIRCLE ( 'NONE', #142530, 0.09999999999999971412 ) ;
#45741=ORIENTED_EDGE ( 'NONE', *, *, #136759, .T. ) ;
#45781=CARTESIAN_POINT ( 'NONE',  ( -1.874158809982179319, 3.299964346911585356, 0.3999999999999993006 ) ) ;
#45973=CARTESIAN_POINT ( 'NONE',  ( 0.6801582343749796866, -0.9114583329919088150, -1.178068619123886718 ) ) ;
#46021=DIRECTION ( 'NONE',  ( -3.330669073875479482E-16, 3.330669073875479482E-16, 1.000000000000000000 ) ) ;
#46089=CARTESIAN_POINT ( 'NONE',  ( -0.3782569160207248093, 3.049340702855435570, -0.4285286083246230282 ) ) ;
#46182=CARTESIAN_POINT ( 'NONE',  ( 0.4999999999999761302, -2.775557561562891351E-14, 0.4999999999999605316 ) ) ;
#46279=CARTESIAN_POINT ( 'NONE',  ( 1.360316468749955598, -0.7135416663252973635, -0.7853790794159122290 ) ) ;
#46375=CARTESIAN_POINT ( 'NONE',  ( -9.514659125335341649E-15, 1.359375000341400463, -1.570758158831806250 ) ) ;
#46425=DIRECTION ( 'NONE',  ( 1.276756478318932585E-15, -1.000000000000000000, 1.665334536937738262E-16 ) ) ;
#46479=ORIENTED_EDGE ( 'NONE', *, *, #104334, .F. ) ;
#46502=CARTESIAN_POINT ( 'NONE',  ( -3.755786496842897795E-14, 1.078125000341431106, -1.570758158831814466 ) ) ;
#46526=FACE_OUTER_BOUND ( 'NONE', #169309, .T. ) ;
#46538=CARTESIAN_POINT ( 'NONE',  ( 1.886017674307032266, 3.298060805577429644, -0.4014564593431638739 ) ) ;
#46553=AXIS2_PLACEMENT_3D ( 'NONE', #174655, #9981, #59806 ) ;
#46678=CIRCLE ( 'NONE', #139923, 0.05000000000000002359 ) ;
#46743=CARTESIAN_POINT ( 'NONE',  ( 0.6801582343749726922, 0.7552083336747339448, 1.178068619123784355 ) ) ;
#46783=CARTESIAN_POINT ( 'NONE',  ( -4.757329562667670667E-14, 1.953125000341451312, 1.570758158831762286 ) ) ;
#46878=LINE ( 'NONE', #197355, #65193 ) ;
#46955=CARTESIAN_POINT ( 'NONE',  ( -0.4123176713736718679, 3.999999999999981348, -0.8977835139438229417 ) ) ;
#46967=AXIS2_PLACEMENT_3D ( 'NONE', #199644, #137888, #45448 ) ;
#47040=CARTESIAN_POINT ( 'NONE',  ( -2.353626204688216217E-14, 2.828125000341407347, -1.570758158831798257 ) ) ;
#47173=ORIENTED_EDGE ( 'NONE', *, *, #157223, .F. ) ;
#47178=DIRECTION ( 'NONE',  ( 3.497202527569253358E-15, -0.000000000000000000, 1.000000000000000000 ) ) ;
#47276=ORIENTED_EDGE ( 'NONE', *, *, #152637, .T. ) ;
#47352=CARTESIAN_POINT ( 'NONE',  ( 1.360316468749969587, -0.7343749996585879902, -3.642919299551294898E-14 ) ) ;
#47419=DIRECTION ( 'NONE',  ( -1.276756478318932585E-15, 1.000000000000000000, -1.665334536937738262E-16 ) ) ;
#47452=CARTESIAN_POINT ( 'NONE',  ( -0.6801582343750282034, 1.963541667008045222, 1.178068619123803451 ) ) ;
#47457=ORIENTED_EDGE ( 'NONE', *, *, #39783, .T. ) ;
#47471=DIRECTION ( 'NONE',  ( 0.000000000000000000, 0.000000000000000000, -1.000000000000000000 ) ) ;
#47501=DIRECTION ( 'NONE',  ( 0.8656921114426504582, -0.5005768354468328463, -3.032296636007458012E-15 ) ) ;
#47583=CARTESIAN_POINT ( 'NONE',  ( -5.558564015327489343E-14, -0.4218749996585599571, -1.570758158831802254 ) ) ;
#47597=DIRECTION ( 'NONE',  ( 1.276756478318932585E-15, -1.000000000000000000, 1.665334536937738262E-16 ) ) ;
#47719=CARTESIAN_POINT ( 'NONE',  ( -1.874158809982179319, 3.299964346911585356, 0.3999999999999993006 ) ) ;
#47724=VECTOR ( 'NONE', #1342, 1000.000000000000000 ) ;
#47747=ADVANCED_FACE ( 'NONE', ( #49043 ), #211513, .F. ) ;
#47814=VECTOR ( 'NONE', #158028, 1000.000000000000000 ) ;
#47817=CARTESIAN_POINT ( 'NONE',  ( 1.360316468749957597, 0.7760416670081098367, 0.7853790794158520550 ) ) ;
#47856=CARTESIAN_POINT ( 'NONE',  ( -0.6801582343750091075, 2.848958333674732391, -1.178068619123848526 ) ) ;
#47980=( BOUNDED_CURVE ( )  B_SPLINE_CURVE ( 3, ( #160124, #78856, #190476, #27990 ),
 .UNSPECIFIED., .F., .T. ) 
 B_SPLINE_CURVE_WITH_KNOTS ( ( 4, 4 ),
 ( 3.705870088530767159, 4.712388980384695003 ),
 .UNSPECIFIED. ) 
 CURVE ( )  GEOMETRIC_REPRESENTATION_ITEM ( )  RATIONAL_B_SPLINE_CURVE ( ( 1.000000000000000000, 0.9173434942194453878, 0.9173434942194453878, 1.000000000000000000 ) ) 
 REPRESENTATION_ITEM ( '' )  );
#47983=VERTEX_POINT ( 'NONE', #213629 ) ;
#48087=AXIS2_PLACEMENT_3D ( 'NONE', #153132, #9008, #136893 ) ;
#48113=CARTESIAN_POINT ( 'NONE',  ( 1.360316468749992236, 2.765625000341414896, -4.683753385137379155E-14 ) ) ;
#48129=CARTESIAN_POINT ( 'NONE',  ( 0.4288785890452541105, 3.049942316455306113, 0.4196807566830256797 ) ) ;
#48153=ADVANCED_FACE ( 'NONE', ( #212583 ), #169962, .T. ) ;
#48229=CARTESIAN_POINT ( 'NONE',  ( -0.4170821662629279336, 3.033599471985628959, -0.4170821662629279336 ) ) ;
#48232=ORIENTED_EDGE ( 'NONE', *, *, #65201, .F. ) ;
#48252=CARTESIAN_POINT ( 'NONE',  ( -0.3282377607281349308, 2.448664549684623104, -1.225000000000029177 ) ) ;
#48267=EDGE_CURVE ( 'NONE', #98321, #75836, #38556, .T. ) ;
#48280=DIRECTION ( 'NONE',  ( 1.276756478318932585E-15, -1.000000000000000000, 1.665334536937738262E-16 ) ) ;
#48311=CARTESIAN_POINT ( 'NONE',  ( -0.3423093779010097926, 2.999999999999995559, 0.3999999999999906408 ) ) ;
#48350=FILL_AREA_STYLE_COLOUR ( '', #152055 ) ;
#48360=CARTESIAN_POINT ( 'NONE',  ( -1.360316468750013108, 2.921875000341411788, -1.734723475976807094E-14 ) ) ;
#48402=ORIENTED_EDGE ( 'NONE', *, *, #180391, .F. ) ;
#48510=CARTESIAN_POINT ( 'NONE',  ( 0.6801582343749674742, 1.755208333674734833, 1.178068619123803451 ) ) ;
#48560=CARTESIAN_POINT ( 'NONE',  ( 1.886017674307056691, 3.298060805577443411, 0.4014564593430875461 ) ) ;
#48626=CARTESIAN_POINT ( 'NONE',  ( -0.4516138619288407874, 3.070015318549076166, -0.4124855346667993805 ) ) ;
#48636=CARTESIAN_POINT ( 'NONE',  ( -0.6801582343750213200, -1.067708332991926135, 1.178068619123832983 ) ) ;
#48703=CARTESIAN_POINT ( 'NONE',  ( 0.2999999999999860556, 4.000000000000010658, 1.007084189318397938 ) ) ;
#48802=ORIENTED_EDGE ( 'NONE', *, *, #155697, .F. ) ;
#48861=CARTESIAN_POINT ( 'NONE',  ( -0.6801582343750334214, 0.3802083336747336118, -1.178068619123869398 ) ) ;
#48874=CIRCLE ( 'NONE', #114636, 1.914481421317578258 ) ;
#48899=CARTESIAN_POINT ( 'NONE',  ( -1.360316468750032870, 0.6614583336747411613, 0.7853790794158620470 ) ) ;
#48914=ORIENTED_EDGE ( 'NONE', *, *, #199415, .F. ) ;
#48923=CARTESIAN_POINT ( 'NONE',  ( -1.225000000000028066, 0.3125000006828221322, -4.336808689942017736E-14 ) ) ;
#49024=VECTOR ( 'NONE', #119671, 1000.000000000000000 ) ;
#49032=ORIENTED_EDGE ( 'NONE', *, *, #8819, .F. ) ;
#49043=FACE_OUTER_BOUND ( 'NONE', #204304, .T. ) ;
#49161=CARTESIAN_POINT ( 'NONE',  ( -1.360316468749997565, 2.890625000341401574, 1.734723475976807094E-15 ) ) ;
#49285=B_SPLINE_CURVE_WITH_KNOTS ( 'NONE', 3,
 ( #80559, #147704, #146658, #197497 ),
 .UNSPECIFIED., .F., .F.,
 ( 4, 4 ),
 ( 0.000000000000000000, 3.548791410040124229E-05 ),
 .UNSPECIFIED. ) ;
#49293=VECTOR ( 'NONE', #92118, 1000.000000000000000 ) ;
#49547=AXIS2_PLACEMENT_3D ( 'NONE', #22001, #19889, #205035 ) ;
#49554=CARTESIAN_POINT ( 'NONE',  ( 0.6801582343749761339, 1.838541667008058988, -1.178068619123876282 ) ) ;
#49579=DIRECTION ( 'NONE',  ( -0.5005768354468330683, -0.8656921114426503472, 1.942890293094028284E-15 ) ) ;
#49604=DIRECTION ( 'NONE',  ( 5.828670879282089587E-16, -0.8656921114426507913, 0.5005768354468322912 ) ) ;
#49608=CARTESIAN_POINT ( 'NONE',  ( 1.913843809498073645, 3.268536626279786805, 0.4294081188992979192 ) ) ;
#49687=CARTESIAN_POINT ( 'NONE',  ( 0.6801582343749952297, -0.9427083329919122567, -1.178068619123855409 ) ) ;
#49709=CARTESIAN_POINT ( 'NONE',  ( 0.6801582343749761339, 1.973958333674710630, 1.178068619123801675 ) ) ;
#49897=CARTESIAN_POINT ( 'NONE',  ( 0.3282377607281084519, 1.676335450315393993, -1.225000000000026512 ) ) ;
#49917=CARTESIAN_POINT ( 'NONE',  ( -1.360316468750028651, -0.5781249996585913209, -4.510281037539698445E-14 ) ) ;
#49955=CARTESIAN_POINT ( 'NONE',  ( -3.755786496842899057E-14, 1.453125000341440876, 1.570758158831776052 ) ) ;
#49976=ORIENTED_EDGE ( 'NONE', *, *, #95699, .F. ) ;
#50021=CARTESIAN_POINT ( 'NONE',  ( 1.772826578342723503, 3.950000000000526867, 0.3999999999999847566 ) ) ;
#50038=EDGE_CURVE ( 'NONE', #35460, #72572, #122072, .T. ) ;
#50089=VERTEX_POINT ( 'NONE', #147584 ) ;
#50091=AXIS2_PLACEMENT_3D ( 'NONE', #151568, #69205, #135325 ) ;
#50165=DIRECTION ( 'NONE',  ( -2.498001805406606160E-16, 0.8656921114426522346, -0.5005768354468299597 ) ) ;
#50210=CARTESIAN_POINT ( 'NONE',  ( -0.3000000000000322409, 3.975028841772310084, 0.9637995837462181026 ) ) ;
#50217=CARTESIAN_POINT ( 'NONE',  ( -3.555477883677943599E-14, 1.578125000341449535, -1.570758158831814466 ) ) ;
#50222=DIRECTION ( 'NONE',  ( 0.000000000000000000, 0.000000000000000000, 1.000000000000000000 ) ) ;
#50266=DIRECTION ( 'NONE',  ( 0.000000000000000000, 0.000000000000000000, 1.000000000000000000 ) ) ;
#50330=CARTESIAN_POINT ( 'NONE',  ( -0.5000000000000264233, 3.999999999999976019, -0.4500000000000458633 ) ) ;
#50347=DIRECTION ( 'NONE',  ( 0.8660254037844399289, -0.4999999999999976130, -6.938893903907224526E-18 ) ) ;
#50375=FACE_OUTER_BOUND ( 'NONE', #4457, .T. ) ;
#50390=PRODUCT_DEFINITION_CONTEXT ( 'detailed design', #81028, 'design' ) ;
#50462=CARTESIAN_POINT ( 'NONE',  ( -1.826099658462952746, 3.981846818258216292, -0.4000000000000286104 ) ) ;
#50487=CARTESIAN_POINT ( 'NONE',  ( 0.6124999999999655165, 0.08333333333334497217, 1.060881119635885828 ) ) ;
#50498=AXIS2_PLACEMENT_3D ( 'NONE', #204986, #154133, #188754 ) ;
#50550=CARTESIAN_POINT ( 'NONE',  ( -1.734723475976807094E-15, 2.999999999999988898, -6.938893903907228378E-15 ) ) ;
#50624=CARTESIAN_POINT ( 'NONE',  ( 1.360316468749963592, 1.317708333674712184, -0.7853790794158981292 ) ) ;
#50642=DIRECTION ( 'NONE',  ( 1.000000000000000000, -7.771561172376097755E-16, -4.440892098500627148E-16 ) ) ;
#50775=CARTESIAN_POINT ( 'NONE',  ( 0.6801582343749970061, 2.223958333674731946, 1.178068619123799898 ) ) ;
#50904=CARTESIAN_POINT ( 'NONE',  ( 1.224999999999961231, 1.416666667349490760, 0.7072540797572558491 ) ) ;
#50917=CARTESIAN_POINT ( 'NONE',  ( -0.6124999999999984901, 2.354166667349471886, 1.060881119635896264 ) ) ;
#50931=CARTESIAN_POINT ( 'NONE',  ( 1.772826578343066117, 3.950000000000009059, 0.4499999999999590994 ) ) ;
#50943=CARTESIAN_POINT ( 'NONE',  ( -0.6125000000000053735, 2.708333333333333481, -1.060881119635955327 ) ) ;
#50983=CARTESIAN_POINT ( 'NONE',  ( 0.6801582343749674742, -0.2447916663252461267, 1.178068619123796568 ) ) ;
#51024=CARTESIAN_POINT ( 'NONE',  ( 1.360316468749953600, 1.786458333674746601, -0.7853790794159161148 ) ) ;
#51047=DIRECTION ( 'NONE',  ( -1.000000000000000000, 0.000000000000000000, 0.000000000000000000 ) ) ;
#51090=DIRECTION ( 'NONE',  ( 1.000000000000000000, -7.771561172376097755E-16, -4.440892098500627148E-16 ) ) ;
#51224=FACE_OUTER_BOUND ( 'NONE', #91690, .T. ) ;
#51232=CARTESIAN_POINT ( 'NONE',  ( 0.2999999999999842792, 3.372708439410100567, -0.5000000000000299760 ) ) ;
#51290=DIRECTION ( 'NONE',  ( -1.276756478318932585E-15, 1.000000000000000000, -1.665334536937738262E-16 ) ) ;
#51320=CARTESIAN_POINT ( 'NONE',  ( -1.502314598737159228E-15, 1.125000000682793377, 1.414508159514577423 ) ) ;
#51417=VECTOR ( 'NONE', #203218, 1000.000000000000000 ) ;
#51419=DIRECTION ( 'NONE',  ( -4.163336342344327166E-17, -0.5005768354468325132, 0.8656921114426507913 ) ) ;
#51459=CARTESIAN_POINT ( 'NONE',  ( -0.3282377607281345422, 1.113835450998177157, 1.224999999999983880 ) ) ;
#51475=EDGE_CURVE ( 'NONE', #105749, #55379, #159924, .T. ) ;
#51534=FACE_OUTER_BOUND ( 'NONE', #29839, .T. ) ;
#51537=CARTESIAN_POINT ( 'NONE',  ( -1.360316468750007779, 2.171875000341411344, -4.336808689942017736E-14 ) ) ;
#51561=CARTESIAN_POINT ( 'NONE',  ( -1.225000000000038058, 0.4791666666666983265, -0.7072540797573158011 ) ) ;
#51629=DIRECTION ( 'NONE',  ( -3.330669073875479975E-16, 2.334947598634344260E-16, 1.000000000000000000 ) ) ;
#51644=LINE ( 'NONE', #117768, #193187 ) ;
#51700=ORIENTED_EDGE ( 'NONE', *, *, #139653, .T. ) ;
#51712=CARTESIAN_POINT ( 'NONE',  ( -5.558564015327488080E-14, 0.4843750003414603600, 1.570758158831762286 ) ) ;
#51760=CARTESIAN_POINT ( 'NONE',  ( -0.3282377607281419252, 0.8638354509981874818, 1.224999999999977440 ) ) ;
#51856=CARTESIAN_POINT ( 'NONE',  ( 0.6801582343749796866, 1.723958333674766141, 1.178068619123784355 ) ) ;
#51884=CARTESIAN_POINT ( 'NONE',  ( 1.931056844935808314, 3.481093093210268830, -0.4000000000000272227 ) ) ;
#51941=CARTESIAN_POINT ( 'NONE',  ( -1.914442667406943910, 3.262253226108043247, -0.4355078757044400506 ) ) ;
#51956=ORIENTED_EDGE ( 'NONE', *, *, #181210, .F. ) ;
#51960=CARTESIAN_POINT ( 'NONE',  ( -2.449742653233033085, 3.949999999999988187, 0.4499999999999608757 ) ) ;
#52005=VERTEX_POINT ( 'NONE', #98793 ) ;
#52006=CARTESIAN_POINT ( 'NONE',  ( 0.2999999999999869993, 3.999999999999974243, -0.9782388782689304119 ) ) ;
#52013=CARTESIAN_POINT ( 'NONE',  ( 0.4465194593917843902, 3.080450244942134486, 0.4155024747329351120 ) ) ;
#52016=CARTESIAN_POINT ( 'NONE',  ( -1.225000000000047162, -0.1874999993171852508, -2.775557561562891351E-14 ) ) ;
#52024=FACE_OUTER_BOUND ( 'NONE', #124803, .T. ) ;
#52040=CARTESIAN_POINT ( 'NONE',  ( 0.3282377607281163345, 1.136164550367434467, 1.224999999999968114 ) ) ;
#52050=CARTESIAN_POINT ( 'NONE',  ( -3.956095110007852622E-14, -0.1406249996585586248, -1.570758158831808249 ) ) ;
#52089=CARTESIAN_POINT ( 'NONE',  ( -1.953008978358306879E-14, 0.7031250003414775129, 1.570758158831782048 ) ) ;
#52098=CARTESIAN_POINT ( 'NONE',  ( -0.3282377607281426468, 1.863835450998160281, 1.224999999999969003 ) ) ;
#52348=( BOUNDED_CURVE ( )  B_SPLINE_CURVE ( 2, ( #119346, #185333, #181080, #161, #7641, #21743, #186399, #203702, #124699 ),
 .UNSPECIFIED., .F., .T. ) 
 B_SPLINE_CURVE_WITH_KNOTS ( ( 3, 2, 2, 2, 3 ),
 ( 0.5781250000000001110, 0.5833333333333333703, 0.5937500000000000000, 0.6041666666666666297, 0.6093749999999996669 ),
 .UNSPECIFIED. ) 
 CURVE ( )  GEOMETRIC_REPRESENTATION_ITEM ( )  RATIONAL_B_SPLINE_CURVE ( ( 0.9330127018922192983, 0.9330127018922207416, 1.000000000000000000, 0.8660254037844387076, 1.000000000000000000, 0.8660254037844387076, 1.000000000000000000, 0.9330127018922236282, 0.9330127018922194093 ) ) 
 REPRESENTATION_ITEM ( '' )  );
#52385=CARTESIAN_POINT ( 'NONE',  ( -7.511572993685796537E-15, 1.750000000682812251, -1.414508159514599628 ) ) ;
#52417=( BOUNDED_CURVE ( )  B_SPLINE_CURVE ( 3, ( #91452, #57858, #138056, #121875 ),
 .UNSPECIFIED., .F., .T. ) 
 B_SPLINE_CURVE_WITH_KNOTS ( ( 4, 4 ),
 ( 4.712388980384560000, 5.557022599642902350 ),
 .UNSPECIFIED. ) 
 CURVE ( )  GEOMETRIC_REPRESENTATION_ITEM ( )  RATIONAL_B_SPLINE_CURVE ( ( 1.000000000000000000, 0.9414278581755095576, 0.9414278581755095576, 1.000000000000000000 ) ) 
 REPRESENTATION_ITEM ( '' )  );
#52450=LINE ( 'NONE', #118576, #153418 ) ;
#52591=CARTESIAN_POINT ( 'NONE',  ( -1.360316468750004448, 1.671875000341424666, -8.673617379884035472E-15 ) ) ;
#52612=CARTESIAN_POINT ( 'NONE',  ( -1.225000000000040279, 0.2500000000000002220, -4.857225732735059864E-14 ) ) ;
#52662=CARTESIAN_POINT ( 'NONE',  ( 0.6760876847618801921, -1.398214087147084248E-14, 1.193909349079574245 ) ) ;
#52715=EDGE_LOOP ( 'NONE', ( #54452, #126809, #113120, #110162, #34076, #169516, #157038, #85244 ) ) ;
#52759=CARTESIAN_POINT ( 'NONE',  ( 1.360316468749989571, 0.5677083336747246189, -0.7853790794158941324 ) ) ;
#52803=CARTESIAN_POINT ( 'NONE',  ( 0.6124999999999862776, 1.083333333333352799, 1.060881119635887604 ) ) ;
#52841=AXIS2_PLACEMENT_3D ( 'NONE', #106769, #89416, #74222 ) ;
#52907=CARTESIAN_POINT ( 'NONE',  ( -3.555477883677943599E-14, 1.578125000341449535, -1.570758158831814466 ) ) ;
#52977=CARTESIAN_POINT ( 'NONE',  ( -5.358255402162534516E-14, 2.562499999999964473, 1.414508159514571428 ) ) ;
#53009=DIRECTION ( 'NONE',  ( 0.000000000000000000, 0.000000000000000000, 1.000000000000000000 ) ) ;
#53064=CARTESIAN_POINT ( 'NONE',  ( 0.4288785890452541105, 3.049942316455306113, 0.4196807566830256797 ) ) ;
#53068=CARTESIAN_POINT ( 'NONE',  ( 0.6124999999999534150, -1.104166665983841167, 1.060881119635882497 ) ) ;
#53087=ORIENTED_EDGE ( 'NONE', *, *, #118912, .F. ) ;
#53150=CARTESIAN_POINT ( 'NONE',  ( -1.360316468750013108, 1.140625000341413564, -2.081668171172168513E-14 ) ) ;
#53218=CARTESIAN_POINT ( 'NONE',  ( 1.947569660854353790, 3.752493983412333645, 0.4616071351972801939 ) ) ;
#53279=ORIENTED_EDGE ( 'NONE', *, *, #174533, .T. ) ;
#53338=DIRECTION ( 'NONE',  ( 1.000000000000000000, -7.771561172376096769E-16, -4.440892098500627148E-16 ) ) ;
#53348=CARTESIAN_POINT ( 'NONE',  ( 0.3282377607281172782, 0.4263354503153867214, -1.225000000000017852 ) ) ;
#53408=VERTEX_POINT ( 'NONE', #65216 ) ;
#53443=CARTESIAN_POINT ( 'NONE',  ( -1.225000000000044276, 1.791666667349484321, -0.7072540797573277915 ) ) ;
#53504=CARTESIAN_POINT ( 'NONE',  ( -0.4000000000000236144, -3.469446951953614189E-14, -3.989863994746656317E-14 ) ) ;
#53572=LINE ( 'NONE', #85001, #54653 ) ;
#53580=CARTESIAN_POINT ( 'NONE',  ( 3.602337597214539753E-15, 1.000000000682806034, -1.225000000000015410 ) ) ;
#53658=CARTESIAN_POINT ( 'NONE',  ( -1.360316468750036645, 1.901041667008058988, -0.7853790794159222211 ) ) ;
#53679=( BOUNDED_SURFACE ( )  B_SPLINE_SURFACE ( 3, 2, ( 
 ( #86221, #167476, #183715 ),
 ( #19071, #87289, #214046 ),
 ( #99288, #35323, #17995 ),
 ( #101401, #181575, #182643 ) ),
 .UNSPECIFIED., .F., .F., .T. ) 
 B_SPLINE_SURFACE_WITH_KNOTS ( ( 4, 4 ),
 ( 3, 3 ),
 ( 1.570796326794896558, 2.636531018672052085 ),
 ( 0.000000000000000000, 1.000000000000000000 ),
 .UNSPECIFIED. ) 
 GEOMETRIC_REPRESENTATION_ITEM ( )  RATIONAL_B_SPLINE_SURFACE ( (
 ( 1.000000000000000000, 0.7071067811865716646, 1.000000000000000000),
 ( 1.000000000000000000, 0.8161930835858144384, 1.000000000000000000),
 ( 1.000000000000000000, 0.8980788380693711659, 1.000000000000000000),
 ( 1.000000000000000000, 0.9374448844494299715, 1.000000000000000000) ) ) 
 REPRESENTATION_ITEM ( '' )  SURFACE ( )  );
#53682=CARTESIAN_POINT ( 'NONE',  ( -0.6125000000000314637, 0.9583333333333388104, -1.060881119635965764 ) ) ;
#53696=CARTESIAN_POINT ( 'NONE',  ( -0.5000000000000038858, 3.949999999999995293, -0.4000000000000166755 ) ) ;
#53788=VERTEX_POINT ( 'NONE', #40211 ) ;
#53951=DIRECTION ( 'NONE',  ( 1.276756478318932585E-15, -1.000000000000000000, 1.665334536937738262E-16 ) ) ;
#53980=ORIENTED_EDGE ( 'NONE', *, *, #57301, .T. ) ;
#53982=CARTESIAN_POINT ( 'NONE',  ( 0.6801582343749813520, 0.2239583336747300035, 1.178068619123796568 ) ) ;
#54055=CARTESIAN_POINT ( 'NONE',  ( -3.956095110007852622E-14, 2.937500000000021760, -1.414508159514583419 ) ) ;
#54089=CARTESIAN_POINT ( 'NONE',  ( -1.914442667406964116, 3.262253226107984183, 0.4355078757043848170 ) ) ;
#54098=ORIENTED_EDGE ( 'NONE', *, *, #89413, .F. ) ;
#54102=CARTESIAN_POINT ( 'NONE',  ( 1.157928058570472318, -6.779921613290400011E-15, -0.6014056109540196760 ) ) ;
#54147=CARTESIAN_POINT ( 'NONE',  ( -0.6125000000000053735, -1.145833332650537884, 1.060881119635925796 ) ) ;
#54179=CARTESIAN_POINT ( 'NONE',  ( -0.6801582343750559589, -0.03645833299194961574, 1.178068619123796568 ) ) ;
#54214=CARTESIAN_POINT ( 'NONE',  ( -1.360316468750008667, 2.369791667008076974, -0.7853790794159001276 ) ) ;
#54223=CARTESIAN_POINT ( 'NONE',  ( 1.360316468749988683, 0.2656250003413990202, -1.387778780781445676E-14 ) ) ;
#54280=ADVANCED_FACE ( 'NONE', ( #107403 ), #132586, .T. ) ;
#54386=EDGE_LOOP ( 'NONE', ( #149977, #174401, #94219, #193501, #85663, #8235 ) ) ;
#54387=CARTESIAN_POINT ( 'NONE',  ( -0.4000000000000166755, 3.949999999999995293, -0.8338124244296005738 ) ) ;
#54452=ORIENTED_EDGE ( 'NONE', *, *, #118396, .T. ) ;
#54496=CARTESIAN_POINT ( 'NONE',  ( -0.4288785890453234995, 3.049942316455299451, -0.4196807566834767078 ) ) ;
#54513=AXIS2_PLACEMENT_3D ( 'NONE', #202513, #20572, #102909 ) ;
#54517=CARTESIAN_POINT ( 'NONE',  ( 1.224999999999961009, 1.416666667349490538, 0.7072540797572558491 ) ) ;
#54633=CARTESIAN_POINT ( 'NONE',  ( 0.3999999999999858113, 3.372708439410149417, -0.5000000000000373035 ) ) ;
#54653=VECTOR ( 'NONE', #153208, 1000.000000000000114 ) ;
#54725=CARTESIAN_POINT ( 'NONE',  ( -9.514659125335341649E-15, 1.359375000341400463, -1.570758158831806250 ) ) ;
#54747=CARTESIAN_POINT ( 'NONE',  ( -1.225000000000042277, 0.5208333333333544646, 0.7072540797572777205 ) ) ;
#54768=ORIENTED_EDGE ( 'NONE', *, *, #202175, .F. ) ;
#54770=EDGE_CURVE ( 'NONE', #41218, #143294, #160389, .T. ) ;
#54790=CARTESIAN_POINT ( 'NONE',  ( 0.4499999999999764744, 3.999999999999955147, 0.4999999999999813483 ) ) ;
#54847=CARTESIAN_POINT ( 'NONE',  ( -1.162044386198238935E-15, 2.625000000682799151, 1.224999999999985656 ) ) ;
#54901=CARTESIAN_POINT ( 'NONE',  ( 0.6801582343749970061, 0.8385416670080649837, -1.178068619123841643 ) ) ;
#55037=CARTESIAN_POINT ( 'NONE',  ( -1.946531837068944615, 3.754233237397059497, -0.4615996190889526951 ) ) ;
#55050=CARTESIAN_POINT ( 'NONE',  ( -1.360316468750023544, 0.8906250003414064587, -2.602085213965210642E-14 ) ) ;
#55093=LINE ( 'NONE', #174203, #28039 ) ;
#55122=CARTESIAN_POINT ( 'NONE',  ( -0.6124999999999967137, 1.708333333333339477, -1.060881119635938008 ) ) ;
#55213=CARTESIAN_POINT ( 'NONE',  ( 0.6124999999999550804, -0.02083333265050224536, -1.060881119635993519 ) ) ;
#55216=VECTOR ( 'NONE', #96504, 1000.000000000000000 ) ;
#55280=CARTESIAN_POINT ( 'NONE',  ( -2.353626204688216217E-14, 2.453125000341405570, 1.570758158831792262 ) ) ;
#55288=CARTESIAN_POINT ( 'NONE',  ( -1.360316468749999119, 0.3906250003414130090, -8.673617379884035472E-15 ) ) ;
#55298=VERTEX_POINT ( 'NONE', #201009 ) ;
#55352=CARTESIAN_POINT ( 'NONE',  ( 1.898855744251417788, 3.739179606816488199, 0.3999999999999848677 ) ) ;
#55379=VERTEX_POINT ( 'NONE', #198878 ) ;
#55434=DIRECTION ( 'NONE',  ( 1.276756478318932585E-15, -1.000000000000000000, 1.665334536937738262E-16 ) ) ;
#55482=DIRECTION ( 'NONE',  ( 1.000000000000000000, 0.000000000000000000, 0.000000000000000000 ) ) ;
#55583=CARTESIAN_POINT ( 'NONE',  ( 0.6125000000000019318, 1.229166667349464115, -1.060881119635941339 ) ) ;
#55688=VERTEX_POINT ( 'NONE', #203156 ) ;
#55789=CARTESIAN_POINT ( 'NONE',  ( -0.6801582343750386395, 2.380208333674735499, -1.178068619123869398 ) ) ;
#55813=CARTESIAN_POINT ( 'NONE',  ( 1.225000000000008971, -0.6250000000000005551, -1.561251128379126385E-14 ) ) ;
#55962=LINE ( 'NONE', #57031, #95710 ) ;
#55970=CARTESIAN_POINT ( 'NONE',  ( 1.360316468749989571, 0.8177083336747339448, -0.7853790794159001276 ) ) ;
#56003=CARTESIAN_POINT ( 'NONE',  ( 0.3713344243775092424, 2.999999999999998668, -0.3713344243776030007 ) ) ;
#56015=CARTESIAN_POINT ( 'NONE',  ( -0.5000000000000056621, 3.172938907704293765, -0.4000000000000305533 ) ) ;
#56038=VERTEX_POINT ( 'NONE', #178161 ) ;
#56108=ORIENTED_EDGE ( 'NONE', *, *, #44491, .F. ) ;
#56118=CARTESIAN_POINT ( 'NONE',  ( -0.6801582343750022241, -0.1510416663252633906, -1.178068619123841643 ) ) ;
#56177=ADVANCED_FACE ( 'NONE', ( #60126 ), #77340, .T. ) ;
#56188=CARTESIAN_POINT ( 'NONE',  ( -1.225000000000045386, 2.250000000000001776, -4.683753385137379155E-14 ) ) ;
#56227=DIRECTION ( 'NONE',  ( -3.330669073875472579E-16, 1.665334536937734318E-16, 1.000000000000000000 ) ) ;
#56232=CARTESIAN_POINT ( 'NONE',  ( 1.872871967411074756, 3.299999999999997158, -0.4000000000000131783 ) ) ;
#56270=CARTESIAN_POINT ( 'NONE',  ( 0.4465194593917913846, 3.080450244942120719, -0.4155024747329958412 ) ) ;
#56280=CARTESIAN_POINT ( 'NONE',  ( 0.6125000000000019318, -1.020833332650530778, -1.060881119635948444 ) ) ;
#56307=EDGE_LOOP ( 'NONE', ( #170664, #200986, #75474, #162678 ) ) ;
#56346=CARTESIAN_POINT ( 'NONE',  ( -1.360316468750007779, 2.390625000341400685, -1.734723475976807094E-15 ) ) ;
#56353=CARTESIAN_POINT ( 'NONE',  ( 1.360316468749949825, 0.2447916670081152490, 0.7853790794158739264 ) ) ;
#56392=CARTESIAN_POINT ( 'NONE',  ( 0.4999999999999622524, 2.999999999999960920, -0.4000000000000305533 ) ) ;
#56395=AXIS2_PLACEMENT_3D ( 'NONE', #126151, #209424, #187849 ) ;
#56410=VECTOR ( 'NONE', #15625, 1000.000000000000000 ) ;
#56495=CARTESIAN_POINT ( 'NONE',  ( -1.214306433183764966E-14, 3.299999999999969624, -3.122502256758252770E-14 ) ) ;
#56547=CARTESIAN_POINT ( 'NONE',  ( -0.6125000000000383471, 0.6041666673494219264, 1.060881119635901593 ) ) ;
#56557=CARTESIAN_POINT ( 'NONE',  ( 1.224999999999982991, 1.395833333333318826, -0.7072540797572817173 ) ) ;
#56580=CARTESIAN_POINT ( 'NONE',  ( 0.6801582343749761339, 1.838541667008058988, -1.178068619123876282 ) ) ;
#56627=ADVANCED_FACE ( 'NONE', ( #23083 ), #155251, .T. ) ;
#56657=CARTESIAN_POINT ( 'NONE',  ( -1.225000000000030065, 0.3333333340161495628, 0.7072540797572656190 ) ) ;
#56748=CARTESIAN_POINT ( 'NONE',  ( 1.225000000000000977, 0.6458333333333310389, -0.7072540797572937077 ) ) ;
#56761=CARTESIAN_POINT ( 'NONE',  ( 0.3817069231124412543, 4.000000000000008882, 1.007084182327167454 ) ) ;
#56764=ORIENTED_EDGE ( 'NONE', *, *, #209073, .F. ) ;
#56767=CARTESIAN_POINT ( 'NONE',  ( 4.067155351693835485E-15, 1.250000000682825130, -1.225000000000013411 ) ) ;
#56821=CARTESIAN_POINT ( 'NONE',  ( -1.224999999999995204, 3.000000000000002665, -1.387778780781445676E-14 ) ) ;
#56862=CARTESIAN_POINT ( 'NONE',  ( 1.360316468749955598, 0.5260416670081085044, 0.7853790794158820310 ) ) ;
#56883=CARTESIAN_POINT ( 'NONE',  ( -1.225000000000036060, 0.02083333333335212617, 0.7072540797572677285 ) ) ;
#56993=ORIENTED_EDGE ( 'NONE', *, *, #129837, .F. ) ;
#57031=CARTESIAN_POINT ( 'NONE',  ( -1.326716514427061987E-15, 2.999999999999988454, -1.225000000000003864 ) ) ;
#57038=AXIS2_PLACEMENT_3D ( 'NONE', #126600, #110339, #160083 ) ;
#57095=DIRECTION ( 'NONE',  ( 1.276756478318932585E-15, -1.000000000000000000, 1.665334536937738262E-16 ) ) ;
#57183=CARTESIAN_POINT ( 'NONE',  ( -0.6801582343750125492, 1.098958333674737720, -1.178068619123855409 ) ) ;
#57256=CARTESIAN_POINT ( 'NONE',  ( -3.755786496842897795E-14, 1.937500000000033085, -1.414508159514593411 ) ) ;
#57301=EDGE_CURVE ( 'NONE', #80420, #112800, #55093, .T. ) ;
#57363=VECTOR ( 'NONE', #121652, 1000.000000000000000 ) ;
#57407=CARTESIAN_POINT ( 'NONE',  ( -0.6801582343750004478, 2.348958333674739052, -1.178068619123869398 ) ) ;
#57443=( BOUNDED_SURFACE ( )  B_SPLINE_SURFACE ( 3, 2, ( 
 ( #113815, #145218, #127964 ),
 ( #179815, #144161, #196070 ),
 ( #210153, #193916, #78037 ),
 ( #60718, #212285, #80168 ) ),
 .UNSPECIFIED., .F., .F., .F. ) 
 B_SPLINE_SURFACE_WITH_KNOTS ( ( 4, 4 ),
 ( 3, 3 ),
 ( 0.0002170249176783703470, 0.0009435326495461454589 ),
 ( 0.000000000000000000, 1.000000000000000000 ),
 .UNSPECIFIED. ) 
 GEOMETRIC_REPRESENTATION_ITEM ( )  RATIONAL_B_SPLINE_SURFACE ( (
 ( 1.000000000000000000, 0.6273451206645686007, 1.000000000000000000),
 ( 1.000000000000000000, 0.6198154398457387249, 1.000000000000000000),
 ( 1.000000000000000000, 0.6183696555398903172, 1.000000000000000000),
 ( 1.000000000000000000, 0.6222646319068203535, 1.000000000000000000) ) ) 
 REPRESENTATION_ITEM ( '' )  SURFACE ( )  );
#57643=CARTESIAN_POINT ( 'NONE',  ( 0.6801582343749987825, 2.338541667008108060, -1.178068619123883165 ) ) ;
#57698=CARTESIAN_POINT ( 'NONE',  ( -0.4170821662629279336, 3.033599471985628959, -0.4170821662629279336 ) ) ;
#57722=CARTESIAN_POINT ( 'NONE',  ( -1.225000000000044276, 1.083333334016145066, 0.7072540797572517413 ) ) ;
#57768=VECTOR ( 'NONE', #9639, 1000.000000000000000 ) ;
#57775=CARTESIAN_POINT ( 'NONE',  ( -1.225000000000014078, 1.479166666666654972, -0.7072540797573017013 ) ) ;
#57858=CARTESIAN_POINT ( 'NONE',  ( 0.3713344243775348885, 3.000000000000001776, 0.3713344243775348885 ) ) ;
#57876=CARTESIAN_POINT ( 'NONE',  ( -1.225000000000045386, 2.250000000000001776, -4.683753385137379155E-14 ) ) ;
#57927=CARTESIAN_POINT ( 'NONE',  ( 1.360316468749989793, 0.5677083336747246189, -0.7853790794158941324 ) ) ;
#57949=CARTESIAN_POINT ( 'NONE',  ( -1.151774525698488676E-14, -0.6874999999999952260, 1.414508159514557439 ) ) ;
#58063=AXIS2_PLACEMENT_3D ( 'NONE', #38660, #105830, #156689 ) ;
#58161=CARTESIAN_POINT ( 'NONE',  ( 6.856061878569608298E-15, 0.1875000000000181521, -1.225000000000034950 ) ) ;
#58247=CARTESIAN_POINT ( 'NONE',  ( -1.360316468750021768, 0.6406250003414132310, -3.469446951953614189E-14 ) ) ;
#58261=ORIENTED_EDGE ( 'NONE', *, *, #59473, .T. ) ;
#58319=CARTESIAN_POINT ( 'NONE',  ( -2.153317591523261390E-14, 2.187499999999986233, -1.414508159514625385 ) ) ;
#58354=CARTESIAN_POINT ( 'NONE',  ( -0.6801582343750386395, 2.380208333674735499, -1.178068619123869398 ) ) ;
#58365=AXIS2_PLACEMENT_3D ( 'NONE', #131294, #80344, #51047 ) ;
#58461=CARTESIAN_POINT ( 'NONE',  ( -0.6311622855796912290, 3.299999999999990496, -0.4000000000000270561 ) ) ;
#58477=CARTESIAN_POINT ( 'NONE',  ( 1.360316468749983576, 0.9947916670081107249, 0.7853790794158601596 ) ) ;
#58485=CARTESIAN_POINT ( 'NONE',  ( 1.360316468749978025, 0.5364583336746844289, -0.7853790794159001276 ) ) ;
#58509=CARTESIAN_POINT ( 'NONE',  ( 1.913843478179629631, 3.256154753185150241, -0.4414708703500153653 ) ) ;
#58521=CARTESIAN_POINT ( 'NONE',  ( 0.3282377607280981269, 2.426335450315351139, -1.225000000000014300 ) ) ;
#58547=DIRECTION ( 'NONE',  ( -3.330669073875478989E-16, 3.540251991789410786E-16, 1.000000000000000000 ) ) ;
#58549=CARTESIAN_POINT ( 'NONE',  ( 1.997444822565041855, 3.480956003828838075, 0.4000000000000185074 ) ) ;
#58606=ORIENTED_EDGE ( 'NONE', *, *, #92773, .F. ) ;
#58649=ORIENTED_EDGE ( 'NONE', *, *, #10768, .T. ) ;
#58706=CARTESIAN_POINT ( 'NONE',  ( 1.360316468750005559, 1.567708333674729282, -0.7853790794158981292 ) ) ;
#58724=AXIS2_PLACEMENT_3D ( 'NONE', #102819, #88713, #20478 ) ;
#58774=AXIS2_PLACEMENT_3D ( 'NONE', #197951, #210997, #163344 ) ;
#58784=CARTESIAN_POINT ( 'NONE',  ( -1.225000000000040057, 0.5833333340161187541, 0.7072540797572817173 ) ) ;
#58897=CARTESIAN_POINT ( 'NONE',  ( 0.4123176713737538024, 4.000000000000008882, 0.8977835139437831957 ) ) ;
#58997=CARTESIAN_POINT ( 'NONE',  ( -0.6801582343750022241, 1.130208333674734167, -1.178068619123841643 ) ) ;
#59016=CARTESIAN_POINT ( 'NONE',  ( -1.360316468750038643, 2.901041667008071645, -0.7853790794159161148 ) ) ;
#59081=DIRECTION ( 'NONE',  ( -1.000000000000000000, 0.000000000000000000, 4.336808689942015369E-15 ) ) ;
#59127=DIRECTION ( 'NONE',  ( -9.436895709313856232E-16, 0.8656921114426506803, 0.5005768354468324022 ) ) ;
#59153=ORIENTED_EDGE ( 'NONE', *, *, #95699, .T. ) ;
#59307=CARTESIAN_POINT ( 'NONE',  ( 1.360316468749981800, -1.005208332991882614, 0.7853790794158560518 ) ) ;
#59375=ORIENTED_EDGE ( 'NONE', *, *, #201642, .T. ) ;
#59473=EDGE_CURVE ( 'NONE', #133087, #160120, #16784, .T. ) ;
#59531=CARTESIAN_POINT ( 'NONE',  ( 1.360316468749949825, 0.2447916670081152490, 0.7853790794158741484 ) ) ;
#59606=CARTESIAN_POINT ( 'NONE',  ( 0.4254946254913888892, 3.044090126848115307, -0.4192457809237770117 ) ) ;
#59680=DIRECTION ( 'NONE',  ( -1.000000000000000000, 7.771561172376097755E-16, 4.440892098500627148E-16 ) ) ;
#59768=CARTESIAN_POINT ( 'NONE',  ( -6.960724307482170605E-14, 1.484375000341481066, 1.570758158831758289 ) ) ;
#59806=DIRECTION ( 'NONE',  ( -3.330669073875478989E-16, 3.330669073875478989E-16, 1.000000000000000000 ) ) ;
#59826=VERTEX_POINT ( 'NONE', #139105 ) ;
#59849=CARTESIAN_POINT ( 'NONE',  ( -0.6125000000000089262, 0.02083333401611819902, -1.060881119635969094 ) ) ;
#59865=DIRECTION ( 'NONE',  ( 3.330669073875479482E-16, -3.330669073875479482E-16, -1.000000000000000000 ) ) ;
#59971=CARTESIAN_POINT ( 'NONE',  ( -1.734723475976807094E-15, 2.999999999999988898, -6.938893903907228378E-15 ) ) ;
#60021=CARTESIAN_POINT ( 'NONE',  ( -0.3282377607281422582, 2.948664549684636427, -1.225000000000019851 ) ) ;
#60062=CARTESIAN_POINT ( 'NONE',  ( -2.353626204688216217E-14, 0.1093750003414345612, -1.570758158831782270 ) ) ;
#60081=CARTESIAN_POINT ( 'NONE',  ( -4.356712336337761644E-14, 2.859375000341351392, -1.570758158831810247 ) ) ;
#60116=ORIENTED_EDGE ( 'NONE', *, *, #42362, .F. ) ;
#60126=FACE_OUTER_BOUND ( 'NONE', #126371, .T. ) ;
#60369=CARTESIAN_POINT ( 'NONE',  ( -1.360316468750006225, -0.3593749996585737794, -1.734723475976807094E-15 ) ) ;
#60474=CARTESIAN_POINT ( 'NONE',  ( 1.360316468749961594, 2.817708333674743049, -0.7853790794159141164 ) ) ;
#60522=CARTESIAN_POINT ( 'NONE',  ( -1.992711204631002198E-15, 2.999999999999989342, 1.224999999999989875 ) ) ;
#60534=CARTESIAN_POINT ( 'NONE',  ( -0.3000000000000103140, 3.322650755865456773, 0.5865692111442551981 ) ) ;
#60599=CARTESIAN_POINT ( 'NONE',  ( -1.360316468750046859, 0.6197916670081009549, -0.7853790794159322131 ) ) ;
#60614=CARTESIAN_POINT ( 'NONE',  ( 0.3776192402222087741, 3.049641483663570352, -0.4287046358292833648 ) ) ;
#60633=CARTESIAN_POINT ( 'NONE',  ( 1.904329973710251034, 3.286760881231379106, -0.4119279214153375723 ) ) ;
#60718=CARTESIAN_POINT ( 'NONE',  ( -1.859587702710848944, 3.245828361968106535, 0.3999999999999837574 ) ) ;
#60812=CARTESIAN_POINT ( 'NONE',  ( 0.3282377607281167786, 1.323664549684625324, 1.224999999999979217 ) ) ;
#60836=CARTESIAN_POINT ( 'NONE',  ( -3.355169270512988773E-14, 1.234375000341463968, 1.570758158831764062 ) ) ;
#60845=ORIENTED_EDGE ( 'NONE', *, *, #196992, .F. ) ;
#60855=AXIS2_PLACEMENT_3D ( 'NONE', #183452, #200746, #50266 ) ;
#60873=CARTESIAN_POINT ( 'NONE',  ( -1.360316468750006225, 2.640625000341401130, 3.469446951953614189E-15 ) ) ;
#60914=VERTEX_POINT ( 'NONE', #201479 ) ;
#60956=CARTESIAN_POINT ( 'NONE',  ( -1.772826578343126736, 4.000000000000003553, 0.4499999999999538813 ) ) ;
#61007=ORIENTED_EDGE ( 'NONE', *, *, #161592, .F. ) ;
#61014=CARTESIAN_POINT ( 'NONE',  ( 0.6124999999999967137, 0.5833333333333314830, 1.060881119635929348 ) ) ;
#61048=CARTESIAN_POINT ( 'NONE',  ( -0.6125000000000053735, 2.020833334016133964, -1.060881119635941339 ) ) ;
#61084=CARTESIAN_POINT ( 'NONE',  ( -0.6125000000000158096, 0.1041666673494701101, 1.060881119635906700 ) ) ;
#61099=ORIENTED_EDGE ( 'NONE', *, *, #115015, .T. ) ;
#61131=CARTESIAN_POINT ( 'NONE',  ( -1.360316468750042862, 0.1510416670080827195, -0.7853790794159282163 ) ) ;
#61236=LINE ( 'NONE', #193364, #174382 ) ;
#61280=EDGE_LOOP ( 'NONE', ( #15850, #124326, #151645, #27339 ) ) ;
#61376=EDGE_CURVE ( 'NONE', #160120, #138011, #24876, .T. ) ;
#61416=DIRECTION ( 'NONE',  ( 1.276756478318932585E-15, -1.000000000000000000, 1.665334536937738262E-16 ) ) ;
#61442=CARTESIAN_POINT ( 'NONE',  ( -1.360316468750030428, -0.6093749996585878792, -1.908195823574487804E-14 ) ) ;
#61523=DIRECTION ( 'NONE',  ( 0.2460297208025343518, 8.326672684688694761E-16, 0.9692622846690297500 ) ) ;
#61544=CARTESIAN_POINT ( 'NONE',  ( -0.6801582343750108839, 2.880208333674722176, -1.178068619123848526 ) ) ;
#61547=EDGE_CURVE ( 'NONE', #34023, #149597, #73640, .T. ) ;
#61549=EDGE_LOOP ( 'NONE', ( #111173, #153638, #147456 ) ) ;
#61620=EDGE_CURVE ( 'NONE', #143294, #125996, #105738, .T. ) ;
#61669=ORIENTED_EDGE ( 'NONE', *, *, #76744, .F. ) ;
#61673=CARTESIAN_POINT ( 'NONE',  ( 1.360316468749963592, 0.03645833367470611985, -0.7853790794159122290 ) ) ;
#61908=CARTESIAN_POINT ( 'NONE',  ( 1.360316468749955598, 0.5260416670081085044, 0.7853790794158820310 ) ) ;
#61933=VERTEX_POINT ( 'NONE', #196981 ) ;
#61946=CARTESIAN_POINT ( 'NONE',  ( -4.957638175832625493E-14, 2.078125000341435769, -1.570758158831802254 ) ) ;
#61967=ORIENTED_EDGE ( 'NONE', *, *, #170552, .T. ) ;
#62036=VERTEX_POINT ( 'NONE', #98424 ) ;
#62104=ORIENTED_EDGE ( 'NONE', *, *, #136759, .F. ) ;
#62112=VERTEX_POINT ( 'NONE', #73098 ) ;
#62207=CARTESIAN_POINT ( 'NONE',  ( 1.360316468749971364, -0.7031249996586053097, -3.469446951953614189E-14 ) ) ;
#62408=DIRECTION ( 'NONE',  ( 3.219646771412963434E-15, 1.665334536937739741E-16, 1.000000000000000000 ) ) ;
#62450=CARTESIAN_POINT ( 'NONE',  ( 0.6801582343749831283, 2.755208333674742605, 1.178068619123796568 ) ) ;
#62460=LINE ( 'NONE', #111284, #85573 ) ;
#62493=VERTEX_POINT ( 'NONE', #120884 ) ;
#62503=ORIENTED_EDGE ( 'NONE', *, *, #61376, .F. ) ;
#62504=CARTESIAN_POINT ( 'NONE',  ( -5.558564015327489343E-14, -0.4218749996585599571, -1.570758158831802254 ) ) ;
#62601=CARTESIAN_POINT ( 'NONE',  ( -1.360316468750032870, 0.9427083336747505982, 0.7853790794158641564 ) ) ;
#62604=AXIS2_PLACEMENT_3D ( 'NONE', #192868, #206991, #95419 ) ;
#62622=CARTESIAN_POINT ( 'NONE',  ( -5.204170427930421283E-14, 3.949999999999960654, -4.683753385137379155E-14 ) ) ;
#62726=CARTESIAN_POINT ( 'NONE',  ( -1.360316468750042862, -0.08854166632527044056, 0.7853790794158801436 ) ) ;
#62734=CARTESIAN_POINT ( 'NONE',  ( -1.214306433183764966E-14, 3.299999999999969624, -3.122502256758252770E-14 ) ) ;
#62740=CARTESIAN_POINT ( 'NONE',  ( 0.3788956605885723250, 3.049042541176466337, -0.4283520265746156852 ) ) ;
#62748=CARTESIAN_POINT ( 'NONE',  ( -0.6801582343750282034, 2.682291667008049441, 1.178068619123805227 ) ) ;
#62804=CARTESIAN_POINT ( 'NONE',  ( 4.067155351693835485E-15, 0.2500000006828133059, -1.225000000000014300 ) ) ;
#62818=EDGE_CURVE ( 'NONE', #50089, #126346, #116085, .T. ) ;
#62917=CARTESIAN_POINT ( 'NONE',  ( -5.265089941164633594E-14, 3.949999999999961542, 1.829047314007895997 ) ) ;
#62935=EDGE_LOOP ( 'NONE', ( #112309, #92282, #102310 ) ) ;
#62961=CARTESIAN_POINT ( 'NONE',  ( -0.6801582343750177673, 0.9635416670080582113, 1.178068619123796568 ) ) ;
#62971=VERTEX_POINT ( 'NONE', #105137 ) ;
#62999=DIRECTION ( 'NONE',  ( -1.276756478318932191E-15, 1.000000000000000000, -3.330669073875483426E-16 ) ) ;
#63001=CARTESIAN_POINT ( 'NONE',  ( -2.353626204688216217E-14, 2.453125000341405570, 1.570758158831792262 ) ) ;
#63265=CARTESIAN_POINT ( 'NONE',  ( -0.6801582343750229853, -0.3697916663252601155, -1.178068619123890270 ) ) ;
#63320=VERTEX_POINT ( 'NONE', #165366 ) ;
#63326=CARTESIAN_POINT ( 'NONE',  ( -9.296355089585910693E-16, 2.750000000682797818, -1.225000000000007860 ) ) ;
#63421=ORIENTED_EDGE ( 'NONE', *, *, #188015, .F. ) ;
#63479=CARTESIAN_POINT ( 'NONE',  ( 1.224999999999961231, 1.708333334016140181, -0.7072540797573118043 ) ) ;
#63515=( NAMED_UNIT ( * ) PLANE_ANGLE_UNIT ( ) SI_UNIT ( $, .RADIAN. ) );
#63577=CARTESIAN_POINT ( 'NONE',  ( 1.360316468749949825, -0.9635416663252907021, -0.7853790794159282163 ) ) ;
#63624=ADVANCED_FACE ( 'NONE', ( #105741 ), #39632, .T. ) ;
#63646=CARTESIAN_POINT ( 'NONE',  ( -1.813763795902447518, 3.999999999999955147, 0.4499999999999590994 ) ) ;
#63678=CARTESIAN_POINT ( 'NONE',  ( -0.6801582343750334214, 1.213541667008023683, 1.178068619123810334 ) ) ;
#63696=CARTESIAN_POINT ( 'NONE',  ( 0.2999999999999686806, 3.950000000000016165, 1.007084189318352863 ) ) ;
#63723=CARTESIAN_POINT ( 'NONE',  ( 1.874158809982156670, 3.299964346911599122, 0.3999999999999681033 ) ) ;
#63801=CARTESIAN_POINT ( 'NONE',  ( -0.6801582343750213200, -0.3177083329919394572, 1.178068619123815663 ) ) ;
#63825=CARTESIAN_POINT ( 'NONE',  ( 1.360316468749947605, 2.536458333674726173, -0.7853790794159141164 ) ) ;
#64010=ORIENTED_EDGE ( 'NONE', *, *, #171411, .T. ) ;
#64038=CARTESIAN_POINT ( 'NONE',  ( 1.360316468749978469, 1.046875000341403128, -2.602085213965210642E-14 ) ) ;
#64078=CARTESIAN_POINT ( 'NONE',  ( 1.360316468749997565, 2.744791667008062763, 0.7853790794158921340 ) ) ;
#64119=CARTESIAN_POINT ( 'NONE',  ( 7.320879633048903241E-15, 0.3750000006828252408, 1.224999999999981659 ) ) ;
#64165=ORIENTED_EDGE ( 'NONE', *, *, #210348, .T. ) ;
#64255=CARTESIAN_POINT ( 'NONE',  ( -0.6125000000000244693, 1.520833334016126415, -1.060881119635955327 ) ) ;
#64339=CARTESIAN_POINT ( 'NONE',  ( 0.6801582343749726922, -0.9947916663252467373, 1.178068619123801675 ) ) ;
#64377=DIRECTION ( 'NONE',  ( 3.330669073875478989E-16, -3.540251991789410786E-16, -1.000000000000000000 ) ) ;
#64395=CARTESIAN_POINT ( 'NONE',  ( 7.785697387528199762E-15, 0.4375000000000076605, -1.225000000000032951 ) ) ;
#64456=VERTEX_POINT ( 'NONE', #126889 ) ;
#64570=CARTESIAN_POINT ( 'NONE',  ( -2.091679895156829610E-15, 2.562499999999987121, 1.224999999999973888 ) ) ;
#64640=CARTESIAN_POINT ( 'NONE',  ( -0.6125000000000210276, 1.354166667349498976, 1.060881119635887604 ) ) ;
#64709=EDGE_CURVE ( 'NONE', #30458, #30345, #112484, .T. ) ;
#64736=CARTESIAN_POINT ( 'NONE',  ( 0.6801582343749917881, 1.255208333674727506, 1.178068619123834759 ) ) ;
#64824=CIRCLE ( 'NONE', #185879, 0.04999999999999969746 ) ;
#64852=CARTESIAN_POINT ( 'NONE',  ( -0.4000000000000171196, 3.248764396332275872, -0.4641653677812850320 ) ) ;
#64864=CARTESIAN_POINT ( 'NONE',  ( 1.360316468749981800, -1.005208332991882614, 0.7853790794158560518 ) ) ;
#64885=CARTESIAN_POINT ( 'NONE',  ( -1.360316468750052854, 2.661458333674782573, 0.7853790794158580502 ) ) ;
#64954=( BOUNDED_CURVE ( )  B_SPLINE_CURVE ( 2, ( #66593, #51459, #134860, #18926, #117580, #184631, #135908, #199815, #53580 ),
 .UNSPECIFIED., .F., .T. ) 
 B_SPLINE_CURVE_WITH_KNOTS ( ( 3, 2, 2, 2, 3 ),
 ( 0.4218749999999998890, 0.4270833333333333148, 0.4375000000000000000, 0.4479166666666666852, 0.4531250000000002220 ),
 .UNSPECIFIED. ) 
 CURVE ( )  GEOMETRIC_REPRESENTATION_ITEM ( )  RATIONAL_B_SPLINE_CURVE ( ( 0.9330127018922192983, 0.9330127018922178550, 1.000000000000000000, 0.8660254037844387076, 1.000000000000000000, 0.8660254037844387076, 1.000000000000000000, 0.9330127018922165227, 0.9330127018922194093 ) ) 
 REPRESENTATION_ITEM ( '' )  );
#65017=CARTESIAN_POINT ( 'NONE',  ( -1.225000000000040057, 2.333333334016199245, 0.7072540797572636206 ) ) ;
#65038=TOROIDAL_SURFACE ( 'NONE', #148094, 1.914481421317583587, 0.05000000000000000278 ) ;
#65039=( BOUNDED_SURFACE ( )  B_SPLINE_SURFACE ( 3, 2, ( 
 ( #183996, #164560, #83290 ),
 ( #99561, #133160, #81178 ),
 ( #51884, #114805, #31372 ),
 ( #132101, #150460, #181852 ) ),
 .UNSPECIFIED., .F., .F., .T. ) 
 B_SPLINE_SURFACE_WITH_KNOTS ( ( 4, 4 ),
 ( 3, 3 ),
 ( 0.0002170249176783571197, 0.0009435326495461319064 ),
 ( 0.000000000000000000, 1.000000000000000000 ),
 .UNSPECIFIED. ) 
 GEOMETRIC_REPRESENTATION_ITEM ( )  RATIONAL_B_SPLINE_SURFACE ( (
 ( 1.000000000000000000, 0.6273451206645743738, 1.000000000000000000),
 ( 1.000000000000000000, 0.6198154398457538239, 1.000000000000000000),
 ( 1.000000000000000000, 0.6183696555398915384, 1.000000000000000000),
 ( 1.000000000000000000, 0.6222646319068302345, 1.000000000000000000) ) ) 
 REPRESENTATION_ITEM ( '' )  SURFACE ( )  );
#65077=CARTESIAN_POINT ( 'NONE',  ( -1.953008978358306879E-14, 0.2343750003414031002, 1.570758158831794260 ) ) ;
#65115=CARTESIAN_POINT ( 'NONE',  ( 1.360316468749994012, 2.265625000341386919, -1.387778780781445676E-14 ) ) ;
#65137=CARTESIAN_POINT ( 'NONE',  ( -1.225000000000022071, 0.2916666673494853756, -0.7072540797573118043 ) ) ;
#65193=VECTOR ( 'NONE', #182160, 1000.000000000000114 ) ;
#65201=EDGE_CURVE ( 'NONE', #28319, #75836, #34700, .T. ) ;
#65216=CARTESIAN_POINT ( 'NONE',  ( -0.4500000000000232703, 4.000000000000003553, 0.8338124244295432863 ) ) ;
#65242=ORIENTED_EDGE ( 'NONE', *, *, #201642, .F. ) ;
#65287=CARTESIAN_POINT ( 'NONE',  ( -0.3282377607281391496, 1.613835450998152288, 1.224999999999981881 ) ) ;
#65320=CARTESIAN_POINT ( 'NONE',  ( -1.162044386198238837E-16, 2.062499999999991562, 1.224999999999974332 ) ) ;
#65367=CARTESIAN_POINT ( 'NONE',  ( -0.6801582343750265380, -0.2864583329919220822, 1.178068619123820771 ) ) ;
#65393=AXIS2_PLACEMENT_3D ( 'NONE', #6634, #142028, #190723 ) ;
#65702=CARTESIAN_POINT ( 'NONE',  ( -0.5000000000000386358, 3.949999999999988187, -0.4500000000000284883 ) ) ;
#65770=CARTESIAN_POINT ( 'NONE',  ( -3.755786496842899057E-14, 2.109375000341444206, -1.570758158831810247 ) ) ;
#65776=LINE ( 'NONE', #78851, #210192 ) ;
#65799=VERTEX_POINT ( 'NONE', #166314 ) ;
#65902=CARTESIAN_POINT ( 'NONE',  ( -0.6801582343750213200, -0.4010416663252705516, -1.178068619123886718 ) ) ;
#65924=CARTESIAN_POINT ( 'NONE',  ( -5.157946788997579689E-14, 1.203125000341463746, 1.570758158831762286 ) ) ;
#66035=VECTOR ( 'NONE', #142742, 1000.000000000000000 ) ;
#66082=CARTESIAN_POINT ( 'NONE',  ( -0.4000000000000496492, 3.372708439410135206, 0.4999999999999483746 ) ) ;
#66106=CARTESIAN_POINT ( 'NONE',  ( -2.905110965495596944E-15, 1.687500000000013101, -1.225000000000019851 ) ) ;
#66108=ORIENTED_EDGE ( 'NONE', *, *, #89116, .F. ) ;
#66124=CARTESIAN_POINT ( 'NONE',  ( 0.6801582343749726922, -0.9947916663252467373, 1.178068619123801675 ) ) ;
#66163=CARTESIAN_POINT ( 'NONE',  ( 0.6801582343749865700, 1.307291667008089853, -1.178068619123883165 ) ) ;
#66172=ORIENTED_EDGE ( 'NONE', *, *, #66555, .F. ) ;
#66257=CARTESIAN_POINT ( 'NONE',  ( 0.4499999999999712563, 3.949999999999981526, -6.938893903907228378E-15 ) ) ;
#66289=CIRCLE ( 'NONE', #94027, 1.872309607372811158 ) ;
#66424=CARTESIAN_POINT ( 'NONE',  ( -1.360316468750052854, 2.661458333674782573, 0.7853790794158580502 ) ) ;
#66483=CARTESIAN_POINT ( 'NONE',  ( -1.225000000000056044, 2.541666667349471886, -0.7072540797572937077 ) ) ;
#66555=EDGE_CURVE ( 'NONE', #203057, #38441, #187870, .T. ) ;
#66564=CARTESIAN_POINT ( 'NONE',  ( -1.225000000000042277, 2.479166666666715368, -0.7072540797573197979 ) ) ;
#66593=CARTESIAN_POINT ( 'NONE',  ( -1.626862140677534470E-15, 1.125000000682806034, 1.224999999999975886 ) ) ;
#66834=CARTESIAN_POINT ( 'NONE',  ( -1.360316468750036645, 1.901041667008058988, -0.7853790794159222211 ) ) ;
#66843=FACE_OUTER_BOUND ( 'NONE', #207187, .T. ) ;
#66851=CARTESIAN_POINT ( 'NONE',  ( -0.4809368265653978236, 3.139971263792654899, 0.3999999999999597211 ) ) ;
#66888=CARTESIAN_POINT ( 'NONE',  ( -0.3282377607281410370, 0.7611645503674365765, -1.225000000000029399 ) ) ;
#66959=CARTESIAN_POINT ( 'NONE',  ( -0.4205683736966969177, 3.129384673317391563, -0.4296503687815703687 ) ) ;
#66993=CARTESIAN_POINT ( 'NONE',  ( 0.6801582343749952297, 1.807291667008069425, -1.178068619123869398 ) ) ;
#66999=CARTESIAN_POINT ( 'NONE',  ( -1.225000000000012523, 2.906250000341427331, -4.336808689942017736E-14 ) ) ;
#67066=FACE_OUTER_BOUND ( 'NONE', #98656, .T. ) ;
#67133=CARTESIAN_POINT ( 'NONE',  ( -0.6125000000000158096, 2.270833334016133964, -1.060881119635972647 ) ) ;
#67176=B_SPLINE_CURVE_WITH_KNOTS ( 'NONE', 3,
 ( #107494, #85840, #72777, #119472 ),
 .UNSPECIFIED., .F., .F.,
 ( 4, 4 ),
 ( 0.000000000000000000, 1.930757672285080358E-06 ),
 .UNSPECIFIED. ) ;
#67196=CARTESIAN_POINT ( 'NONE',  ( -1.360316468750016439, -0.07812499965861169349, -3.469446951953614189E-14 ) ) ;
#67238=CARTESIAN_POINT ( 'NONE',  ( 0.6801582343749987825, 1.557291667008103841, -1.178068619123876282 ) ) ;
#67246=CARTESIAN_POINT ( 'NONE',  ( -0.3282377607281289911, 1.761164550367436021, -1.225000000000013634 ) ) ;
#67300=LINE ( 'NONE', #3373, #80816 ) ;
#67437=CARTESIAN_POINT ( 'NONE',  ( -9.296355089585910693E-16, 2.750000000682797818, -1.225000000000007860 ) ) ;
#67444=CARTESIAN_POINT ( 'NONE',  ( -1.225000000000028066, 2.020833333333377446, 0.7072540797572697269 ) ) ;
#67492=CARTESIAN_POINT ( 'NONE',  ( 1.360316468750001784, 2.286458333674732835, -0.7853790794158941324 ) ) ;
#67532=VECTOR ( 'NONE', #114422, 1000.000000000000000 ) ;
#67541=VERTEX_POINT ( 'NONE', #111304 ) ;
#67673=AXIS2_PLACEMENT_3D ( 'NONE', #169245, #106436, #40331 ) ;
#67734=CARTESIAN_POINT ( 'NONE',  ( 0.6801582343749987825, 2.338541667008108060, -1.178068619123883165 ) ) ;
#67757=CARTESIAN_POINT ( 'NONE',  ( -0.6125000000000105915, 0.5416666666666625218, 1.060881119635880721 ) ) ;
#67772=ADVANCED_FACE ( 'NONE', ( #45189 ), #91135, .T. ) ;
#67795=ORIENTED_EDGE ( 'NONE', *, *, #212859, .F. ) ;
#67867=CARTESIAN_POINT ( 'NONE',  ( -0.4000000000000183964, 3.222996591249000176, 0.4134307888557075539 ) ) ;
#67872=EDGE_CURVE ( 'NONE', #6267, #184258, #178380, .T. ) ;
#67897=CARTESIAN_POINT ( 'NONE',  ( 0.2999999999999877764, 3.322650755865456773, -0.5865692111442898371 ) ) ;
#67906=CARTESIAN_POINT ( 'NONE',  ( 0.6801582343749847936, 0.5052083336747614783, 1.178068619123803451 ) ) ;
#67931=ORIENTED_EDGE ( 'NONE', *, *, #119884, .T. ) ;
#67956=CARTESIAN_POINT ( 'NONE',  ( -0.6125000000000314637, 0.8541666673494846540, 1.060881119635901593 ) ) ;
#68024=DIRECTION ( 'NONE',  ( 3.330669073875478989E-16, -3.540251991789410786E-16, -1.000000000000000000 ) ) ;
#68042=CARTESIAN_POINT ( 'NONE',  ( -1.772826578343124959, 3.950000000000009059, -0.4500000000000423661 ) ) ;
#68054=CARTESIAN_POINT ( 'NONE',  ( -1.743066579297358008E-15, 2.187499999999992006, -1.225000000000032951 ) ) ;
#68057=CARTESIAN_POINT ( 'NONE',  ( -0.6801582343750125492, 2.182291667008062763, 1.178068619123824323 ) ) ;
#68186=DIRECTION ( 'NONE',  ( 3.330669073875479482E-16, -3.330669073875479482E-16, -1.000000000000000000 ) ) ;
#68202=CARTESIAN_POINT ( 'NONE',  ( -0.3282377607281385390, 2.363835450998165388, 1.224999999999973221 ) ) ;
#68265=( NAMED_UNIT ( * ) PLANE_ANGLE_UNIT ( ) SI_UNIT ( $, .RADIAN. ) );
#68267=CARTESIAN_POINT ( 'NONE',  ( -1.360316468750042862, -0.5572916663252566183, 0.7853790794158701516 ) ) ;
#68309=CARTESIAN_POINT ( 'NONE',  ( 0.6801582343749970061, 0.8072916670080754198, -1.178068619123858962 ) ) ;
#68405=ORIENTED_EDGE ( 'NONE', *, *, #201770, .F. ) ;
#68527=EDGE_CURVE ( 'NONE', #31530, #62971, #52450, .T. ) ;
#68599=CARTESIAN_POINT ( 'NONE',  ( 6.856061878569608298E-15, 0.9375000000000238698, -1.225000000000010303 ) ) ;
#68605=CARTESIAN_POINT ( 'NONE',  ( 0.6124999999999949374, 1.645833334016133520, 1.060881119635922243 ) ) ;
#68627=AXIS2_PLACEMENT_3D ( 'NONE', #65702, #179506, #181606 ) ;
#68707=CARTESIAN_POINT ( 'NONE',  ( -1.225000000000046052, 2.520833333333404092, 0.7072540797572777205 ) ) ;
#68743=EDGE_CURVE ( 'NONE', #163067, #30915, #184621, .T. ) ;
#68814=CARTESIAN_POINT ( 'NONE',  ( 1.360316468749951602, 2.526041667008117830, 0.7853790794158560518 ) ) ;
#68833=( BOUNDED_SURFACE ( )  B_SPLINE_SURFACE ( 3, 2, ( 
 ( #208325, #75148, #76205 ),
 ( #56761, #142315, #141258 ),
 ( #207266, #58897, #125050 ),
 ( #191005, #108780, #174806 ) ),
 .UNSPECIFIED., .F., .F., .T. ) 
 B_SPLINE_SURFACE_WITH_KNOTS ( ( 4, 4 ),
 ( 3, 3 ),
 ( 3.141592653589793116, 4.712388980384689674 ),
 ( 0.000000000000000000, 1.000000000000000000 ),
 .UNSPECIFIED. ) 
 GEOMETRIC_REPRESENTATION_ITEM ( )  RATIONAL_B_SPLINE_SURFACE ( (
 ( 1.000000000000000000, 0.8661919058288514162, 1.000000000000000000),
 ( 1.000000000000000000, 0.8676977444974305342, 1.000000000000000000),
 ( 1.000000000000000000, 0.8014503788335436418, 1.000000000000000000),
 ( 1.000000000000000000, 0.7071067811865416886, 1.000000000000000000) ) ) 
 REPRESENTATION_ITEM ( '' )  SURFACE ( )  );
#68837=CARTESIAN_POINT ( 'NONE',  ( -0.6124999999999880540, 0.2916666666666900554, 1.060881119635892933 ) ) ;
#68850=CARTESIAN_POINT ( 'NONE',  ( -0.3423093779010150106, 2.999999999999981792, -0.3423093779010167315 ) ) ;
#68973=VERTEX_POINT ( 'NONE', #126066 ) ;
#68985=CARTESIAN_POINT ( 'NONE',  ( 1.360316468749957597, 0.7760416670081096147, 0.7853790794158520550 ) ) ;
#69040=EDGE_LOOP ( 'NONE', ( #83118, #125798 ) ) ;
#69060=CARTESIAN_POINT ( 'NONE',  ( -0.5000000000000108802, 3.950000000000001954, -0.5000000000000091038 ) ) ;
#69100=CARTESIAN_POINT ( 'NONE',  ( -0.4336004510535704792, 3.058108253035755730, 0.4198436715060500091 ) ) ;
#69131=CARTESIAN_POINT ( 'NONE',  ( 1.360316468749981800, 1.744791667008098290, 0.7853790794158680422 ) ) ;
#69180=FACE_OUTER_BOUND ( 'NONE', #13047, .T. ) ;
#69203=CARTESIAN_POINT ( 'NONE',  ( 0.6124999999999914957, 2.583333333333347248, 1.060881119635894487 ) ) ;
#69205=DIRECTION ( 'NONE',  ( -1.276756478318932585E-15, 1.000000000000000000, -1.665334536937738262E-16 ) ) ;
#69250=CARTESIAN_POINT ( 'NONE',  ( 0.8018101603110124875, -8.116362469078496434E-15, -0.9920850708466935064 ) ) ;
#69289=CARTESIAN_POINT ( 'NONE',  ( 0.6124999999999932720, 1.979166667349464781, -1.060881119635938008 ) ) ;
#69294=CARTESIAN_POINT ( 'NONE',  ( -1.225000000000000089, -0.1666666659838688114, 0.7072540797572937077 ) ) ;
#69330=CARTESIAN_POINT ( 'NONE',  ( -4.757329562667670667E-14, -0.8906249996585621220, -1.570758158831818241 ) ) ;
#69360=ORIENTED_EDGE ( 'NONE', *, *, #107456, .F. ) ;
#69369=ADVANCED_FACE ( 'NONE', ( #20769 ), #152930, .T. ) ;
#69374=CARTESIAN_POINT ( 'NONE',  ( 1.360316468749955598, 1.536458333674721288, -0.7853790794159342115 ) ) ;
#69494=ORIENTED_EDGE ( 'NONE', *, *, #160909, .F. ) ;
#69547=PLANE ( 'NONE',  #11995 ) ;
#69560=CARTESIAN_POINT ( 'NONE',  ( -2.449742653233059286, 3.300000000000011369, 0.3999999999999750422 ) ) ;
#69666=AXIS2_PLACEMENT_3D ( 'NONE', #53504, #155280, #137969 ) ;
#69672=CARTESIAN_POINT ( 'NONE',  ( -1.225000000000038058, 2.083333334016205907, 0.7072540797572697269 ) ) ;
#69737=DIRECTION ( 'NONE',  ( 1.276756478318932585E-15, -1.000000000000000000, 1.665334536937738262E-16 ) ) ;
#69876=CARTESIAN_POINT ( 'NONE',  ( -4.156403723172807449E-14, 1.859375000341410678, -1.570758158831802254 ) ) ;
#69898=CARTESIAN_POINT ( 'NONE',  ( -0.6125000000000226930, 0.2083333333333242665, -1.060881119635965764 ) ) ;
#69938=ORIENTED_EDGE ( 'NONE', *, *, #124980, .T. ) ;
#69962=AXIS2_PLACEMENT_3D ( 'NONE', #29753, #30829, #11341 ) ;
#70031=ORIENTED_EDGE ( 'NONE', *, *, #10962, .T. ) ;
#70037=CARTESIAN_POINT ( 'NONE',  ( 0.3275200278799236253, 3.116672424413495790, -0.4674645318178084485 ) ) ;
#70059=DIRECTION ( 'NONE',  ( -9.436895709313856232E-16, 0.8656921114426506803, 0.5005768354468324022 ) ) ;
#70094=CARTESIAN_POINT ( 'NONE',  ( -1.225000000000005640, 1.387778780781445676E-14, -1.387778780781445676E-14 ) ) ;
#70168=FACE_OUTER_BOUND ( 'NONE', #41501, .T. ) ;
#70169=CARTESIAN_POINT ( 'NONE',  ( -1.225000000000026512, 1.750000000000015543, -1.734723475976807094E-14 ) ) ;
#70197=CARTESIAN_POINT ( 'NONE',  ( -4.957638175832625493E-14, 2.078125000341435769, -1.570758158831802254 ) ) ;
#70269=CARTESIAN_POINT ( 'NONE',  ( -0.6125000000000123679, 2.958333333333326820, -1.060881119635965764 ) ) ;
#70315=CARTESIAN_POINT ( 'NONE',  ( 1.208258962943321357, -6.100893924328829751E-15, -0.5075860003171979162 ) ) ;
#70357=AXIS2_PLACEMENT_3D ( 'NONE', #135803, #20944, #154185 ) ;
#70360=CARTESIAN_POINT ( 'NONE',  ( 1.224999999999969225, -0.8333333326504639427, 0.7072540797572596238 ) ) ;
#70393=CARTESIAN_POINT ( 'NONE',  ( 1.360316468749989793, -0.4322916663252800995, -0.7853790794158961308 ) ) ;
#70434=CARTESIAN_POINT ( 'NONE',  ( -0.6801582343750438575, 1.932291667008062541, 1.178068619123787908 ) ) ;
#70452=ORIENTED_EDGE ( 'NONE', *, *, #35454, .F. ) ;
#70562=EDGE_LOOP ( 'NONE', ( #6885, #92366, #120595, #163922 ) ) ;
#70579=DIRECTION ( 'NONE',  ( 1.276756478318932585E-15, -1.000000000000000000, 1.665334536937738262E-16 ) ) ;
#70626=EDGE_CURVE ( 'NONE', #102463, #28948, #205366, .T. ) ;
#70640=EDGE_LOOP ( 'NONE', ( #170498, #171264, #74068, #81768 ) ) ;
#70731=CARTESIAN_POINT ( 'NONE',  ( -1.225000000000006084, 2.041666667349461672, -0.7072540797572977045 ) ) ;
#70809=LINE ( 'NONE', #50330, #12487 ) ;
#70825=FACE_OUTER_BOUND ( 'NONE', #165371, .T. ) ;
#70848=VECTOR ( 'NONE', #85725, 1000.000000000000000 ) ;
#70944=CARTESIAN_POINT ( 'NONE',  ( -1.360316468750062846, 1.401041667008104508, -0.7853790794158941324 ) ) ;
#70967=CARTESIAN_POINT ( 'NONE',  ( 0.6124999999999932720, 0.9166666666666906105, -1.060881119635955327 ) ) ;
#71022=ADVANCED_FACE ( 'NONE', ( #43346 ), #27061, .T. ) ;
#71120=CARTESIAN_POINT ( 'NONE',  ( -1.953008978358306879E-14, 0.2343750003414031002, 1.570758158831794260 ) ) ;
#71255=EDGE_CURVE ( 'NONE', #134733, #213643, #167735, .T. ) ;
#71267=CARTESIAN_POINT ( 'NONE',  ( 0.6801582343749935644, -0.02604166632526327962, 1.178068619123817218 ) ) ;
#71320=( BOUNDED_CURVE ( )  B_SPLINE_CURVE ( 2, ( #189543, #41191, #124641, #105123, #88870, #92076, #91006, #154924, #157068 ),
 .UNSPECIFIED., .F., .T. ) 
 B_SPLINE_CURVE_WITH_KNOTS ( ( 3, 2, 2, 2, 3 ),
 ( 0.01562500000000013531, 0.02083333333333333218, 0.03125000000000000000, 0.04166666666666666435, 0.04687499999999977796 ),
 .UNSPECIFIED. ) 
 CURVE ( )  GEOMETRIC_REPRESENTATION_ITEM ( )  RATIONAL_B_SPLINE_CURVE ( ( 0.9330127018922194093, 0.9330127018922211857, 1.000000000000000000, 0.8660254037844387076, 1.000000000000000000, 0.8660254037844387076, 1.000000000000000000, 0.9330127018922221849, 0.9330127018922194093 ) ) 
 REPRESENTATION_ITEM ( '' )  );
#71336=CARTESIAN_POINT ( 'NONE',  ( 1.224999999999959233, 2.104166666666714480, 0.7072540797572757221 ) ) ;
#71379=CARTESIAN_POINT ( 'NONE',  ( -2.255140518769849223E-14, 3.249999999999988898, -4.336808689942017736E-14 ) ) ;
#71424=CARTESIAN_POINT ( 'NONE',  ( 0.3282377607281107279, 1.988835450998174492, -1.225000000000013411 ) ) ;
#71431=CARTESIAN_POINT ( 'NONE',  ( -1.225000000000026512, -0.6874999993171926338, -2.428612866367529932E-14 ) ) ;
#71448=CARTESIAN_POINT ( 'NONE',  ( -1.734723475976807094E-15, 2.999999999999988898, -6.938893903907228378E-15 ) ) ;
#71501=CARTESIAN_POINT ( 'NONE',  ( -1.360316468750026875, 2.140625000341400685, -4.857225732735059864E-14 ) ) ;
#71532=CARTESIAN_POINT ( 'NONE',  ( 1.913201741516656895, 3.249623237789923902, -0.4478572873796519138 ) ) ;
#71719=CARTESIAN_POINT ( 'NONE',  ( 0.3999999999999819811, 3.049942316455271474, -0.4288785890452975202 ) ) ;
#71767=CARTESIAN_POINT ( 'NONE',  ( 0.4288785890452437299, 3.049942316455264812, -0.4196807566835009662 ) ) ;
#71804=CARTESIAN_POINT ( 'NONE',  ( -1.225000000000045386, 1.312500000682802259, -4.336808689942017736E-14 ) ) ;
#71818=DIRECTION ( 'NONE',  ( -0.5005768354468330683, -0.8656921114426503472, 1.942890293094028284E-15 ) ) ;
#71936=CARTESIAN_POINT ( 'NONE',  ( 1.926047848139553986, 3.520667328614982328, -0.3999999999999993006 ) ) ;
#72014=CARTESIAN_POINT ( 'NONE',  ( 1.360316468749941610, 2.276041667008116942, 0.7853790794158921340 ) ) ;
#72036=CARTESIAN_POINT ( 'NONE',  ( 1.224999999999995204, 0.1249999999999862332, -6.938893903907228378E-15 ) ) ;
#72069=VERTEX_POINT ( 'NONE', #79827 ) ;
#72086=CARTESIAN_POINT ( 'NONE',  ( 1.184414575232636047, -6.859386807788068932E-15, 0.6925866048970821254 ) ) ;
#72117=EDGE_CURVE ( 'NONE', #3320, #141010, #158958, .T. ) ;
#72222=CARTESIAN_POINT ( 'NONE',  ( 0.3423093779009924731, 3.000000000000002665, -0.3423093779010306092 ) ) ;
#72249=CARTESIAN_POINT ( 'NONE',  ( 0.3282377607281096732, 2.573664549684620884, 1.224999999999963674 ) ) ;
#72311=AXIS2_PLACEMENT_3D ( 'NONE', #92176, #44479, #27131 ) ;
#72340=CARTESIAN_POINT ( 'NONE',  ( -1.360316468750009555, -0.1093749996585596795, -2.081668171172168513E-14 ) ) ;
#72377=EDGE_CURVE ( 'NONE', #106774, #72069, #88102, .T. ) ;
#72414=CARTESIAN_POINT ( 'NONE',  ( -3.555477883677943599E-14, 2.312499999999986677, 1.414508159514561436 ) ) ;
#72454=DIRECTION ( 'NONE',  ( -1.276756478318932585E-15, 1.000000000000000000, -1.665334536937738262E-16 ) ) ;
#72508=CARTESIAN_POINT ( 'NONE',  ( -0.6125000000000314637, -0.8958333326505307781, 1.060881119635913583 ) ) ;
#72526=CYLINDRICAL_SURFACE ( 'NONE', #158181, 1.224999999999996980 ) ;
#72549=( GEOMETRIC_REPRESENTATION_CONTEXT ( 3 ) GLOBAL_UNCERTAINTY_ASSIGNED_CONTEXT ( ( #78715 ) ) GLOBAL_UNIT_ASSIGNED_CONTEXT ( ( #194570, #164213, #208674 ) ) REPRESENTATION_CONTEXT ( 'NONE', 'WORKASPACE' ) );
#72572=VERTEX_POINT ( 'NONE', #183720 ) ;
#72576=CARTESIAN_POINT ( 'NONE',  ( 0.6801582343749952297, 1.807291667008069425, -1.178068619123869398 ) ) ;
#72594=ORIENTED_EDGE ( 'NONE', *, *, #27793, .F. ) ;
#72655=CARTESIAN_POINT ( 'NONE',  ( -0.3275200278800330378, 3.116672424413140963, -0.4674645318176217090 ) ) ;
#72708=ORIENTED_EDGE ( 'NONE', *, *, #135923, .T. ) ;
#72777=CARTESIAN_POINT ( 'NONE',  ( -1.872871967411093186, 3.300000000000011369, -0.3999999999999993006 ) ) ;
#72808=CARTESIAN_POINT ( 'NONE',  ( -4.957638175832625493E-14, 2.359375000341373152, -1.570758158831806250 ) ) ;
#72881=CARTESIAN_POINT ( 'NONE',  ( -1.225000000000024736, 1.062500000682836676, -3.122502256758252770E-14 ) ) ;
#72908=CYLINDRICAL_SURFACE ( 'NONE', #49547, 1.224999999999996980 ) ;
#72940=CARTESIAN_POINT ( 'NONE',  ( -0.6125000000000019318, 1.458333333333332371, -1.060881119635941339 ) ) ;
#73015=ADVANCED_FACE ( 'NONE', ( #42580 ), #26287, .T. ) ;
#73057=ORIENTED_EDGE ( 'NONE', *, *, #77906, .T. ) ;
#73089=CARTESIAN_POINT ( 'NONE',  ( 1.360316468749987573, 0.2760416670081234369, 0.7853790794158701516 ) ) ;
#73098=CARTESIAN_POINT ( 'NONE',  ( -0.4500000000000545231, 4.000000000000003553, -0.8338124244296075682 ) ) ;
#73111=CARTESIAN_POINT ( 'NONE',  ( -4.156403723172807449E-14, -0.06249999999999229089, -1.414508159514581642 ) ) ;
#73206=CARTESIAN_POINT ( 'NONE',  ( 1.224999999999995204, 2.666666667349464781, 0.7072540797572858251 ) ) ;
#73225=CARTESIAN_POINT ( 'NONE',  ( 4.996790860652426159E-15, 0.6250000006827882704, 1.224999999999976330 ) ) ;
#73281=CARTESIAN_POINT ( 'NONE',  ( -0.5445930744354000597, 3.250057683544679943, -0.4000000000000062395 ) ) ;
#73310=CYLINDRICAL_SURFACE ( 'NONE', #27112, 0.09999999999999971412 ) ;
#73389=B_SPLINE_CURVE_WITH_KNOTS ( 'NONE', 3,
 ( #87126, #88199, #38377, #5847, #138027, #153196, #6917 ),
 .UNSPECIFIED., .F., .F.,
 ( 4, 3, 4 ),
 ( 0.000000000000000000, 4.270488675891434798E-05, 4.488495215206818762E-05 ),
 .UNSPECIFIED. ) ;
#73414=VERTEX_POINT ( 'NONE', #211435 ) ;
#73416=CARTESIAN_POINT ( 'NONE',  ( -0.6801582343750334214, 0.1822916670080609869, 1.178068619123799898 ) ) ;
#73418=CARTESIAN_POINT ( 'NONE',  ( 0.6311622855796495957, 3.299999999999997158, -0.4000000000000131783 ) ) ;
#73435=DIRECTION ( 'NONE',  ( 1.276756478318932585E-15, -1.000000000000000000, 1.665334536937738262E-16 ) ) ;
#73490=EDGE_LOOP ( 'NONE', ( #64010, #116015, #160386, #123709 ) ) ;
#73492=CARTESIAN_POINT ( 'NONE',  ( -1.225000000000042277, 2.229166666666690499, -0.7072540797573217963 ) ) ;
#73530=FACE_OUTER_BOUND ( 'NONE', #160893, .T. ) ;
#73536=CARTESIAN_POINT ( 'NONE',  ( 1.326446625878273444, -2.791019202464277584E-14, 0.3259839236695623588 ) ) ;
#73557=CARTESIAN_POINT ( 'NONE',  ( -0.3282377607281442011, 1.301335450315356468, 1.224999999999969003 ) ) ;
#73571=AXIS2_PLACEMENT_3D ( 'NONE', #69560, #201694, #53338 ) ;
#73640=LINE ( 'NONE', #92053, #90672 ) ;
#73645=CARTESIAN_POINT ( 'NONE',  ( 0.4169036860910191322, 3.145283463680761393, -0.4342470185719746190 ) ) ;
#73655=CARTESIAN_POINT ( 'NONE',  ( 1.360316468749949825, 2.244791667008100511, 0.7853790794158780342 ) ) ;
#73663=CARTESIAN_POINT ( 'NONE',  ( 0.6801582343750038895, 0.3072916670080680368, -1.178068619123848526 ) ) ;
#73679=ORIENTED_EDGE ( 'NONE', *, *, #41144, .T. ) ;
#73802=DIRECTION ( 'NONE',  ( -1.276756478318932585E-15, 1.000000000000000000, -1.665334536937738262E-16 ) ) ;
#73876=AXIS2_PLACEMENT_3D ( 'NONE', #143360, #10108, #27429 ) ;
#73893=CARTESIAN_POINT ( 'NONE',  ( -0.6801582343750386395, 2.380208333674735499, -1.178068619123869398 ) ) ;
#73970=CARTESIAN_POINT ( 'NONE',  ( -0.6125000000000296874, 0.3541666673494772710, 1.060881119635899816 ) ) ;
#74030=CARTESIAN_POINT ( 'NONE',  ( -1.225000000000058265, 1.520833333333367232, 0.7072540797572596238 ) ) ;
#74068=ORIENTED_EDGE ( 'NONE', *, *, #145048, .F. ) ;
#74123=EDGE_CURVE ( 'NONE', #170783, #153954, #8733, .T. ) ;
#74132=EDGE_CURVE ( 'NONE', #163067, #73414, #184575, .T. ) ;
#74191=CARTESIAN_POINT ( 'NONE',  ( -1.360316468750016439, -0.07812499965861169349, -3.469446951953614189E-14 ) ) ;
#74211=CARTESIAN_POINT ( 'NONE',  ( -1.552391752028397856E-14, -0.5624999999999785727, -1.414508159514605401 ) ) ;
#74222=DIRECTION ( 'NONE',  ( 1.000000000000000000, 0.000000000000000000, -4.336808689942015369E-15 ) ) ;
#74424=ADVANCED_FACE ( 'NONE', ( #6861 ), #89228, .F. ) ;
#74494=( BOUNDED_CURVE ( )  B_SPLINE_CURVE ( 3, ( #163373, #164428, #179620, #211024 ),
 .UNSPECIFIED., .F., .T. ) 
 B_SPLINE_CURVE_WITH_KNOTS ( ( 4, 4 ),
 ( 4.712388980384530690, 6.283185307179586232 ),
 .UNSPECIFIED. ) 
 CURVE ( )  GEOMETRIC_REPRESENTATION_ITEM ( )  RATIONAL_B_SPLINE_CURVE ( ( 1.000000000000000000, 0.8047378541243275230, 0.8047378541243275230, 1.000000000000000000 ) ) 
 REPRESENTATION_ITEM ( '' )  );
#74501=ORIENTED_EDGE ( 'NONE', *, *, #31532, .T. ) ;
#74503=CARTESIAN_POINT ( 'NONE',  ( -1.360316468750013108, 1.140625000341413564, -2.081668171172168513E-14 ) ) ;
#74505=PLANE ( 'NONE',  #117220 ) ;
#74569=VERTEX_POINT ( 'NONE', #202930 ) ;
#74573=CARTESIAN_POINT ( 'NONE',  ( 0.6124999999999914957, 1.416666666666690944, -1.060881119635986414 ) ) ;
#74607=CARTESIAN_POINT ( 'NONE',  ( -1.360316468750013108, 2.921875000341411788, -1.734723475976807094E-14 ) ) ;
#74722=CARTESIAN_POINT ( 'NONE',  ( -0.4000000000000357714, 2.999999999999975131, -0.3423093779010444870 ) ) ;
#74727=CARTESIAN_POINT ( 'NONE',  ( -1.360316468750044860, 1.411458333674720622, 0.7853790794158801436 ) ) ;
#74736=CARTESIAN_POINT ( 'NONE',  ( 0.6801582343749900117, 0.05729166700808169255, -1.178068619123848526 ) ) ;
#74778=CARTESIAN_POINT ( 'NONE',  ( 3.486133158594716510E-16, 2.312499999999992006, 1.224999999999971889 ) ) ;
#74804=CARTESIAN_POINT ( 'NONE',  ( -1.734723475976807094E-15, 2.999999999999988898, -6.938893903907228378E-15 ) ) ;
#74826=VERTEX_POINT ( 'NONE', #9021 ) ;
#74834=CARTESIAN_POINT ( 'NONE',  ( 6.856061878569608298E-15, 0.1875000000000181521, -1.225000000000034950 ) ) ;
#74836=DIRECTION ( 'NONE',  ( 1.000000000000000000, -7.771561172376097755E-16, -4.440892098500627148E-16 ) ) ;
#74847=CARTESIAN_POINT ( 'NONE',  ( -0.4809368265653611307, 3.139971263792674439, -0.4000000000000453748 ) ) ;
#74876=FACE_OUTER_BOUND ( 'NONE', #88435, .T. ) ;
#74958=CARTESIAN_POINT ( 'NONE',  ( -1.360316468750048635, 1.942708333674827204, 0.7853790794158580502 ) ) ;
#75037=CARTESIAN_POINT ( 'NONE',  ( 1.224999999999979217, 0.2083333340161329650, -0.7072540797572937077 ) ) ;
#75070=DIRECTION ( 'NONE',  ( -0.5131086435338335638, 0.8583236685137312083, 5.079270337660091961E-15 ) ) ;
#75093=ADVANCED_FACE ( 'NONE', ( #67066 ), #36547, .F. ) ;
#75114=CARTESIAN_POINT ( 'NONE',  ( -0.3868389748196900402, 3.100956225802461663, 0.4583768147623411560 ) ) ;
#75118=AXIS2_PLACEMENT_3D ( 'NONE', #43998, #209654, #175066 ) ;
#75148=CARTESIAN_POINT ( 'NONE',  ( 0.2999999999999846123, 4.000000000000008882, 0.9782388782688751228 ) ) ;
#75155=CARTESIAN_POINT ( 'NONE',  ( -0.6125000000000210276, 1.354166667349498976, 1.060881119635887604 ) ) ;
#75211=CARTESIAN_POINT ( 'NONE',  ( -1.225000000000018074, 2.979166666666678065, -0.7072540797572998139 ) ) ;
#75251=CARTESIAN_POINT ( 'NONE',  ( -1.360316468750044860, 1.151041667008095404, -0.7853790794159261068 ) ) ;
#75272=CARTESIAN_POINT ( 'NONE',  ( -4.757329562667670667E-14, -0.9374999999999723554, 1.414508159514539454 ) ) ;
#75401=ORIENTED_EDGE ( 'NONE', *, *, #146195, .T. ) ;
#75465=DIRECTION ( 'NONE',  ( 0.000000000000000000, -3.330669073875420317E-16, -1.000000000000000000 ) ) ;
#75474=ORIENTED_EDGE ( 'NONE', *, *, #214379, .F. ) ;
#75478=CARTESIAN_POINT ( 'NONE',  ( 0.3282377607280986820, 0.07366454968464808406, 1.224999999999942801 ) ) ;
#75524=VECTOR ( 'NONE', #49604, 1000.000000000000114 ) ;
#75566=CARTESIAN_POINT ( 'NONE',  ( -0.6801582343749917881, 0.4322916670080681478, 1.178068619123841643 ) ) ;
#75580=EDGE_LOOP ( 'NONE', ( #37311, #108091, #63421, #121333 ) ) ;
#75603=CARTESIAN_POINT ( 'NONE',  ( -1.946706258588004168, 3.753940929402450610, 0.4616008842494395692 ) ) ;
#75638=CARTESIAN_POINT ( 'NONE',  ( -0.6125000000000192513, 1.958333333333318826, -1.060881119635962211 ) ) ;
#75680=DIRECTION ( 'NONE',  ( 0.5131086435338284568, -0.8583236685137343169, -8.049116928532389848E-16 ) ) ;
#75792=CARTESIAN_POINT ( 'NONE',  ( -1.360316468750046859, 0.3697916670080757529, -0.7853790794159101196 ) ) ;
#75836=VERTEX_POINT ( 'NONE', #121995 ) ;
#75861=EDGE_CURVE ( 'NONE', #16624, #53408, #470, .T. ) ;
#75994=VERTEX_POINT ( 'NONE', #143539 ) ;
#76022=CARTESIAN_POINT ( 'NONE',  ( -1.360316468750038643, 1.651041667008089853, -0.7853790794159041244 ) ) ;
#76048=EDGE_CURVE ( 'NONE', #52005, #179471, #108104, .T. ) ;
#76054=ADVANCED_FACE ( 'NONE', ( #95838 ), #161894, .T. ) ;
#76056=VERTEX_POINT ( 'NONE', #174950 ) ;
#76099=CARTESIAN_POINT ( 'NONE',  ( -1.225000000000048939, 0.06250000068282191013, -4.336808689942017736E-14 ) ) ;
#76181=DIRECTION ( 'NONE',  ( 3.219646771412963434E-15, 1.665334536937739741E-16, 1.000000000000000000 ) ) ;
#76205=CARTESIAN_POINT ( 'NONE',  ( 0.2999999999999866107, 3.975028841772350940, 0.9637995837462389748 ) ) ;
#76230=EDGE_CURVE ( 'NONE', #137780, #55298, #197851, .T. ) ;
#76259=LINE ( 'NONE', #138069, #92121 ) ;
#76262=CARTESIAN_POINT ( 'NONE',  ( -1.225000000000048939, 0.06250000068282191013, -4.336808689942017736E-14 ) ) ;
#76312=CARTESIAN_POINT ( 'NONE',  ( -2.353626204688216217E-14, 0.7343750003414536431, 1.570758158831780271 ) ) ;
#76334=CARTESIAN_POINT ( 'NONE',  ( 0.6124999999999828360, -0.9166666666666628549, 1.060881119635932679 ) ) ;
#76415=LINE ( 'NONE', #164874, #99353 ) ;
#76440=ORIENTED_EDGE ( 'NONE', *, *, #188508, .T. ) ;
#76479=ORIENTED_EDGE ( 'NONE', *, *, #91562, .T. ) ;
#76620=CARTESIAN_POINT ( 'NONE',  ( 1.360316468749957597, -0.5052083329919204724, 0.7853790794159082322 ) ) ;
#76722=CARTESIAN_POINT ( 'NONE',  ( 1.360316468750004448, 2.546875000341383810, -3.295974604355933479E-14 ) ) ;
#76744=EDGE_CURVE ( 'NONE', #64456, #72069, #44423, .T. ) ;
#76755=DIRECTION ( 'NONE',  ( 1.276756478318932585E-15, -1.000000000000000000, 1.665334536937738262E-16 ) ) ;
#76812=AXIS2_PLACEMENT_3D ( 'NONE', #31125, #694, #130813 ) ;
#76845=CARTESIAN_POINT ( 'NONE',  ( 0.6801582343749935644, 0.9739583336747514863, 1.178068619123805227 ) ) ;
#76866=CARTESIAN_POINT ( 'NONE',  ( -0.6801582343750004478, 2.598958333674746157, -1.178068619123848526 ) ) ;
#76917=CARTESIAN_POINT ( 'NONE',  ( 0.6124999999999914957, 0.2291666673494702211, -1.060881119635965764 ) ) ;
#77054=CARTESIAN_POINT ( 'NONE',  ( -1.772826578343107640, 3.949999999999974420, 0.4499999999999487188 ) ) ;
#77078=CARTESIAN_POINT ( 'NONE',  ( 1.360316468749992236, 1.546875000341396689, -1.040834085586084257E-14 ) ) ;
#77201=EDGE_CURVE ( 'NONE', #99096, #21883, #148554, .T. ) ;
#77286=LINE ( 'NONE', #209395, #43454 ) ;
#77287=DIRECTION ( 'NONE',  ( 3.330669073875478989E-16, -3.540251991789410786E-16, -1.000000000000000000 ) ) ;
#77340=TOROIDAL_SURFACE ( 'NONE', #198391, 1.052419468952678239, 0.9475805310473219834 ) ;
#77352=ADVANCED_FACE ( 'NONE', ( #80092 ), #125436, .T. ) ;
#77378=CARTESIAN_POINT ( 'NONE',  ( -1.360316468750042862, 0.9010416670080622081, -0.7853790794159041244 ) ) ;
#77399=CARTESIAN_POINT ( 'NONE',  ( 0.6801582343749831283, 2.755208333674742605, 1.178068619123796568 ) ) ;
#77422=CARTESIAN_POINT ( 'NONE',  ( -0.4500000000000382583, 3.999999999999934275, 0.9353126743250876896 ) ) ;
#77438=CARTESIAN_POINT ( 'NONE',  ( -1.162044386198238935E-15, 2.625000000682799151, 1.224999999999985656 ) ) ;
#77479=DIRECTION ( 'NONE',  ( -3.330669073875478989E-16, 3.330669073875478989E-16, 1.000000000000000000 ) ) ;
#77589=CARTESIAN_POINT ( 'NONE',  ( -0.6311622855796790166, 3.199999999999973532, -0.4000000000000444311 ) ) ;
#77608=( BOUNDED_CURVE ( )  B_SPLINE_CURVE ( 2, ( #197975, #136209, #34413, #166560, #131963, #214189, #52803, #181719, #18149 ),
 .UNSPECIFIED., .F., .T. ) 
 B_SPLINE_CURVE_WITH_KNOTS ( ( 3, 2, 2, 2, 3 ),
 ( 0.4531250000000001665, 0.4583333333333333148, 0.4687500000000000000, 0.4791666666666666852, 0.4843749999999998335 ),
 .UNSPECIFIED. ) 
 CURVE ( )  GEOMETRIC_REPRESENTATION_ITEM ( )  RATIONAL_B_SPLINE_CURVE ( ( 0.9330127018922194093, 0.9330127018922215187, 1.000000000000000000, 0.8660254037844387076, 1.000000000000000000, 0.8660254037844387076, 1.000000000000000000, 0.9330127018922215187, 0.9330127018922194093 ) ) 
 REPRESENTATION_ITEM ( '' )  );
#77664=ADVANCED_FACE ( 'NONE', ( #183986 ), #119056, .T. ) ;
#77689=CARTESIAN_POINT ( 'NONE',  ( -0.6801582343750213200, -1.067708332991926135, 1.178068619123832983 ) ) ;
#77793=CARTESIAN_POINT ( 'NONE',  ( -4.957638175832625493E-14, 2.359375000341373152, -1.570758158831806250 ) ) ;
#77834=VERTEX_POINT ( 'NONE', #37747 ) ;
#77841=EDGE_CURVE ( 'NONE', #137780, #55379, #18275, .T. ) ;
#77851=AXIS2_PLACEMENT_3D ( 'NONE', #177489, #46425, #32298 ) ;
#77906=EDGE_CURVE ( 'NONE', #141010, #101381, #156850, .T. ) ;
#77917=CARTESIAN_POINT ( 'NONE',  ( -1.360316468750006669, 0.1614583336747227316, 0.7853790794158981292 ) ) ;
#77952=CARTESIAN_POINT ( 'NONE',  ( 1.899436509991839772, 3.291494839451058585, -0.4074537448169834319 ) ) ;
#78031=CARTESIAN_POINT ( 'NONE',  ( -0.4626273691814333788, 3.108307088186319955, -0.4053073865230780726 ) ) ;
#78037=CARTESIAN_POINT ( 'NONE',  ( -1.981527703613581659, 3.480048614628247439, 0.4617793045967767407 ) ) ;
#78052=CARTESIAN_POINT ( 'NONE',  ( -6.158835246850665884E-15, 0.8125000000000031086, 1.224999999999960565 ) ) ;
#78055=ORIENTED_EDGE ( 'NONE', *, *, #147413, .F. ) ;
#78057=VERTEX_POINT ( 'NONE', #6287 ) ;
#78073=AXIS2_PLACEMENT_3D ( 'NONE', #111443, #75680, #45323 ) ;
#78125=DIRECTION ( 'NONE',  ( 0.000000000000000000, 0.000000000000000000, -1.000000000000000000 ) ) ;
#78146=CARTESIAN_POINT ( 'NONE',  ( 0.6801582343749970061, 0.8385416670080649837, -1.178068619123841643 ) ) ;
#78155=ORIENTED_EDGE ( 'NONE', *, *, #68743, .F. ) ;
#78213=B_SPLINE_CURVE_WITH_KNOTS ( 'NONE', 3,
 ( #174505, #200808, #185640, #102268 ),
 .UNSPECIFIED., .F., .F.,
 ( 4, 4 ),
 ( 0.000000000000000000, 0.0007699926951938504535 ),
 .UNSPECIFIED. ) ;
#78311=CARTESIAN_POINT ( 'NONE',  ( -1.872228381520320672, 3.299999999999962519, 0.3999999999999628852 ) ) ;
#78358=CARTESIAN_POINT ( 'NONE',  ( -1.225000000000038058, 2.083333334016205907, 0.7072540797572697269 ) ) ;
#78374=CARTESIAN_POINT ( 'NONE',  ( 0.3782569160206556425, 3.049340702855431129, 0.4285286083245459787 ) ) ;
#78432=CARTESIAN_POINT ( 'NONE',  ( -0.3000000000000352940, 3.999999999999973799, 0.9782388782688533624 ) ) ;
#78443=CARTESIAN_POINT ( 'NONE',  ( 1.360316468749955598, -0.7239583329918893861, 0.7853790794158480582 ) ) ;
#78547=DIRECTION ( 'NONE',  ( -3.330669073875478989E-16, 3.540251991789410786E-16, 1.000000000000000000 ) ) ;
#78649=CARTESIAN_POINT ( 'NONE',  ( 0.3282377607281126708, 1.738835450998185372, -1.225000000000013634 ) ) ;
#78664=AXIS2_PLACEMENT_3D ( 'NONE', #29281, #74836, #160345 ) ;
#78715=UNCERTAINTY_MEASURE_WITH_UNIT (LENGTH_MEASURE( 1.000000000000000082E-05 ), #194570, 'distance_accuracy_value', 'NONE');
#78749=CARTESIAN_POINT ( 'NONE',  ( -0.6801582343750125492, -0.6510416663252707181, -1.178068619123848526 ) ) ;
#78803=AXIS2_PLACEMENT_3D ( 'NONE', #18823, #23896, #184526 ) ;
#78847=CARTESIAN_POINT ( 'NONE',  ( 0.6801582343749917881, 1.005208333674747934, 1.178068619123807004 ) ) ;
#78851=CARTESIAN_POINT ( 'NONE',  ( -2.449742653233059286, 3.300000000000011369, 0.3999999999999750422 ) ) ;
#78856=CARTESIAN_POINT ( 'NONE',  ( -0.4169036860910396713, 3.145283463680773828, -0.4342470185719663478 ) ) ;
#78897=CARTESIAN_POINT ( 'NONE',  ( 1.904329973710225055, 3.286760881231386211, 0.4119279214152646862 ) ) ;
#78955=EDGE_LOOP ( 'NONE', ( #41673, #64165, #157704, #192936 ) ) ;
#78979=CARTESIAN_POINT ( 'NONE',  ( 1.360316468749955598, -0.005208332991877948244, 0.7853790794158660438 ) ) ;
#78994=DIRECTION ( 'NONE',  ( 3.330669073875478989E-16, -3.540251991789410786E-16, -1.000000000000000000 ) ) ;
#79113=EDGE_CURVE ( 'NONE', #23033, #139477, #152097, .T. ) ;
#79128=CARTESIAN_POINT ( 'NONE',  ( -1.813763795902466613, 3.949999999999988187, -0.4000000000000339950 ) ) ;
#79132=EDGE_CURVE ( 'NONE', #142570, #105749, #78213, .T. ) ;
#79139=CARTESIAN_POINT ( 'NONE',  ( 1.224999999999979661, 1.437500000682781387, -2.602085213965210642E-14 ) ) ;
#79155=ORIENTED_EDGE ( 'NONE', *, *, #138823, .T. ) ;
#79169=VECTOR ( 'NONE', #83592, 1000.000000000000000 ) ;
#79181=CIRCLE ( 'NONE', #155260, 0.9475805310473219834 ) ;
#79217=CARTESIAN_POINT ( 'NONE',  ( -1.360316468750030428, 1.171875000341417117, -4.336808689942017736E-14 ) ) ;
#79218=CARTESIAN_POINT ( 'NONE',  ( -0.4170821662629227156, 3.033599471985643170, 0.4170821662629036752 ) ) ;
#79260=CARTESIAN_POINT ( 'NONE',  ( 1.360316468749949825, 1.994791667008131597, 0.7853790794158700406 ) ) ;
#79313=CARTESIAN_POINT ( 'NONE',  ( -0.5000000000000247580, 3.172938907704287104, 0.3999999999999698241 ) ) ;
#79392=ADVANCED_FACE ( 'NONE', ( #161442 ), #57443, .T. ) ;
#79516=CARTESIAN_POINT ( 'NONE',  ( 0.6801582343749883464, -0.7447916663252535097, 1.178068619123796568 ) ) ;
#79520=EDGE_LOOP ( 'NONE', ( #101836, #15925, #143824, #134606 ) ) ;
#79677=CARTESIAN_POINT ( 'NONE',  ( -1.360316468750013108, 2.921875000341411788, -1.734723475976807094E-14 ) ) ;
#79720=CARTESIAN_POINT ( 'NONE',  ( 0.3282377607281143916, 1.636164550367421144, 1.224999999999978995 ) ) ;
#79772=CARTESIAN_POINT ( 'NONE',  ( 3.486133158594716510E-16, 0.8750000006828204668, 1.224999999999968336 ) ) ;
#79818=CARTESIAN_POINT ( 'NONE',  ( 1.360316468749967589, -0.2552083329918390930, 0.7853790794158500566 ) ) ;
#79827=CARTESIAN_POINT ( 'NONE',  ( 0.4999999999999952260, 3.172938907704321743, -0.4000000000000062395 ) ) ;
#79834=CARTESIAN_POINT ( 'NONE',  ( -5.810221930991193690E-16, 2.125000000682803147, 1.224999999999976774 ) ) ;
#79852=CARTESIAN_POINT ( 'NONE',  ( -0.9782388782689256379, 3.999999999999989786, 0.3999999999999559464 ) ) ;
#79917=CARTESIAN_POINT ( 'NONE',  ( 1.360316468749987129, 1.796875000341410900, -3.295974604355933479E-14 ) ) ;
#79942=FACE_OUTER_BOUND ( 'NONE', #18160, .T. ) ;
#79965=CARTESIAN_POINT ( 'NONE',  ( 0.9782388782688926643, 3.999999999999968914, 0.3999999999999576672 ) ) ;
#80048=CARTESIAN_POINT ( 'NONE',  ( -0.6801582343749917881, 0.4322916670080681478, 1.178068619123841643 ) ) ;
#80054=PRODUCT ( 'screw coil', 'screw coil', '', ( #119792 ) ) ;
#80056=ADVANCED_FACE ( 'NONE', ( #115802 ), #11875, .F. ) ;
#80068=ORIENTED_EDGE ( 'NONE', *, *, #117177, .F. ) ;
#80092=FACE_OUTER_BOUND ( 'NONE', #52715, .T. ) ;
#80168=CARTESIAN_POINT ( 'NONE',  ( -1.906195883197663310, 3.231669652568780027, 0.4612786727877704052 ) ) ;
#80239=CARTESIAN_POINT ( 'NONE',  ( 0.3645075752534727709, 3.999999999999974243, -0.9782388703847851863 ) ) ;
#80257=EDGE_LOOP ( 'NONE', ( #40796, #135320, #151450 ) ) ;
#80283=CARTESIAN_POINT ( 'NONE',  ( -0.6801582343750438575, 0.6302083336747199560, -1.178068619123869398 ) ) ;
#80284=CARTESIAN_POINT ( 'NONE',  ( -0.4288785890452732064, 3.049942316455313218, 0.4196807566830707548 ) ) ;
#80342=ORIENTED_EDGE ( 'NONE', *, *, #4745, .T. ) ;
#80344=DIRECTION ( 'NONE',  ( 3.330669073875479482E-16, -3.330669073875479482E-16, -1.000000000000000000 ) ) ;
#80347=EDGE_LOOP ( 'NONE', ( #213002, #45741, #80068, #48402 ) ) ;
#80360=ORIENTED_EDGE ( 'NONE', *, *, #152637, .F. ) ;
#80389=DIRECTION ( 'NONE',  ( 1.276756478318932585E-15, -1.000000000000000000, 1.665334536937738262E-16 ) ) ;
#80420=VERTEX_POINT ( 'NONE', #100560 ) ;
#80469=EDGE_CURVE ( 'NONE', #74826, #132173, #184078, .T. ) ;
#80509=AXIS2_PLACEMENT_3D ( 'NONE', #121500, #154986, #174454 ) ;
#80559=CARTESIAN_POINT ( 'NONE',  ( -0.4288785890453234995, 3.049942316455299451, -0.4196807566834767078 ) ) ;
#80572=FACE_OUTER_BOUND ( 'NONE', #201599, .T. ) ;
#80584=CARTESIAN_POINT ( 'NONE',  ( -3.505400730386704341E-15, 2.703125000341406459, 1.570758158831794260 ) ) ;
#80620=EDGE_CURVE ( 'NONE', #86803, #211691, #166870, .T. ) ;
#80795=LINE ( 'NONE', #48311, #67532 ) ;
#80816=VECTOR ( 'NONE', #17490, 1000.000000000000000 ) ;
#80843=FACE_OUTER_BOUND ( 'NONE', #137875, .T. ) ;
#80851=CARTESIAN_POINT ( 'NONE',  ( -0.3000000000000380695, 3.975028841772282107, 0.9637995837462106641 ) ) ;
#80889=EDGE_CURVE ( 'NONE', #3320, #171576, #104798, .T. ) ;
#80896=CARTESIAN_POINT ( 'NONE',  ( -3.355169270512988773E-14, -0.7968749996585455797, 1.570758158831762286 ) ) ;
#80910=CARTESIAN_POINT ( 'NONE',  ( 0.3282377607281127818, 2.238835450998152954, -1.225000000000007860 ) ) ;
#80994=CARTESIAN_POINT ( 'NONE',  ( 0.6801582343749900117, 1.338541667008072533, -1.178068619123872729 ) ) ;
#81019=( BOUNDED_SURFACE ( )  B_SPLINE_SURFACE ( 3, 2, ( 
 ( #178084, #31836, #148775 ),
 ( #129416, #160758, #98967 ),
 ( #344, #162901, #14483 ),
 ( #147719, #78432, #50210 ) ),
 .UNSPECIFIED., .F., .F., .T. ) 
 B_SPLINE_SURFACE_WITH_KNOTS ( ( 4, 4 ),
 ( 3, 3 ),
 ( 4.712388980384689674, 6.283185307179586232 ),
 ( 0.000000000000000000, 1.000000000000000000 ),
 .UNSPECIFIED. ) 
 GEOMETRIC_REPRESENTATION_ITEM ( )  RATIONAL_B_SPLINE_SURFACE ( (
 ( 1.000000000000000000, 0.7071067811865286989, 1.000000000000000000),
 ( 1.000000000000000000, 0.8014503788334959022, 1.000000000000000000),
 ( 1.000000000000000000, 0.8676977444973670295, 1.000000000000000000),
 ( 1.000000000000000000, 0.8661919058288164441, 1.000000000000000000) ) ) 
 REPRESENTATION_ITEM ( '' )  SURFACE ( )  );
#81028=APPLICATION_CONTEXT ( 'automotive_design' ) ;
#81122=CARTESIAN_POINT ( 'NONE',  ( -1.360316468750014884, -0.8593749996585950957, -6.938893903907228378E-15 ) ) ;
#81142=CARTESIAN_POINT ( 'NONE',  ( 1.224999999999958789, 2.104166666666714036, 0.7072540797572757221 ) ) ;
#81178=CARTESIAN_POINT ( 'NONE',  ( 1.947641667917405117, 3.752373307046534379, -0.4616076617488063527 ) ) ;
#81192=CARTESIAN_POINT ( 'NONE',  ( 0.4499999999999504396, 3.999999999999996891, 0.9353126743250794739 ) ) ;
#81236=CARTESIAN_POINT ( 'NONE',  ( -1.882262909678039886, 3.299172163371803190, -0.4004916885352671763 ) ) ;
#81270=EDGE_CURVE ( 'NONE', #109478, #209652, #101712, .T. ) ;
#81295=CARTESIAN_POINT ( 'NONE',  ( -1.734723475976807094E-15, 2.999999999999988898, -6.938893903907228378E-15 ) ) ;
#81350=CARTESIAN_POINT ( 'NONE',  ( 0.6801582343749744686, 0.3385416670080923507, -1.178068619123886718 ) ) ;
#81383=EDGE_CURVE ( 'NONE', #88486, #4353, #212397, .T. ) ;
#81387=DIRECTION ( 'NONE',  ( -3.330669073875478989E-16, 3.330669073875478989E-16, 1.000000000000000000 ) ) ;
#81388=CARTESIAN_POINT ( 'NONE',  ( -1.360316468750007779, 2.390625000341400685, -1.734723475976807094E-15 ) ) ;
#81519=VERTEX_POINT ( 'NONE', #63326 ) ;
#81530=DIRECTION ( 'NONE',  ( -2.126226658603517140E-31, 1.665334536937738015E-16, 1.000000000000000000 ) ) ;
#81560=CARTESIAN_POINT ( 'NONE',  ( -0.4000000000000200617, 3.963633530850230180, -0.9046180958551521822 ) ) ;
#81642=CARTESIAN_POINT ( 'NONE',  ( 0.6801582343749674742, -0.2447916663252461267, 1.178068619123796568 ) ) ;
#81735=AXIS2_PLACEMENT_3D ( 'NONE', #51232, #50165, #135690 ) ;
#81768=ORIENTED_EDGE ( 'NONE', *, *, #139653, .F. ) ;
#81780=CARTESIAN_POINT ( 'NONE',  ( -2.324088772396477673E-16, 1.562500000000000666, 1.224999999999980549 ) ) ;
#81837=ORIENTED_EDGE ( 'NONE', *, *, #87216, .F. ) ;
#81956=ORIENTED_EDGE ( 'NONE', *, *, #37910, .F. ) ;
#82038=ORIENTED_EDGE ( 'NONE', *, *, #57301, .F. ) ;
#82049=CARTESIAN_POINT ( 'NONE',  ( 0.6801582343749883464, 1.505208333674713739, 1.178068619123805227 ) ) ;
#82176=CARTESIAN_POINT ( 'NONE',  ( 0.6801582343749674742, -0.4427083329919187515, -1.178068619123886718 ) ) ;
#82198=CARTESIAN_POINT ( 'NONE',  ( -1.360316468750008667, 2.369791667008076974, -0.7853790794159001276 ) ) ;
#82320=ADVANCED_FACE ( 'NONE', ( #212506 ), #30589, .F. ) ;
#82343=DIRECTION ( 'NONE',  ( 1.276756478318932585E-15, -1.000000000000000000, 1.665334536937738262E-16 ) ) ;
#82366=CARTESIAN_POINT ( 'NONE',  ( -0.6125000000000226930, 0.2083333333333242665, -1.060881119635965764 ) ) ;
#82384=CARTESIAN_POINT ( 'NONE',  ( 1.224999999999979661, 1.624999999999987566, -3.989863994746656317E-14 ) ) ;
#82400=CARTESIAN_POINT ( 'NONE',  ( 0.4499999999999834133, 3.949999999999995293, 0.8338124244295450627 ) ) ;
#82403=CARTESIAN_POINT ( 'NONE',  ( -5.558564015327489343E-14, 0.4843750003414603600, 1.570758158831762286 ) ) ;
#82440=CARTESIAN_POINT ( 'NONE',  ( -3.555477883677943599E-14, 1.578125000341449535, -1.570758158831814466 ) ) ;
#82545=B_SPLINE_CURVE_WITH_KNOTS ( 'NONE', 3,
 ( #167378, #183615, #198779, #36290 ),
 .UNSPECIFIED., .F., .F.,
 ( 4, 4 ),
 ( 0.000000000000000000, 1.930757672285080358E-06 ),
 .UNSPECIFIED. ) ;
#82628=AXIS2_PLACEMENT_3D ( 'NONE', #212180, #47597, #78994 ) ;
#82699=( BOUNDED_CURVE ( )  B_SPLINE_CURVE ( 2, ( #143216, #156235, #122751, #175680, #25137, #93376, #7812, #188713, #207087 ),
 .UNSPECIFIED., .F., .T. ) 
 B_SPLINE_CURVE_WITH_KNOTS ( ( 3, 2, 2, 2, 3 ),
 ( 0.07812500000000022204, 0.08333333333333332871, 0.09375000000000000000, 0.1041666666666666713, 0.1093749999999998473 ),
 .UNSPECIFIED. ) 
 CURVE ( )  GEOMETRIC_REPRESENTATION_ITEM ( )  RATIONAL_B_SPLINE_CURVE ( ( 0.9330127018922194093, 0.9330127018922221849, 1.000000000000000000, 0.8660254037844387076, 1.000000000000000000, 0.8660254037844387076, 1.000000000000000000, 0.9330127018922212967, 0.9330127018922194093 ) ) 
 REPRESENTATION_ITEM ( '' )  );
#82702=CARTESIAN_POINT ( 'NONE',  ( -1.360316468750024876, -0.8072916663252578395, 0.7853790794158560518 ) ) ;
#82754=DIRECTION ( 'NONE',  ( 1.000000000000000000, 0.000000000000000000, -4.440892098500751393E-16 ) ) ;
#82837=PLANE ( 'NONE',  #138706 ) ;
#82844=EDGE_CURVE ( 'NONE', #47983, #171576, #177615, .T. ) ;
#82847=CARTESIAN_POINT ( 'NONE',  ( -0.6125000000000175859, 2.541666666666664298, 1.060881119635903147 ) ) ;
#82850=ORIENTED_EDGE ( 'NONE', *, *, #185099, .F. ) ;
#82886=EDGE_CURVE ( 'NONE', #210405, #68973, #67300, .T. ) ;
#83031=EDGE_CURVE ( 'NONE', #192043, #163067, #85711, .T. ) ;
#83073=DIRECTION ( 'NONE',  ( -1.000000000000000000, 7.771561172376097755E-16, 4.440892098500627148E-16 ) ) ;
#83101=EDGE_LOOP ( 'NONE', ( #46479, #140019, #31812, #208324 ) ) ;
#83107=ADVANCED_FACE ( 'NONE', ( #183213 ), #20089, .T. ) ;
#83112=CARTESIAN_POINT ( 'NONE',  ( -0.6801582343750368631, 2.130208333674714183, -1.178068619123862515 ) ) ;
#83118=ORIENTED_EDGE ( 'NONE', *, *, #118396, .F. ) ;
#83130=EDGE_CURVE ( 'NONE', #108528, #50089, #4883, .T. ) ;
#83238=CARTESIAN_POINT ( 'NONE',  ( 1.360316468749949825, -0.9635416663252907021, -0.7853790794159282163 ) ) ;
#83260=CARTESIAN_POINT ( 'NONE',  ( -0.6801582343750438575, 1.932291667008062541, 1.178068619123787908 ) ) ;
#83277=DIRECTION ( 'NONE',  ( 1.000000000000000000, -7.771561172376097755E-16, -4.440892098500627148E-16 ) ) ;
#83290=CARTESIAN_POINT ( 'NONE',  ( 1.814759087649971958, 3.975067388631723819, -0.4606438099578624157 ) ) ;
#83334=CARTESIAN_POINT ( 'NONE',  ( -0.6125000000000053735, 2.708333333333333481, -1.060881119635955327 ) ) ;
#83469=CARTESIAN_POINT ( 'NONE',  ( -3.755786496842897795E-14, -0.01562499965858205574, 1.570758158831768281 ) ) ;
#83507=CARTESIAN_POINT ( 'NONE',  ( 1.360316468749943608, 1.494791667008105174, 0.7853790794158440614 ) ) ;
#83592=DIRECTION ( 'NONE',  ( 1.276756478318932585E-15, -1.000000000000000000, 1.665334536937738262E-16 ) ) ;
#83602=DIRECTION ( 'NONE',  ( 1.000000000000000000, 0.000000000000000000, -4.440892098500751393E-16 ) ) ;
#83718=LINE ( 'NONE', #2444, #88449 ) ;
#83767=CARTESIAN_POINT ( 'NONE',  ( -1.360316468749998675, 2.411458333674741716, 0.7853790794158941324 ) ) ;
#83831=LINE ( 'NONE', #149923, #56410 ) ;
#83937=CARTESIAN_POINT ( 'NONE',  ( -1.225000000000001865, 0.7291666666666755114, -0.7072540797572917093 ) ) ;
#83994=ORIENTED_EDGE ( 'NONE', *, *, #65201, .T. ) ;
#84017=CARTESIAN_POINT ( 'NONE',  ( -1.360316468750026653, 2.192708333674788346, 0.7853790794158680422 ) ) ;
#84042=CARTESIAN_POINT ( 'NONE',  ( -1.225000000000002309, 0.7291666666666755114, -0.7072540797572917093 ) ) ;
#84097=CARTESIAN_POINT ( 'NONE',  ( 1.224999999999971001, 2.187500000682782275, -4.683753385137379155E-14 ) ) ;
#84186=ORIENTED_EDGE ( 'NONE', *, *, #2174, .T. ) ;
#84190=CARTESIAN_POINT ( 'NONE',  ( 0.6801582343749935644, 0.2552083336747196229, 1.178068619123780802 ) ) ;
#84225=DIRECTION ( 'NONE',  ( -1.000000000000000000, 7.771561172376097755E-16, 4.440892098500627148E-16 ) ) ;
#84236=LINE ( 'NONE', #135147, #75524 ) ;
#84254=EDGE_CURVE ( 'NONE', #195414, #205644, #183317, .T. ) ;
#84291=AXIS2_PLACEMENT_3D ( 'NONE', #4508, #70579, #42411 ) ;
#84303=CARTESIAN_POINT ( 'NONE',  ( 0.3282377607281126153, 0.8861645503674525637, 1.224999999999959455 ) ) ;
#84311=VECTOR ( 'NONE', #15849, 1000.000000000000000 ) ;
#84340=CARTESIAN_POINT ( 'NONE',  ( 0.6801582343749831283, 1.223958333674737720, 1.178068619123822547 ) ) ;
#84367=AXIS2_PLACEMENT_3D ( 'NONE', #38590, #104667, #77479 ) ;
#84408=ORIENTED_EDGE ( 'NONE', *, *, #192933, .F. ) ;
#84457=EDGE_LOOP ( 'NONE', ( #81837, #17550, #161688, #47173 ) ) ;
#84486=CARTESIAN_POINT ( 'NONE',  ( -1.734723475976807094E-15, 2.999999999999988898, -6.938893903907228378E-15 ) ) ;
#84499=CARTESIAN_POINT ( 'NONE',  ( -0.3282377607281437570, 2.801335450315371567, 1.224999999999956790 ) ) ;
#84500=CARTESIAN_POINT ( 'NONE',  ( 6.856061878569608298E-15, 0.1875000000000181521, -1.225000000000034950 ) ) ;
#84530=CARTESIAN_POINT ( 'NONE',  ( 0.6125000000000019318, 1.229166667349464115, -1.060881119635941339 ) ) ;
#84537=DIRECTION ( 'NONE',  ( -1.665334536937739149E-15, 5.551115123125797493E-17, -1.000000000000000000 ) ) ;
#84538=SURFACE_STYLE_FILL_AREA ( #150628 ) ;
#84540=CARTESIAN_POINT ( 'NONE',  ( -1.360316468750028651, -0.8281249996586054207, -3.469446951953614189E-14 ) ) ;
#84541=CARTESIAN_POINT ( 'NONE',  ( 0.5445930744353757458, 3.250057683544679943, 0.3999999999999542255 ) ) ;
#84551=DIRECTION ( 'NONE',  ( 3.330669073875478989E-16, -4.632576442341012461E-16, -1.000000000000000000 ) ) ;
#84584=CARTESIAN_POINT ( 'NONE',  ( 1.360316468749983576, 1.515625000341386253, -4.163336342344337027E-14 ) ) ;
#84593=ORIENTED_EDGE ( 'NONE', *, *, #88639, .F. ) ;
#84759=DIRECTION ( 'NONE',  ( 1.165734175856416734E-15, -0.5005768354468322912, -0.8656921114426507913 ) ) ;
#84876=CARTESIAN_POINT ( 'NONE',  ( 1.224999999999974998, 2.416666667349527842, 0.7072540797572656190 ) ) ;
#84896=EDGE_CURVE ( 'NONE', #132409, #72572, #45279, .T. ) ;
#84983=ORIENTED_EDGE ( 'NONE', *, *, #202085, .F. ) ;
#85001=CARTESIAN_POINT ( 'NONE',  ( 0.2999999999999981570, 3.999999999999996447, -0.9782388782689065421 ) ) ;
#85086=CARTESIAN_POINT ( 'NONE',  ( -1.930984528693968194, 3.480873151564079837, -0.4000000000000285549 ) ) ;
#85089=CARTESIAN_POINT ( 'NONE',  ( -4.957638175832625493E-14, 2.359375000341373152, -1.570758158831806250 ) ) ;
#85109=CARTESIAN_POINT ( 'NONE',  ( -1.225000000000014300, 0.7500000000000145439, -2.602085213965210642E-14 ) ) ;
#85122=CARTESIAN_POINT ( 'NONE',  ( -0.3713344243775550391, 2.999999999999984901, -0.3713344243775790754 ) ) ;
#85152=MANIFOLD_SOLID_BREP ( 'Cut-Extrude3', #91447 ) ;
#85244=ORIENTED_EDGE ( 'NONE', *, *, #22906, .F. ) ;
#85255=CARTESIAN_POINT ( 'NONE',  ( -0.6801582343750438575, 0.1302083336747333897, -1.178068619123883165 ) ) ;
#85392=DIRECTION ( 'NONE',  ( -0.5131086435338325646, -0.8583236685137316524, 4.218847493575600376E-15 ) ) ;
#85407=CARTESIAN_POINT ( 'NONE',  ( -1.360316468750007779, 2.390625000341400685, -1.734723475976807094E-15 ) ) ;
#85480=CARTESIAN_POINT ( 'NONE',  ( -1.225000000000014300, 2.750000000000002665, -3.469446951953614189E-14 ) ) ;
#85493=CARTESIAN_POINT ( 'NONE',  ( -1.874158809982213958, 3.299964346911606228, -0.4000000000000374922 ) ) ;
#85534=CARTESIAN_POINT ( 'NONE',  ( -1.872228381520322449, 3.300000000000011369, -0.3999999999999993006 ) ) ;
#85567=CARTESIAN_POINT ( 'NONE',  ( -0.6125000000000105915, -0.7291666659838408338, -1.060881119635976200 ) ) ;
#85573=VECTOR ( 'NONE', #162110, 1000.000000000000000 ) ;
#85603=SURFACE_STYLE_USAGE ( .BOTH. , #16316 ) ;
#85605=CARTESIAN_POINT ( 'NONE',  ( -3.956095110007852622E-14, -1.015624999658570893, 1.570758158831770279 ) ) ;
#85647=CARTESIAN_POINT ( 'NONE',  ( -1.360316468750040642, 1.161458333674751486, 0.7853790794158861388 ) ) ;
#85663=ORIENTED_EDGE ( 'NONE', *, *, #13041, .T. ) ;
#85711=LINE ( 'NONE', #132379, #163860 ) ;
#85725=DIRECTION ( 'NONE',  ( -3.497202527569253358E-15, 0.000000000000000000, -1.000000000000000000 ) ) ;
#85728=ADVANCED_FACE ( 'NONE', ( #190859 ), #26229, .T. ) ;
#85840=CARTESIAN_POINT ( 'NONE',  ( -1.873515663034590606, 3.299988112486754943, -0.4000000000000374922 ) ) ;
#85916=EDGE_CURVE ( 'NONE', #150426, #107948, #86531, .T. ) ;
#85951=CARTESIAN_POINT ( 'NONE',  ( -4.957638175832625493E-14, 2.375000000682783163, 1.414508159514561436 ) ) ;
#85972=CIRCLE ( 'NONE', #68627, 0.04999999999999985706 ) ;
#86051=EDGE_CURVE ( 'NONE', #62971, #184258, #71320, .T. ) ;
#86055=CARTESIAN_POINT ( 'NONE',  ( -1.360316468750033980, 2.906250000341399797, -3.469446951953614189E-14 ) ) ;
#86058=EDGE_LOOP ( 'NONE', ( #151666, #27358, #14388 ) ) ;
#86067=AXIS2_PLACEMENT_3D ( 'NONE', #199403, #164796, #16388 ) ;
#86068=CARTESIAN_POINT ( 'NONE',  ( 0.2999999999999859446, 3.322650755865473204, -0.5865692111442881718 ) ) ;
#86100=( BOUNDED_CURVE ( )  B_SPLINE_CURVE ( 2, ( #208380, #93609, #61084, #161798, #76262, #162864, #43794, #211579, #175918 ),
 .UNSPECIFIED., .F., .T. ) 
 B_SPLINE_CURVE_WITH_KNOTS ( ( 3, 2, 2, 2, 3 ),
 ( 0.6718749999999998890, 0.6770833333333333703, 0.6875000000000000000, 0.6979166666666666297, 0.7031250001592646015 ),
 .UNSPECIFIED. ) 
 CURVE ( )  GEOMETRIC_REPRESENTATION_ITEM ( )  RATIONAL_B_SPLINE_CURVE ( ( 0.9330127018922192983, 0.9330127018922178550, 1.000000000000000000, 0.8660254037844387076, 1.000000000000000000, 0.8660254037844387076, 1.000000000000000000, 0.9330126998438279529, 0.9330127018922194093 ) ) 
 REPRESENTATION_ITEM ( '' )  );
#86160=CARTESIAN_POINT ( 'NONE',  ( -0.6801582343750282034, 1.963541667008045222, 1.178068619123803451 ) ) ;
#86183=CARTESIAN_POINT ( 'NONE',  ( -1.225000000000019407, 1.250000000000028866, -1.734723475976807094E-14 ) ) ;
#86221=CARTESIAN_POINT ( 'NONE',  ( 0.2999999999999511391, 3.322650755865479866, 0.5865692111442165624 ) ) ;
#86444=CARTESIAN_POINT ( 'NONE',  ( 3.486133158594716510E-16, 0.8750000006828204668, 1.224999999999968336 ) ) ;
#86479=CARTESIAN_POINT ( 'NONE',  ( 0.6801582343749883464, 2.473958333674766585, 1.178068619123824323 ) ) ;
#86531=( BOUNDED_CURVE ( )  B_SPLINE_CURVE ( 2, ( #209228, #143239, #47856, #212436, #113968, #44645, #12112, #64078, #15300, #195149, #130221, #30523, #60873, #162655, #161593, #179965, #29452, #176758, #97662, #163719, #13182, #63001, #45716, #145377, #81388, #144312, #111834, #131271, #109700, #213493, #65115, #210310, #43584, #178908, #175705, #27295, #93402, #159439, #11037, #61946, #128105, #194063, #177838, #79260, #211375, #46783, #70434, #98713, #199377, #18504, #133372, #150671, #167968, #51024, #164772, #118216, #197259, #100826, #17424, #169029, #198314, #166911, #3304, #82440, #67238, #69374, #84584, #83507, #184202, #49955, #102971, #35825, #116074, #99773, #149590, #182064, #66163, #16362, #19574, #101903, #1173, #148530, #201504, #85647, #53150, #33696, #165838, #151734, #20626, #134440, #135482, #119280, #97, #185266, #2232, #36889, #183149, #132308, #86715, #152784, #68309, #32636, #117145, #34752, #200443, #52089, #4364, #48899, #115019, #181015, #121438, #170090, #204703, #58485, #37971, #205788, #136550, #25970, #202571, #158133, #55288, #173322, #7578, #22752, #73663, #153860, #54223, #56353, #6509, #137620, #140841, #187407, #188479, #39038, #5429, #190598, #74736, #203637, #107298, #171163, #40109 ),
 .UNSPECIFIED., .F., .T. ) 
 B_SPLINE_CURVE_WITH_KNOTS ( ( 3, 2, 2, 2, 2, 2, 2, 2, 2, 2, 2, 2, 2, 2, 2, 2, 2, 2, 2, 2, 2, 2, 2, 2, 2, 2, 2, 2, 2, 2, 2, 2, 2, 2, 2, 2, 2, 2, 2, 2, 2, 2, 2, 2, 2, 2, 2, 2, 2, 2, 2, 2, 2, 2, 2, 2, 2, 2, 2, 2, 2, 2, 2, 2, 2, 2, 2, 2, 2, 2, 3 ),
 ( 0.000000000000000000, 0.01041666666666666609, 0.02083333333333333218, 0.03125000000000000000, 0.04166666666666666435, 0.05208333333333334259, 0.06250000000000000000, 0.07291666666666667129, 0.08333333333333332871, 0.09375000000000000000, 0.1041666666666666852, 0.1145833333333333148, 0.1250000000000000000, 0.1354166666666666574, 0.1458333333333333426, 0.1562500000000000000, 0.1666666666666666574, 0.1770833333333333426, 0.1875000000000000000, 0.1979166666666666574, 0.2083333333333333703, 0.2187499999999999722, 0.2291666666666666297, 0.2395833333333333426, 0.2500000000000000000, 0.2604166666666666852, 0.2708333333333333148, 0.2812500000000000000, 0.2916666666666666852, 0.3020833333333333148, 0.3125000000000000000, 0.3229166666666666852, 0.3333333333333333148, 0.3437500000000000000, 0.3541666666666666852, 0.3645833333333333148, 0.3750000000000000000, 0.3854166666666666852, 0.3958333333333333148, 0.4062500000000000000, 0.4166666666666667407, 0.4270833333333333148, 0.4374999999999999445, 0.4479166666666666852, 0.4583333333333332593, 0.4687500000000000000, 0.4791666666666666852, 0.4895833333333333148, 0.5000000000000000000, 0.5104166666666666297, 0.5208333333333333703, 0.5312500000000000000, 0.5416666666666666297, 0.5520833333333333703, 0.5625000000000000000, 0.5729166666666666297, 0.5833333333333333703, 0.5937500000000000000, 0.6041666666666666297, 0.6145833333333333703, 0.6250000000000000000, 0.6354166666666666297, 0.6458333333333333703, 0.6562500000000000000, 0.6666666666666666297, 0.6770833333333333703, 0.6875000000000000000, 0.6979166666666666297, 0.7083333333333333703, 0.7187500000000000000, 0.7227386901363775928 ),
 .UNSPECIFIED. ) 
 CURVE ( )  GEOMETRIC_REPRESENTATION_ITEM ( )  RATIONAL_B_SPLINE_CURVE ( ( 1.000000000000000000, 0.8660254037844387076, 1.000000000000000000, 0.8660254037844387076, 1.000000000000000000, 0.8660254037844387076, 1.000000000000000000, 0.8660254037844387076, 1.000000000000000000, 0.8660254037844387076, 1.000000000000000000, 0.8660254037844387076, 1.000000000000000000, 0.8660254037844387076, 1.000000000000000000, 0.8660254037844387076, 1.000000000000000000, 0.8660254037844387076, 1.000000000000000000, 0.8660254037844387076, 1.000000000000000000, 0.8660254037844387076, 1.000000000000000000, 0.8660254037844387076, 1.000000000000000000, 0.8660254037844387076, 1.000000000000000000, 0.8660254037844387076, 1.000000000000000000, 0.8660254037844387076, 1.000000000000000000, 0.8660254037844387076, 1.000000000000000000, 0.8660254037844387076, 1.000000000000000000, 0.8660254037844387076, 1.000000000000000000, 0.8660254037844387076, 1.000000000000000000, 0.8660254037844387076, 1.000000000000000000, 0.8660254037844387076, 1.000000000000000000, 0.8660254037844387076, 1.000000000000000000, 0.8660254037844387076, 1.000000000000000000, 0.8660254037844387076, 1.000000000000000000, 0.8660254037844387076, 1.000000000000000000, 0.8660254037844387076, 1.000000000000000000, 0.8660254037844387076, 1.000000000000000000, 0.8660254037844387076, 1.000000000000000000, 0.8660254037844387076, 1.000000000000000000, 0.8660254037844387076, 1.000000000000000000, 0.8660254037844387076, 1.000000000000000000, 0.8660254037844387076, 1.000000000000000000, 0.8660254037844387076, 1.000000000000000000, 0.8660254037844387076, 1.000000000000000000, 0.8660254037844387076, 1.000000000000000000, 0.8660254037844387076, 1.000000000000000000, 0.8660254037844387076, 1.000000000000000000, 0.8660254037844387076, 1.000000000000000000, 0.8660254037844387076, 1.000000000000000000, 0.8660254037844387076, 1.000000000000000000, 0.8660254037844387076, 1.000000000000000000, 0.8660254037844387076, 1.000000000000000000, 0.8660254037844387076, 1.000000000000000000, 0.8660254037844387076, 1.000000000000000000, 0.8660254037844387076, 1.000000000000000000, 0.8660254037844387076, 1.000000000000000000, 0.8660254037844387076, 1.000000000000000000, 0.8660254037844387076, 1.000000000000000000, 0.8660254037844387076, 1.000000000000000000, 0.8660254037844387076, 1.000000000000000000, 0.8660254037844387076, 1.000000000000000000, 0.8660254037844387076, 1.000000000000000000, 0.8660254037844387076, 1.000000000000000000, 0.8660254037844387076, 1.000000000000000000, 0.8660254037844387076, 1.000000000000000000, 0.8660254037844387076, 1.000000000000000000, 0.8660254037844387076, 1.000000000000000000, 0.8660254037844387076, 1.000000000000000000, 0.8660254037844387076, 1.000000000000000000, 0.8660254037844387076, 1.000000000000000000, 0.8660254037844387076, 1.000000000000000000, 0.8660254037844387076, 1.000000000000000000, 0.8660254037844387076, 1.000000000000000000, 0.8660254037844387076, 1.000000000000000000, 0.8660254037844387076, 1.000000000000000000, 0.8660254037844387076, 1.000000000000000000, 0.8660254037844387076, 1.000000000000000000, 0.8660254037844387076, 1.000000000000000000, 0.8660254037844387076, 1.000000000000000000, 0.9486992175567839913, 0.9366860366981510921 ) ) 
 REPRESENTATION_ITEM ( '' )  );
#86550=CARTESIAN_POINT ( 'NONE',  ( -1.224999999999995204, 3.000000000000002665, -1.387778780781445676E-14 ) ) ;
#86559=EDGE_CURVE ( 'NONE', #182627, #175466, #157437, .T. ) ;
#86635=CARTESIAN_POINT ( 'NONE',  ( -3.486133158594716510E-16, 2.687500000000001332, -1.225000000000008749 ) ) ;
#86639=CARTESIAN_POINT ( 'NONE',  ( 1.224999999999961009, -0.7916666659838317299, -0.7072540797572958171 ) ) ;
#86654=CARTESIAN_POINT ( 'NONE',  ( 1.224999999999989209, 1.604166666666679619, 0.7072540797572898219 ) ) ;
#86675=CARTESIAN_POINT ( 'NONE',  ( -0.6801582343750229853, -0.3697916663252601155, -1.178068619123890270 ) ) ;
#86715=CARTESIAN_POINT ( 'NONE',  ( -0.6801582343750282034, 0.8489583336747236197, -1.178068619123876282 ) ) ;
#86803=VERTEX_POINT ( 'NONE', #101183 ) ;
#86908=CARTESIAN_POINT ( 'NONE',  ( -0.3282377607281271592, 0.5111645503674250302, -1.225000000000009859 ) ) ;
#87006=VECTOR ( 'NONE', #71818, 1000.000000000000114 ) ;
#87011=CARTESIAN_POINT ( 'NONE',  ( -1.225000000000040057, 2.333333334016198801, 0.7072540797572637317 ) ) ;
#87070=CARTESIAN_POINT ( 'NONE',  ( -2.324088772396477673E-16, 1.562500000000000666, 1.224999999999980549 ) ) ;
#87123=ORIENTED_EDGE ( 'NONE', *, *, #74132, .T. ) ;
#87126=CARTESIAN_POINT ( 'NONE',  ( -0.4170821662629227156, 3.033599471985643170, 0.4170821662629036752 ) ) ;
#87194=EDGE_CURVE ( 'NONE', #40528, #171576, #116010, .T. ) ;
#87216=EDGE_CURVE ( 'NONE', #42660, #168515, #209885, .T. ) ;
#87223=CARTESIAN_POINT ( 'NONE',  ( -0.4465194593918104249, 3.080450244942127380, 0.4155024747329021939 ) ) ;
#87226=CARTESIAN_POINT ( 'NONE',  ( 1.360316468749964480, 2.046875000341397133, -4.857225732735059864E-14 ) ) ;
#87249=CARTESIAN_POINT ( 'NONE',  ( 1.224999999999995204, 1.125000000000000888, -2.949029909160572061E-14 ) ) ;
#87269=ORIENTED_EDGE ( 'NONE', *, *, #35714, .F. ) ;
#87277=EDGE_CURVE ( 'NONE', #35460, #23166, #93520, .T. ) ;
#87289=CARTESIAN_POINT ( 'NONE',  ( 0.3728825314828132509, 3.227879828479781388, 0.5317689764002214714 ) ) ;
#87313=AXIS2_PLACEMENT_3D ( 'NONE', #99549, #128934, #181840 ) ;
#87346=CARTESIAN_POINT ( 'NONE',  ( 0.6124999999999741762, 2.729166667349444797, -1.060881119635955327 ) ) ;
#87407=CARTESIAN_POINT ( 'NONE',  ( -0.6801582343750316451, 0.8802083336747270614, -1.178068619123876282 ) ) ;
#87431=VERTEX_POINT ( 'NONE', #41035 ) ;
#87552=CARTESIAN_POINT ( 'NONE',  ( -1.752700365193352367E-14, 0.07812500034142640104, -1.570758158831804474 ) ) ;
#87620=CARTESIAN_POINT ( 'NONE',  ( -1.225000000000012301, 2.770833333333349469, 0.7072540797572637317 ) ) ;
#87662=ORIENTED_EDGE ( 'NONE', *, *, #146265, .F. ) ;
#87665=CARTESIAN_POINT ( 'NONE',  ( 0.4205179064188996341, -7.601391327209604134E-15, -1.181179690068133503 ) ) ;
#87707=CARTESIAN_POINT ( 'NONE',  ( 1.224999999999963896, -0.5624999993172064006, -2.428612866367529932E-14 ) ) ;
#87742=CARTESIAN_POINT ( 'NONE',  ( 1.360316468749955821, -0.9531249996585916540, -5.204170427930421283E-14 ) ) ;
#87777=CARTESIAN_POINT ( 'NONE',  ( -0.6801582343750368631, 1.682291667008048552, 1.178068619123803451 ) ) ;
#87854=CARTESIAN_POINT ( 'NONE',  ( 0.3769810270647707684, 3.049942316455285685, -0.4288785890453113980 ) ) ;
#87914=CARTESIAN_POINT ( 'NONE',  ( -0.4000000000000361045, 3.964661556059730696, -0.9099571394229808430 ) ) ;
#88040=CARTESIAN_POINT ( 'NONE',  ( 0.4499999999999834133, 3.949999999999988187, -0.5000000000000299760 ) ) ;
#88063=ORIENTED_EDGE ( 'NONE', *, *, #1238, .F. ) ;
#88079=AXIS2_PLACEMENT_3D ( 'NONE', #135401, #22672, #18425 ) ;
#88086=CARTESIAN_POINT ( 'NONE',  ( 1.224999999999969225, 1.937500000682795820, -2.081668171172168513E-14 ) ) ;
#88102=LINE ( 'NONE', #133952, #87006 ) ;
#88142=VECTOR ( 'NONE', #35468, 1000.000000000000000 ) ;
#88199=CARTESIAN_POINT ( 'NONE',  ( -0.4041367621137837984, 3.038026290190025236, 0.4210133165200240501 ) ) ;
#88246=CARTESIAN_POINT ( 'NONE',  ( -0.3282377607281458110, 2.198664549684619551, -1.225000000000048717 ) ) ;
#88253=ADVANCED_FACE ( 'NONE', ( #191805 ), #124783, .T. ) ;
#88283=ADVANCED_FACE ( 'NONE', ( #143124 ), #19301, .T. ) ;
#88303=CARTESIAN_POINT ( 'NONE',  ( -1.360316468750028651, 1.692708333674761922, 0.7853790794158620470 ) ) ;
#88324=CARTESIAN_POINT ( 'NONE',  ( -2.353626204688216217E-14, 0.9375000000000365263, -1.414508159514579644 ) ) ;
#88340=CARTESIAN_POINT ( 'NONE',  ( 0.5445930744353514319, 3.250057683544645304, -0.4000000000000409339 ) ) ;
#88435=EDGE_LOOP ( 'NONE', ( #48802, #47276, #110361, #146559 ) ) ;
#88443=CARTESIAN_POINT ( 'NONE',  ( 0.3999999999999576672, 0.6284510210557148202, -1.086836331270426781 ) ) ;
#88449=VECTOR ( 'NONE', #147679, 1000.000000000000000 ) ;
#88486=VERTEX_POINT ( 'NONE', #32520 ) ;
#88598=CARTESIAN_POINT ( 'NONE',  ( -0.4465194593918104249, 3.080450244942127380, 0.4155024747329021939 ) ) ;
#88629=CARTESIAN_POINT ( 'NONE',  ( -0.6801582343750420812, -0.06770833299193229626, 1.178068619123801675 ) ) ;
#88639=EDGE_CURVE ( 'NONE', #53408, #122076, #180898, .T. ) ;
#88699=CARTESIAN_POINT ( 'NONE',  ( 1.224999999999979661, 1.624999999999987566, -3.989863994746656317E-14 ) ) ;
#88713=DIRECTION ( 'NONE',  ( -0.2460297208025352678, 6.661338147750954034E-16, 0.9692622846690294169 ) ) ;
#88784=CARTESIAN_POINT ( 'NONE',  ( 0.3282377607281127818, 1.886164550367421588, 1.224999999999948352 ) ) ;
#88791=CARTESIAN_POINT ( 'NONE',  ( -1.225000000000028066, -0.9583333326505286687, -0.7072540797572817173 ) ) ;
#88808=DIRECTION ( 'NONE',  ( 1.276756478318932585E-15, -1.000000000000000000, 1.665334536937738262E-16 ) ) ;
#88815=ADVANCED_FACE ( 'NONE', ( #119156 ), #102852, .T. ) ;
#88862=CARTESIAN_POINT ( 'NONE',  ( -1.360316468750062846, 1.619791667008073643, -0.7853790794159301036 ) ) ;
#88870=CARTESIAN_POINT ( 'NONE',  ( 1.224999999999995204, 2.875000000000002665, 0.000000000000000000 ) ) ;
#88874=CARTESIAN_POINT ( 'NONE',  ( 0.4170821662628897974, 3.033599471985628959, -0.4170821662629418114 ) ) ;
#88897=ORIENTED_EDGE ( 'NONE', *, *, #4984, .F. ) ;
#88956=EDGE_CURVE ( 'NONE', #107948, #75994, #6383, .T. ) ;
#89003=ORIENTED_EDGE ( 'NONE', *, *, #213886, .T. ) ;
#89071=AXIS2_PLACEMENT_3D ( 'NONE', #69060, #151419, #850 ) ;
#89076=ORIENTED_EDGE ( 'NONE', *, *, #72377, .F. ) ;
#89093=CARTESIAN_POINT ( 'NONE',  ( -9.514659125335341649E-15, 1.359375000341400463, -1.570758158831806250 ) ) ;
#89116=EDGE_CURVE ( 'NONE', #62493, #28948, #166783, .T. ) ;
#89172=CARTESIAN_POINT ( 'NONE',  ( 0.6124999999999828360, 0.6458333340161465097, 1.060881119635891157 ) ) ;
#89209=VECTOR ( 'NONE', #192857, 1000.000000000000000 ) ;
#89228=PLANE ( 'NONE',  #69666 ) ;
#89301=CARTESIAN_POINT ( 'NONE',  ( -0.4465194593918104249, 3.080450244942120719, -0.4155024747329819634 ) ) ;
#89379=CARTESIAN_POINT ( 'NONE',  ( -0.6801582343750282034, 0.4635416670080716450, 1.178068619123793015 ) ) ;
#89402=CARTESIAN_POINT ( 'NONE',  ( -4.557020949502716471E-14, 0.06250000000002432776, 1.414508159514535457 ) ) ;
#89413=EDGE_CURVE ( 'NONE', #201878, #75836, #47980, .T. ) ;
#89416=DIRECTION ( 'NONE',  ( 3.219646771412963434E-15, 1.665334536937739741E-16, 1.000000000000000000 ) ) ;
#89419=CARTESIAN_POINT ( 'NONE',  ( 0.2999999999999842792, 3.975028841772351829, 0.9637995837462106641 ) ) ;
#89445=EDGE_CURVE ( 'NONE', #181560, #60914, #167899, .T. ) ;
#89507=VERTEX_POINT ( 'NONE', #175328 ) ;
#89679=( BOUNDED_CURVE ( )  B_SPLINE_CURVE ( 2, ( #204894, #185460, #56547, #122708, #40304, #106411, #103159, #86908, #152976 ),
 .UNSPECIFIED., .F., .T. ) 
 B_SPLINE_CURVE_WITH_KNOTS ( ( 3, 2, 2, 2, 3 ),
 ( 0.5468749999999997780, 0.5520833333333333703, 0.5625000000000000000, 0.5729166666666666297, 0.5781250000000001110 ),
 .UNSPECIFIED. ) 
 CURVE ( )  GEOMETRIC_REPRESENTATION_ITEM ( )  RATIONAL_B_SPLINE_CURVE ( ( 0.9330127018922194093, 0.9330127018922165227, 1.000000000000000000, 0.8660254037844387076, 1.000000000000000000, 0.8660254037844387076, 1.000000000000000000, 0.9330127018922178550, 0.9330127018922192983 ) ) 
 REPRESENTATION_ITEM ( '' )  );
#89704=CARTESIAN_POINT ( 'NONE',  ( 0.6801582343749744686, 0.4739583336747441034, 1.178068619123803451 ) ) ;
#89774=EDGE_LOOP ( 'NONE', ( #36976, #128232, #213614, #119945 ) ) ;
#89779=CARTESIAN_POINT ( 'NONE',  ( 1.224999999999965006, 2.395833333333299286, -0.7072540797573076965 ) ) ;
#89794=DIRECTION ( 'NONE',  ( -0.9692622846690297500, 0.000000000000000000, 0.2460297208025335747 ) ) ;
#89866=CARTESIAN_POINT ( 'NONE',  ( 1.224999999999976996, -0.5833333326504948069, 0.7072540797572697269 ) ) ;
#89870=CARTESIAN_POINT ( 'NONE',  ( -0.3769810270648435990, 3.049942316455334090, 0.4288785890452350702 ) ) ;
#89919=ADVANCED_FACE ( 'NONE', ( #66843 ), #115690, .T. ) ;
#89931=CARTESIAN_POINT ( 'NONE',  ( 1.360316468749955598, 1.536458333674721288, -0.7853790794159342115 ) ) ;
#90038=EDGE_CURVE ( 'NONE', #65799, #13808, #103671, .T. ) ;
#90068=ORIENTED_EDGE ( 'NONE', *, *, #157243, .F. ) ;
#90133=CARTESIAN_POINT ( 'NONE',  ( -1.162044386198238837E-16, 1.437500000000019540, -1.225000000000020739 ) ) ;
#90158=CARTESIAN_POINT ( 'NONE',  ( 0.6801582343749970061, 2.505208333674749266, 1.178068619123801675 ) ) ;
#90211=CARTESIAN_POINT ( 'NONE',  ( -0.4214947629263258722, 3.038568440852373875, -0.4183962726259458642 ) ) ;
#90233=CARTESIAN_POINT ( 'NONE',  ( -0.6125000000000279110, 1.104166667349484765, 1.060881119635904923 ) ) ;
#90322=CARTESIAN_POINT ( 'NONE',  ( 1.224999999999974998, 0.6041666666666989371, 0.7072540797572456350 ) ) ;
#90444=CARTESIAN_POINT ( 'NONE',  ( -3.755786496842897795E-14, -0.01562499965858205574, 1.570758158831768281 ) ) ;
#90467=CARTESIAN_POINT ( 'NONE',  ( 1.224999999999997202, -0.1458333333333367010, 0.7072540797572898219 ) ) ;
#90484=DIRECTION ( 'NONE',  ( 1.000000000000000000, -7.771561172376097755E-16, -4.440892098500627148E-16 ) ) ;
#90617=LINE ( 'NONE', #189159, #130396 ) ;
#90672=VECTOR ( 'NONE', #42230, 1000.000000000000000 ) ;
#90765=CARTESIAN_POINT ( 'NONE',  ( 0.3999999999999663824, 2.999999999999995559, 0.3423093779009733773 ) ) ;
#90769=CARTESIAN_POINT ( 'NONE',  ( 1.360316468749968033, 1.015625000341371820, -4.163336342344337027E-14 ) ) ;
#90838=CARTESIAN_POINT ( 'NONE',  ( -0.6125000000000019318, 1.458333333333332371, -1.060881119635941339 ) ) ;
#90875=CARTESIAN_POINT ( 'NONE',  ( -1.360316468750026875, 2.671875000341383810, -2.602085213965210642E-14 ) ) ;
#90896=DIRECTION ( 'NONE',  ( 0.000000000000000000, 0.000000000000000000, -1.000000000000000000 ) ) ;
#90992=ORIENTED_EDGE ( 'NONE', *, *, #134087, .F. ) ;
#90997=CARTESIAN_POINT ( 'NONE',  ( -5.358255402162534516E-14, 1.328125000341440431, -1.570758158831820239 ) ) ;
#91006=CARTESIAN_POINT ( 'NONE',  ( 0.6124999999999793943, 2.833333333333354354, 1.060881119635899816 ) ) ;
#91029=ORIENTED_EDGE ( 'NONE', *, *, #67872, .F. ) ;
#91135=TOROIDAL_SURFACE ( 'NONE', #118839, 0.05000000000000000278, 0.05000000000000000278 ) ;
#91146=ADVANCED_FACE ( 'NONE', ( #120193 ), #168065, .T. ) ;
#91229=CARTESIAN_POINT ( 'NONE',  ( 1.360316468749987129, 1.796875000341410900, -3.295974604355933479E-14 ) ) ;
#91288=ORIENTED_EDGE ( 'NONE', *, *, #209517, .T. ) ;
#91311=CARTESIAN_POINT ( 'NONE',  ( -0.6125000000000383471, 0.7708333340161397373, -1.060881119635972647 ) ) ;
#91425=CARTESIAN_POINT ( 'NONE',  ( -1.225000000000056044, 1.291666667349482323, -0.7072540797573317883 ) ) ;
#91438=FACE_OUTER_BOUND ( 'NONE', #128554, .T. ) ;
#91447=CLOSED_SHELL ( 'NONE', ( #188068, #77352, #142307, #19046, #89919, #32794, #145814, #119715, #14252, #122793, #117118, #208300, #111109, #207292, #88815, #77664, #44092, #44544, #69369, #88253, #71022, #155335, #135470, #139719, #76054, #102969, #113293, #74424, #201053, #32526, #192557, #147018, #85728, #21731, #160611, #56177, #174383, #177442, #114977, #13122, #184840, #137460, #117749, #22092, #170995, #211724, #39492, #2681, #124225, #212685, #15144, #212331, #133053, #2572, #47747, #203384, #154771, #165444, #80056, #82320, #22541, #123645, #97037, #128250, #63624, #173885, #117453, #180058, #73015, #123995, #88283, #48153, #151834, #136948, #111821, #91146, #21534, #181414, #28766, #10022, #121506, #14684, #125472, #38814, #54280, #197402, #67772, #105264, #79392, #56627, #94082, #83107, #144876, #114460, #132984, #122158, #163826, #75093, #19817 ) ) ;
#91452=CARTESIAN_POINT ( 'NONE',  ( 0.3423093779010028537, 2.999999999999988898, 0.3423093779009768189 ) ) ;
#91508=EDGE_CURVE ( 'NONE', #31530, #213643, #195432, .T. ) ;
#91525=CARTESIAN_POINT ( 'NONE',  ( -1.360316468750018659, 0.6927083336747492659, 0.7853790794158961308 ) ) ;
#91546=CARTESIAN_POINT ( 'NONE',  ( 0.6124999999999671818, -0.8333333333332831883, -1.060881119635969094 ) ) ;
#91562=EDGE_CURVE ( 'NONE', #40528, #77834, #205753, .T. ) ;
#91651=ORIENTED_EDGE ( 'NONE', *, *, #29662, .F. ) ;
#91690=EDGE_LOOP ( 'NONE', ( #29574, #165754, #72708 ) ) ;
#91699=AXIS2_PLACEMENT_3D ( 'NONE', #143067, #28207, #130055 ) ;
#91743=DIRECTION ( 'NONE',  ( -1.000000000000000000, 7.771561172376097755E-16, 4.440892098500627148E-16 ) ) ;
#91756=CARTESIAN_POINT ( 'NONE',  ( 0.3282377607281200538, 0.1763354503153972130, -1.225000000000030953 ) ) ;
#91829=ORIENTED_EDGE ( 'NONE', *, *, #129837, .T. ) ;
#91842=CARTESIAN_POINT ( 'NONE',  ( -2.754243431018125239E-14, 0.2031250003414269978, 1.570758158831750295 ) ) ;
#91913=CARTESIAN_POINT ( 'NONE',  ( -4.356712336337761644E-14, 1.812499999999968470, 1.414508159514561436 ) ) ;
#91921=EDGE_CURVE ( 'NONE', #61933, #210405, #99352, .T. ) ;
#91973=CARTESIAN_POINT ( 'NONE',  ( -1.225000000000028066, 1.229166666666677843, -0.7072540797573078075 ) ) ;
#92053=CARTESIAN_POINT ( 'NONE',  ( -1.992711204631002198E-15, 2.999999999999989342, 1.224999999999989875 ) ) ;
#92067=CARTESIAN_POINT ( 'NONE',  ( -1.360316468750023544, 0.8906250003414064587, -2.602085213965210642E-14 ) ) ;
#92076=CARTESIAN_POINT ( 'NONE',  ( 1.224999999999957012, 2.854166666666677621, 0.7072540797572558491 ) ) ;
#92118=DIRECTION ( 'NONE',  ( 1.276756478318932585E-15, -1.000000000000000000, 1.665334536937738262E-16 ) ) ;
#92121=VECTOR ( 'NONE', #154313, 1000.000000000000114 ) ;
#92147=CARTESIAN_POINT ( 'NONE',  ( 1.224999999999984768, 0.1875000006827803878, -5.377642775528101993E-14 ) ) ;
#92176=CARTESIAN_POINT ( 'NONE',  ( -0.4500000000000163869, 3.950000000000009059, -1.561251128379126385E-14 ) ) ;
#92185=DIRECTION ( 'NONE',  ( -1.276756478318932585E-15, 1.000000000000000000, -1.665334536937738262E-16 ) ) ;
#92222=ORIENTED_EDGE ( 'NONE', *, *, #41993, .F. ) ;
#92282=ORIENTED_EDGE ( 'NONE', *, *, #155989, .T. ) ;
#92309=CARTESIAN_POINT ( 'NONE',  ( 1.360316468749964480, 2.046875000341397133, -4.857225732735059864E-14 ) ) ;
#92366=ORIENTED_EDGE ( 'NONE', *, *, #116999, .T. ) ;
#92378=EDGE_CURVE ( 'NONE', #72572, #50089, #156646, .T. ) ;
#92388=CARTESIAN_POINT ( 'NONE',  ( -1.552391752028397856E-14, 0.1250000006828045906, 1.414508159514549446 ) ) ;
#92474=ORIENTED_EDGE ( 'NONE', *, *, #38562, .F. ) ;
#92481=ORIENTED_EDGE ( 'NONE', *, *, #168793, .F. ) ;
#92598=CARTESIAN_POINT ( 'NONE',  ( -4.957638175832625493E-14, 0.8593750003414141192, -1.570758158831808249 ) ) ;
#92619=CARTESIAN_POINT ( 'NONE',  ( -1.225000000000007416, -0.5000000000000004441, -1.734723475976807094E-15 ) ) ;
#92773=EDGE_CURVE ( 'NONE', #181560, #203057, #98634, .T. ) ;
#92819=CARTESIAN_POINT ( 'NONE',  ( -1.326716514427061987E-15, 2.999999999999988454, -1.225000000000003864 ) ) ;
#92905=CARTESIAN_POINT ( 'NONE',  ( -1.225000000000056044, 2.541666667349471886, -0.7072540797572937077 ) ) ;
#92930=DIRECTION ( 'NONE',  ( 1.000000000000000000, -7.771561172376097755E-16, -4.440892098500627148E-16 ) ) ;
#93009=CARTESIAN_POINT ( 'NONE',  ( 0.6801582343749970061, 2.505208333674749266, 1.178068619123801675 ) ) ;
#93036=CARTESIAN_POINT ( 'NONE',  ( -1.225000000000019407, 1.250000000000028866, -1.734723475976807094E-14 ) ) ;
#93045=CARTESIAN_POINT ( 'NONE',  ( 0.4000000000000045186, 2.999999999999988898, 0.4999999999999674705 ) ) ;
#93116=DIRECTION ( 'NONE',  ( 8.673617379884087537E-15, -1.000000000000000000, 0.000000000000000000 ) ) ;
#93132=CARTESIAN_POINT ( 'NONE',  ( -0.6801582343750299797, 0.9322916670080338974, 1.178068619123803451 ) ) ;
#93153=CARTESIAN_POINT ( 'NONE',  ( -0.6801582343750091075, 2.848958333674732391, -1.178068619123848526 ) ) ;
#93165=ORIENTED_EDGE ( 'NONE', *, *, #74123, .T. ) ;
#93166=CARTESIAN_POINT ( 'NONE',  ( -1.734723475976807094E-15, 2.999999999999988898, -6.938893903907228378E-15 ) ) ;
#93168=B_SPLINE_CURVE_WITH_KNOTS ( 'NONE', 3,
 ( #31098, #148038, #192495, #210881, #110268, #13747, #179474, #96105, #161085, #196775 ),
 .UNSPECIFIED., .F., .F.,
 ( 4, 2, 2, 2, 4 ),
 ( 0.000000000000000000, 0.0006317681591994424740, 0.001263536318398884731, 0.001895304477598327422, 0.002527072636797769896 ),
 .UNSPECIFIED. ) ;
#93194=CARTESIAN_POINT ( 'NONE',  ( 0.3275200278799066389, 3.116672424413486908, 0.4674645318177238495 ) ) ;
#93211=CARTESIAN_POINT ( 'NONE',  ( 0.3282377607281107834, 0.1361645503674392965, 1.224999999999955014 ) ) ;
#93270=CARTESIAN_POINT ( 'NONE',  ( 0.3282377607281070087, 0.8236645496846426440, 1.224999999999953904 ) ) ;
#93366=CARTESIAN_POINT ( 'NONE',  ( -4.957638175832625493E-14, 1.734375000341442208, 1.570758158831756068 ) ) ;
#93376=CARTESIAN_POINT ( 'NONE',  ( 1.224999999999974998, 2.416666667349527842, 0.7072540797572656190 ) ) ;
#93402=CARTESIAN_POINT ( 'NONE',  ( -1.360316468750026875, 2.140625000341400685, -4.857225732735059864E-14 ) ) ;
#93447=CARTESIAN_POINT ( 'NONE',  ( -1.752700365193352367E-14, 0.7500000006828075882, -1.414508159514589636 ) ) ;
#93520=( BOUNDED_CURVE ( )  B_SPLINE_CURVE ( 3, ( #193649, #155839, #190446, #25815 ),
 .UNSPECIFIED., .F., .T. ) 
 B_SPLINE_CURVE_WITH_KNOTS ( ( 4, 4 ),
 ( 4.148111545443665449, 4.712388980384681680 ),
 .UNSPECIFIED. ) 
 CURVE ( )  GEOMETRIC_REPRESENTATION_ITEM ( )  RATIONAL_B_SPLINE_CURVE ( ( 1.000000000000000000, 0.9736414627471525751, 0.9736414627471525751, 1.000000000000000000 ) ) 
 REPRESENTATION_ITEM ( '' )  );
#93572=CARTESIAN_POINT ( 'NONE',  ( 1.224999999999953015, 1.854166666666720698, 0.7072540797572656190 ) ) ;
#93609=CARTESIAN_POINT ( 'NONE',  ( -0.3282377607281345422, 0.1138354509981740759, 1.224999999999971667 ) ) ;
#93657=CARTESIAN_POINT ( 'NONE',  ( -2.353626204688216217E-14, 0.9843750003414547534, 1.570758158831764062 ) ) ;
#93675=DIRECTION ( 'NONE',  ( 1.276756478318932585E-15, -1.000000000000000000, 1.665334536937738262E-16 ) ) ;
#93680=CARTESIAN_POINT ( 'NONE',  ( 1.360316468749964480, 2.796875000341370043, -3.989863994746656317E-14 ) ) ;
#93702=CARTESIAN_POINT ( 'NONE',  ( -0.3878679656440754964, 3.999999999999934275, 1.007084189318353973 ) ) ;
#93798=DIRECTION ( 'NONE',  ( -3.330669073875479482E-16, 3.330669073875479482E-16, 1.000000000000000000 ) ) ;
#93869=CARTESIAN_POINT ( 'NONE',  ( 0.4999999999999779066, 3.949999999999988187, 0.3999999999999576672 ) ) ;
#93936=VECTOR ( 'NONE', #198731, 1000.000000000000000 ) ;
#93973=CARTESIAN_POINT ( 'NONE',  ( -4.156403723172807449E-14, -1.046874999658554906, 1.570758158831744078 ) ) ;
#94027=AXIS2_PLACEMENT_3D ( 'NONE', #115609, #14834, #16958 ) ;
#94077=CARTESIAN_POINT ( 'NONE',  ( 1.360316468749975805, 2.317708333674724841, -0.7853790794158961308 ) ) ;
#94082=ADVANCED_FACE ( 'NONE', ( #165702 ), #210170, .T. ) ;
#94105=CARTESIAN_POINT ( 'NONE',  ( -0.3282377607281460885, 1.198664549684620662, -1.225000000000036726 ) ) ;
#94107=ORIENTED_EDGE ( 'NONE', *, *, #198698, .T. ) ;
#94200=CARTESIAN_POINT ( 'NONE',  ( -0.6801582343750282034, 0.8489583336747236197, -1.178068619123876282 ) ) ;
#94219=ORIENTED_EDGE ( 'NONE', *, *, #37214, .F. ) ;
#94221=CARTESIAN_POINT ( 'NONE',  ( -2.353626204688216217E-14, 2.828125000341407347, -1.570758158831798257 ) ) ;
#94335=CARTESIAN_POINT ( 'NONE',  ( 0.6124999999999932720, 0.9166666666666906105, -1.060881119635955327 ) ) ;
#94411=LINE ( 'NONE', #160450, #2432 ) ;
#94433=CARTESIAN_POINT ( 'NONE',  ( 0.6801582343749900117, 1.338541667008072533, -1.178068619123872729 ) ) ;
#94531=FACE_OUTER_BOUND ( 'NONE', #213135, .T. ) ;
#94539=AXIS2_PLACEMENT_3D ( 'NONE', #194301, #174880, #26460 ) ;
#94540=B_SPLINE_CURVE_WITH_KNOTS ( 'NONE', 3,
 ( #88874, #11854, #179715, #62740, #129975, #60614, #127856 ),
 .UNSPECIFIED., .F., .F.,
 ( 4, 3, 4 ),
 ( 0.000000000000000000, 4.270488675891472745E-05, 4.488495215206831637E-05 ),
 .UNSPECIFIED. ) ;
#94595=EDGE_CURVE ( 'NONE', #160775, #55298, #77286, .T. ) ;
#94633=CARTESIAN_POINT ( 'NONE',  ( -0.5000000000000264233, 3.999999999999976019, -0.4500000000000458633 ) ) ;
#94641=CARTESIAN_POINT ( 'NONE',  ( 8.134310703387671364E-16, 2.000000000682804924, -1.225000000000021849 ) ) ;
#94648=CARTESIAN_POINT ( 'NONE',  ( 1.981037863234367924, 3.482875600935791294, -0.4617754461039013658 ) ) ;
#94726=CARTESIAN_POINT ( 'NONE',  ( 0.6801582343749900117, -0.4114583329919083154, -1.178068619123855409 ) ) ;
#95006=DIRECTION ( 'NONE',  ( -2.126226658603517140E-31, 1.665334536937738015E-16, 1.000000000000000000 ) ) ;
#95033=CARTESIAN_POINT ( 'NONE',  ( -1.352083138863443345E-14, -0.9218749996585863249, -1.570758158831792262 ) ) ;
#95140=ORIENTED_EDGE ( 'NONE', *, *, #11493, .F. ) ;
#95206=ORIENTED_EDGE ( 'NONE', *, *, #50038, .T. ) ;
#95216=CARTESIAN_POINT ( 'NONE',  ( 0.000000000000000000, 0.000000000000000000, 0.000000000000000000 ) ) ;
#95256=CARTESIAN_POINT ( 'NONE',  ( -0.3405876332337993695, 3.079852035184914794, -0.4461735512528283154 ) ) ;
#95267=CARTESIAN_POINT ( 'NONE',  ( -1.360316468750008667, 0.1197916670080665519, -0.7853790794159001276 ) ) ;
#95302=VERTEX_POINT ( 'NONE', #193729 ) ;
#95405=CARTESIAN_POINT ( 'NONE',  ( 1.224999999999947020, 0.8958333333333403647, -0.7072540797573197979 ) ) ;
#95419=DIRECTION ( 'NONE',  ( 1.084202172485506406E-15, -0.5005768354468324022, -0.8656921114426507913 ) ) ;
#95427=AXIS2_PLACEMENT_3D ( 'NONE', #192874, #45598, #159325 ) ;
#95490=ORIENTED_EDGE ( 'NONE', *, *, #110826, .F. ) ;
#95504=DIRECTION ( 'NONE',  ( 0.000000000000000000, -0.5005768354468324022, 0.8656921114426507913 ) ) ;
#95506=CARTESIAN_POINT ( 'NONE',  ( 1.360316468749945606, 0.06770833367471427999, -0.7853790794159161148 ) ) ;
#95618=DIRECTION ( 'NONE',  ( -0.8583236685137333177, -0.5131086435338296781, 0.000000000000000000 ) ) ;
#95699=EDGE_CURVE ( 'NONE', #179471, #203057, #122297, .T. ) ;
#95710=VECTOR ( 'NONE', #122115, 1000.000000000000000 ) ;
#95794=CARTESIAN_POINT ( 'NONE',  ( -0.6801582343750403048, -0.5364583329919083710, 1.178068619123807004 ) ) ;
#95830=AXIS2_PLACEMENT_3D ( 'NONE', #5341, #3221, #184123 ) ;
#95838=FACE_OUTER_BOUND ( 'NONE', #155577, .T. ) ;
#96005=DIRECTION ( 'NONE',  ( 1.276756478318932585E-15, -1.000000000000000000, 1.665334536937738262E-16 ) ) ;
#96039=VECTOR ( 'NONE', #187095, 1000.000000000000000 ) ;
#96049=CARTESIAN_POINT ( 'NONE',  ( -1.360316468750048635, 2.651041667008094738, -0.7853790794159161148 ) ) ;
#96103=CARTESIAN_POINT ( 'NONE',  ( -0.6801582343750161019, -0.9010416663252431846, -1.178068619123869398 ) ) ;
#96105=CARTESIAN_POINT ( 'NONE',  ( 0.09478498853002972901, -7.830875036364503024E-15, 1.351550957883141058 ) ) ;
#96146=DIRECTION ( 'NONE',  ( 1.276756478318932585E-15, -1.000000000000000000, 1.665334536937738262E-16 ) ) ;
#96205=CARTESIAN_POINT ( 'NONE',  ( -6.960724307482170605E-14, 1.484375000341481288, 1.570758158831758289 ) ) ;
#96253=CARTESIAN_POINT ( 'NONE',  ( 1.893304937267579202, 3.295344712542831900, 0.4038802767148412798 ) ) ;
#96327=ORIENTED_EDGE ( 'NONE', *, *, #159688, .F. ) ;
#96331=CARTESIAN_POINT ( 'NONE',  ( 1.360316468749983576, 0.5156250003414062366, -5.204170427930421283E-15 ) ) ;
#96375=CIRCLE ( 'NONE', #165609, 0.1000000000000000472 ) ;
#96418=CIRCLE ( 'NONE', #23857, 0.1000000000000000472 ) ;
#96489=AXIS2_PLACEMENT_3D ( 'NONE', #163547, #214363, #116977 ) ;
#96504=DIRECTION ( 'NONE',  ( -0.5005768354468334014, 0.8656921114426502362, 1.887379141862767696E-15 ) ) ;
#96524=DIRECTION ( 'NONE',  ( -1.000000000000000000, -1.276756478318932585E-15, -3.330669073875474552E-16 ) ) ;
#96532=CIRCLE ( 'NONE', #65393, 0.05000000000000002359 ) ;
#96545=CARTESIAN_POINT ( 'NONE',  ( -2.440293211016301606E-15, 1.312499999999991118, 1.224999999999973888 ) ) ;
#96567=CARTESIAN_POINT ( 'NONE',  ( -1.360316468750032870, 0.9427083336747503761, 0.7853790794158641564 ) ) ;
#96673=DIRECTION ( 'NONE',  ( 0.000000000000000000, 0.5005768354468290715, -0.8656921114426525676 ) ) ;
#96689=CARTESIAN_POINT ( 'NONE',  ( 0.5445930744353514319, 3.250057683544645304, -0.4000000000000409339 ) ) ;
#96704=EDGE_CURVE ( 'NONE', #38441, #176198, #70809, .T. ) ;
#96707=EDGE_LOOP ( 'NONE', ( #175127, #156407, #25001, #207125, #183097, #167991 ) ) ;
#96776=DIRECTION ( 'NONE',  ( 3.330669073875478989E-16, -3.540251991789410786E-16, -1.000000000000000000 ) ) ;
#96864=CARTESIAN_POINT ( 'NONE',  ( 1.360316468749973140, -0.2031249996586187434, -5.030698080332740574E-14 ) ) ;
#96924=CARTESIAN_POINT ( 'NONE',  ( -0.3282377607281344867, 0.5513354503153581332, 1.224999999999968114 ) ) ;
#97037=ADVANCED_FACE ( 'NONE', ( #123953 ), #201628, .F. ) ;
#97071=DIRECTION ( 'NONE',  ( 0.000000000000000000, 3.330669073875420317E-16, 1.000000000000000000 ) ) ;
#97118=DIRECTION ( 'NONE',  ( 3.330669073875478989E-16, -3.540251991789410786E-16, -1.000000000000000000 ) ) ;
#97168=CARTESIAN_POINT ( 'NONE',  ( -3.355169270512988773E-14, 2.500000000682816026, -1.414508159514599628 ) ) ;
#97181=CARTESIAN_POINT ( 'NONE',  ( 0.6124999999999707345, 2.145833334016141070, 1.060881119635899816 ) ) ;
#97189=CARTESIAN_POINT ( 'NONE',  ( -2.440293211016301606E-15, 1.187499999999993117, -1.225000000000025624 ) ) ;
#97264=CARTESIAN_POINT ( 'NONE',  ( -0.6801582343750420812, 1.880208333674727950, -1.178068619123883165 ) ) ;
#97323=AXIS2_PLACEMENT_3D ( 'NONE', #13323, #143369, #115163 ) ;
#97394=CARTESIAN_POINT ( 'NONE',  ( 1.360316468749957597, -0.5052083329919204724, 0.7853790794159082322 ) ) ;
#97509=CARTESIAN_POINT ( 'NONE',  ( -1.907862554904992569, 3.236716050607336914, -0.4606469147255816132 ) ) ;
#97531=CARTESIAN_POINT ( 'NONE',  ( -1.886017674307096437, 3.298060805577381238, 0.4014564593430944850 ) ) ;
#97565=EDGE_LOOP ( 'NONE', ( #61099, #122273, #40939, #39123 ) ) ;
#97623=CARTESIAN_POINT ( 'NONE',  ( -5.558564015327489343E-14, 0.6093750003414449834, -1.570758158831798257 ) ) ;
#97647=ORIENTED_EDGE ( 'NONE', *, *, #71255, .T. ) ;
#97662=CARTESIAN_POINT ( 'NONE',  ( 1.360316468750000896, 2.515625000341401130, -3.469446951953614189E-15 ) ) ;
#97681=ORIENTED_EDGE ( 'NONE', *, *, #114638, .F. ) ;
#97766=ORIENTED_EDGE ( 'NONE', *, *, #127956, .T. ) ;
#97776=CARTESIAN_POINT ( 'NONE',  ( 0.3999999999999567235, 3.251480759208385862, 0.4649507210924435086 ) ) ;
#97802=CARTESIAN_POINT ( 'NONE',  ( 0.4999999999999900080, 3.950000000000009059, -0.5000000000000160982 ) ) ;
#97816=ORIENTED_EDGE ( 'NONE', *, *, #127956, .F. ) ;
#97835=CARTESIAN_POINT ( 'NONE',  ( -0.4000000000000357714, 3.949999999999981526, -0.5000000000000299760 ) ) ;
#97854=FACE_OUTER_BOUND ( 'NONE', #99412, .T. ) ;
#97922=CARTESIAN_POINT ( 'NONE',  ( 1.360316468750003782, -0.1822916663252708847, -0.7853790794158961308 ) ) ;
#97983=CARTESIAN_POINT ( 'NONE',  ( -1.225000000000028066, 0.5000000000000143219, -5.030698080332740574E-14 ) ) ;
#98070=DIRECTION ( 'NONE',  ( 0.000000000000000000, 0.000000000000000000, 1.000000000000000000 ) ) ;
#98316=CARTESIAN_POINT ( 'NONE',  ( -2.754243431018125239E-14, 1.984375000341467299, 1.570758158831788265 ) ) ;
#98321=VERTEX_POINT ( 'NONE', #123704 ) ;
#98364=CARTESIAN_POINT ( 'NONE',  ( 1.910130646976109681, 3.278792710263288779, 0.4195261609910589939 ) ) ;
#98424=CARTESIAN_POINT ( 'NONE',  ( -0.3423093779010132898, 2.999999999999995559, 0.3423093779010045745 ) ) ;
#98444=CARTESIAN_POINT ( 'NONE',  ( -1.360316468750034868, -0.3385416663252556191, 0.7853790794158601596 ) ) ;
#98465=CARTESIAN_POINT ( 'NONE',  ( 0.6801582343749987825, 1.557291667008103841, -1.178068619123876282 ) ) ;
#98605=CARTESIAN_POINT ( 'NONE',  ( 1.874158809982179319, 3.299964346911585356, -0.3999999999999993006 ) ) ;
#98634=CIRCLE ( 'NONE', #91699, 0.05000000000000009298 ) ;
#98635=CARTESIAN_POINT ( 'NONE',  ( 0.4347878448724571410, 3.060161718936325492, 0.4204403343208824584 ) ) ;
#98654=FACE_OUTER_BOUND ( 'NONE', #158264, .T. ) ;
#98655=CARTESIAN_POINT ( 'NONE',  ( -1.326716514427061987E-15, 2.999999999999988454, -1.225000000000003864 ) ) ;
#98656=EDGE_LOOP ( 'NONE', ( #112893, #99997, #137562, #211475, #175052, #207137, #44422, #168351, #4127, #147203, #164969, #20315, #93165, #171725, #13151, #155851, #1654, #128728, #162147, #225, #11181, #156327, #129307, #139585, #69938, #182745, #41904, #40763 ) ) ;
#98673=CARTESIAN_POINT ( 'NONE',  ( -1.360316468750014884, 0.1927083336747308917, 0.7853790794158901356 ) ) ;
#98713=CARTESIAN_POINT ( 'NONE',  ( -1.360316468750040642, 1.911458333674787236, 0.7853790794158660438 ) ) ;
#98793=CARTESIAN_POINT ( 'NONE',  ( 0.4499999999999729772, 3.999999999999940936, -0.5000000000000368594 ) ) ;
#98906=CARTESIAN_POINT ( 'NONE',  ( 0.4170821662628915183, 3.033599471985643170, 0.4170821662628724225 ) ) ;
#98967=CARTESIAN_POINT ( 'NONE',  ( -0.4000000000000281664, 3.963633530850221742, 0.9046180958550756879 ) ) ;
#98974=CARTESIAN_POINT ( 'NONE',  ( -1.360316468750000674, -0.3489583329919356824, -0.7853790794158941324 ) ) ;
#99096=VERTEX_POINT ( 'NONE', #32499 ) ;
#99103=ORIENTED_EDGE ( 'NONE', *, *, #144905, .F. ) ;
#99109=DIRECTION ( 'NONE',  ( 9.436895709313856232E-16, -0.8656921114426507913, -0.5005768354468325132 ) ) ;
#99141=CARTESIAN_POINT ( 'NONE',  ( -2.449742653233059286, 3.300000000000011369, 0.3999999999999750422 ) ) ;
#99288=CARTESIAN_POINT ( 'NONE',  ( 0.3405876332337480772, 3.079852035184937886, 0.4461735512527765790 ) ) ;
#99352=LINE ( 'NONE', #67867, #171129 ) ;
#99353=VECTOR ( 'NONE', #198421, 1000.000000000000000 ) ;
#99386=CARTESIAN_POINT ( 'NONE',  ( 1.360316468749978469, 1.046875000341403128, -2.602085213965210642E-14 ) ) ;
#99412=EDGE_LOOP ( 'NONE', ( #21405, #193829, #177779, #87662 ) ) ;
#99512=CARTESIAN_POINT ( 'NONE',  ( 1.360316468749969587, -0.7343749996585879902, -3.642919299551294898E-14 ) ) ;
#99533=CARTESIAN_POINT ( 'NONE',  ( 1.360316468749963592, 1.286458333674704191, -0.7853790794158961308 ) ) ;
#99540=VECTOR ( 'NONE', #125461, 1000.000000000000000 ) ;
#99549=CARTESIAN_POINT ( 'NONE',  ( -3.122502256758252770E-14, 3.499999999999961364, -3.816391647148975608E-14 ) ) ;
#99561=CARTESIAN_POINT ( 'NONE',  ( 1.898923903056394913, 3.739065552179445806, -0.4000000000000273337 ) ) ;
#99563=B_SPLINE_CURVE_WITH_KNOTS ( 'NONE', 3,
 ( #214194, #29103, #130928, #212087, #180673, #143962, #112544, #196922, #49608, #31240, #98364, #113615, #78897, #209957, #145020, #178554, #96253, #197980, #48560, #146074, #45365, #63723 ),
 .UNSPECIFIED., .F., .F.,
 ( 4, 3, 3, 3, 3, 3, 3, 4 ),
 ( -1.454680003659494146E-06, 0.000000000000000000, 2.747234201904476952E-05, 5.316625080980220638E-05, 7.164957654724449416E-05, 8.369272870876657113E-05, 9.574357740276803535E-05, 0.0001078040709964530740 ),
 .UNSPECIFIED. ) ;
#99612=VERTEX_POINT ( 'NONE', #176367 ) ;
#99634=DIRECTION ( 'NONE',  ( 0.000000000000000000, 0.000000000000000000, 1.000000000000000000 ) ) ;
#99715=CARTESIAN_POINT ( 'NONE',  ( -1.214306433183764966E-14, 3.299999999999969624, -3.122502256758252770E-14 ) ) ;
#99719=CARTESIAN_POINT ( 'NONE',  ( 4.067155351693835485E-15, 1.250000000682825130, -1.225000000000013411 ) ) ;
#99773=CARTESIAN_POINT ( 'NONE',  ( -1.360316468750056851, 1.369791667008064318, -0.7853790794159101196 ) ) ;
#99799=DIRECTION ( 'NONE',  ( 1.000000000000000000, 0.000000000000000000, 0.000000000000000000 ) ) ;
#99892=CIRCLE ( 'NONE', #6466, 0.09999999999999992228 ) ;
#99949=CARTESIAN_POINT ( 'NONE',  ( -0.4000000000000304423, 3.999999999999981348, -0.8338124244295984644 ) ) ;
#99997=ORIENTED_EDGE ( 'NONE', *, *, #86051, .T. ) ;
#100029=( BOUNDED_CURVE ( )  B_SPLINE_CURVE ( 3, ( #151861, #37018, #87914, #203769 ),
 .UNSPECIFIED., .F., .T. ) 
 B_SPLINE_CURVE_WITH_KNOTS ( ( 4, 4 ),
 ( 3.141592653589619921, 4.712388980384721648 ),
 .UNSPECIFIED. ) 
 CURVE ( )  GEOMETRIC_REPRESENTATION_ITEM ( )  RATIONAL_B_SPLINE_CURVE ( ( 1.000000000000000000, 0.8047378541243166428, 0.8047378541243166428, 1.000000000000000000 ) ) 
 REPRESENTATION_ITEM ( '' )  );
#100031=CARTESIAN_POINT ( 'NONE',  ( -1.360316468750040642, 1.911458333674787236, 0.7853790794158660438 ) ) ;
#100154=AXIS2_PLACEMENT_3D ( 'NONE', #193372, #45017, #175014 ) ;
#100275=CARTESIAN_POINT ( 'NONE',  ( 0.6801582343750022241, 2.838541667008094738, -1.178068619123834759 ) ) ;
#100279=FACE_OUTER_BOUND ( 'NONE', #83101, .T. ) ;
#100297=CARTESIAN_POINT ( 'NONE',  ( 0.6124999999999914957, 1.333333333333339255, 1.060881119635932679 ) ) ;
#100348=CARTESIAN_POINT ( 'NONE',  ( 0.6124999999999932720, 2.229166667349451014, -1.060881119635948444 ) ) ;
#100401=EDGE_CURVE ( 'NONE', #198538, #95302, #90617, .T. ) ;
#100441=CARTESIAN_POINT ( 'NONE',  ( 1.360316468749980023, 0.7968750003414099004, -3.122502256758252770E-14 ) ) ;
#100473=CYLINDRICAL_SURFACE ( 'NONE', #105630, 0.04999999999999991257 ) ;
#100518=EDGE_CURVE ( 'NONE', #39288, #87431, #55962, .T. ) ;
#100560=CARTESIAN_POINT ( 'NONE',  ( -1.510657702057710340E-15, 1.375000000682792267, 1.224999999999963229 ) ) ;
#100569=CARTESIAN_POINT ( 'NONE',  ( -4.156403723172807449E-14, -1.046874999658554906, 1.570758158831744078 ) ) ;
#100591=CARTESIAN_POINT ( 'NONE',  ( 1.360316468749957597, 1.265625000341379147, -5.030698080332740574E-14 ) ) ;
#100709=ORIENTED_EDGE ( 'NONE', *, *, #50038, .F. ) ;
#100786=CARTESIAN_POINT ( 'NONE',  ( -1.360316468750002894, -0.3072916663252554526, 0.7853790794158901356 ) ) ;
#100826=CARTESIAN_POINT ( 'NONE',  ( -3.755786496842899057E-14, 1.703125000341434214, 1.570758158831776052 ) ) ;
#100850=CARTESIAN_POINT ( 'NONE',  ( -1.225000000000030065, 0.3333333340161496738, 0.7072540797572656190 ) ) ;
#100893=CARTESIAN_POINT ( 'NONE',  ( 1.826099658462914777, 3.981846818258164777, 0.3999999999999847566 ) ) ;
#100912=EDGE_CURVE ( 'NONE', #204354, #141010, #189216, .T. ) ;
#101117=CARTESIAN_POINT ( 'NONE',  ( -1.225000000000036060, 2.291666667349470998, -0.7072540797573277915 ) ) ;
#101149=CARTESIAN_POINT ( 'NONE',  ( -6.972266317189433020E-16, 1.750000000682810475, -1.225000000000013634 ) ) ;
#101183=CARTESIAN_POINT ( 'NONE',  ( -1.045839947578414805E-15, 1.812499999999992673, 1.224999999999988987 ) ) ;
#101215=CARTESIAN_POINT ( 'NONE',  ( -1.292658234375052784, 2.851562500512133447, -3.816391647148975608E-14 ) ) ;
#101273=( BOUNDED_CURVE ( )  B_SPLINE_CURVE ( 2, ( #68054, #32396, #31337, #116900, #35577, #81142, #166663, #162406, #113716 ),
 .UNSPECIFIED., .F., .T. ) 
 B_SPLINE_CURVE_WITH_KNOTS ( ( 3, 2, 2, 2, 3 ),
 ( 0.2031250000000001388, 0.2083333333333333426, 0.2187500000000000000, 0.2291666666666666574, 0.2343749999999997780 ),
 .UNSPECIFIED. ) 
 CURVE ( )  GEOMETRIC_REPRESENTATION_ITEM ( )  RATIONAL_B_SPLINE_CURVE ( ( 0.9330127018922194093, 0.9330127018922211857, 1.000000000000000000, 0.8660254037844387076, 1.000000000000000000, 0.8660254037844387076, 1.000000000000000000, 0.9330127018922221849, 0.9330127018922194093 ) ) 
 REPRESENTATION_ITEM ( '' )  );
#101325=SHAPE_REPRESENTATION_RELATIONSHIP ( 'NONE' , 'NONE' ,  #121983, #156107 ) ;
#101335=CARTESIAN_POINT ( 'NONE',  ( -1.360316468750011332, 2.421875000341397577, -1.387778780781445676E-14 ) ) ;
#101359=CARTESIAN_POINT ( 'NONE',  ( 1.224999999999994982, 1.145833333333333481, -0.7072540797572898219 ) ) ;
#101375=VECTOR ( 'NONE', #90484, 1000.000000000000000 ) ;
#101381=VERTEX_POINT ( 'NONE', #79313 ) ;
#101401=CARTESIAN_POINT ( 'NONE',  ( 0.4032277238576092993, 3.019957635004406171, 0.4115402804777972268 ) ) ;
#101495=EDGE_LOOP ( 'NONE', ( #48914, #206194, #111320, #39595, #195132, #124836 ) ) ;
#101510=CARTESIAN_POINT ( 'NONE',  ( -0.6801582343750282034, 0.4635416670080716450, 1.178068619123793015 ) ) ;
#101520=AXIS2_PLACEMENT_3D ( 'NONE', #40349, #174628, #39264 ) ;
#101568=ORIENTED_EDGE ( 'NONE', *, *, #112518, .F. ) ;
#101660=CARTESIAN_POINT ( 'NONE',  ( -1.360316468750040642, 2.161458333674780352, 0.7853790794158861388 ) ) ;
#101712=( BOUNDED_CURVE ( )  B_SPLINE_CURVE ( 2, ( #77438, #209549, #172825, #128422, #194389, #66483, #111075, #177081, #31906 ),
 .UNSPECIFIED., .F., .T. ) 
 B_SPLINE_CURVE_WITH_KNOTS ( ( 3, 2, 2, 2, 3 ),
 ( 0.04687499999999993755, 0.05208333333333333565, 0.06250000000000000000, 0.07291666666666667129, 0.07812500000000022204 ),
 .UNSPECIFIED. ) 
 CURVE ( )  GEOMETRIC_REPRESENTATION_ITEM ( )  RATIONAL_B_SPLINE_CURVE ( ( 0.9330127018922192983, 0.9330127018922185211, 1.000000000000000000, 0.8660254037844387076, 1.000000000000000000, 0.8660254037844387076, 1.000000000000000000, 0.9330127018922165227, 0.9330127018922194093 ) ) 
 REPRESENTATION_ITEM ( '' )  );
#101748=CARTESIAN_POINT ( 'NONE',  ( -1.913201741516678434, 3.249623237789960761, -0.4478572873796636822 ) ) ;
#101766=CARTESIAN_POINT ( 'NONE',  ( -1.904329973710278789, 3.286760881231344467, 0.4119279214152820612 ) ) ;
#101819=CARTESIAN_POINT ( 'NONE',  ( -1.225000000000060263, 2.729166666666693164, -0.7072540797573217963 ) ) ;
#101824=CARTESIAN_POINT ( 'NONE',  ( 1.224999999999938805, -1.041666665983848938, -0.7072540797573197979 ) ) ;
#101836=ORIENTED_EDGE ( 'NONE', *, *, #214379, .T. ) ;
#101850=CARTESIAN_POINT ( 'NONE',  ( 0.6124999999999723999, 1.145833334016146843, 1.060881119635889380 ) ) ;
#101853=ORIENTED_EDGE ( 'NONE', *, *, #10962, .F. ) ;
#101861=CARTESIAN_POINT ( 'NONE',  ( -0.6801582343750022241, -0.6197916663252672764, -1.178068619123841643 ) ) ;
#101903=CARTESIAN_POINT ( 'NONE',  ( 1.360316468749963592, 1.244791667008120051, 0.7853790794158761468 ) ) ;
#101980=CARTESIAN_POINT ( 'NONE',  ( 0.3999999999999906408, 3.949999999999988187, -0.8338124244295798126 ) ) ;
#102199=CARTESIAN_POINT ( 'NONE',  ( 1.224999999999955014, 1.958333334016108873, -0.7072540797573237947 ) ) ;
#102216=CARTESIAN_POINT ( 'NONE',  ( 0.4999999999999761302, 3.172938907704328404, 0.3999999999999750422 ) ) ;
#102268=CARTESIAN_POINT ( 'NONE',  ( 1.814759087649938429, 3.975067388631681187, 0.4606438099578180068 ) ) ;
#102287=CIRCLE ( 'NONE', #1914, 0.04999999999999991257 ) ;
#102310=ORIENTED_EDGE ( 'NONE', *, *, #91921, .T. ) ;
#102405=CARTESIAN_POINT ( 'NONE',  ( -0.6801582343750265380, 1.463541667008072533, 1.178068619123799898 ) ) ;
#102427=CARTESIAN_POINT ( 'NONE',  ( -3.555477883677943599E-14, 1.187500000000005773, -1.414508159514621610 ) ) ;
#102463=VERTEX_POINT ( 'NONE', #157075 ) ;
#102471=DIRECTION ( 'NONE',  ( -1.000000000000000000, -1.276756478318932585E-15, -3.330669073875474552E-16 ) ) ;
#102510=CARTESIAN_POINT ( 'NONE',  ( -5.229199737892074420E-15, 0.06250000000001598721, 1.224999999999961009 ) ) ;
#102576=VERTEX_POINT ( 'NONE', #140848 ) ;
#102582=CARTESIAN_POINT ( 'NONE',  ( -2.353626204688216217E-14, 0.1093750003414345612, -1.570758158831782048 ) ) ;
#102588=ORIENTED_EDGE ( 'NONE', *, *, #121327, .F. ) ;
#102699=CARTESIAN_POINT ( 'NONE',  ( 0.6124999999999828360, 0.9791666673494778816, -1.060881119635955327 ) ) ;
#102734=CARTESIAN_POINT ( 'NONE',  ( 1.360316468749943608, 1.494791667008105174, 0.7853790794158439503 ) ) ;
#102756=CIRCLE ( 'NONE', #137399, 0.1000000000000000472 ) ;
#102783=CARTESIAN_POINT ( 'NONE',  ( -1.872871967411080307, 3.299999999999962519, 0.3999999999999628852 ) ) ;
#102819=CARTESIAN_POINT ( 'NONE',  ( -1.772826578343124959, 3.950000000000009059, -0.4500000000000423661 ) ) ;
#102839=CARTESIAN_POINT ( 'NONE',  ( -1.899436509991863531, 3.291494839451026166, 0.4074537448169551768 ) ) ;
#102852=CYLINDRICAL_SURFACE ( 'NONE', #174884, 1.224999999999996980 ) ;
#102890=CARTESIAN_POINT ( 'NONE',  ( -0.6124999999999880540, 0.2916666666666900554, 1.060881119635892933 ) ) ;
#102893=CARTESIAN_POINT ( 'NONE',  ( 1.224999999999962341, -0.3124999993172061785, -1.387778780781445676E-14 ) ) ;
#102909=DIRECTION ( 'NONE',  ( 3.330669073875478989E-16, -4.632576442341012461E-16, -1.000000000000000000 ) ) ;
#102969=ADVANCED_FACE ( 'NONE', ( #21440 ), #166662, .T. ) ;
#102971=CARTESIAN_POINT ( 'NONE',  ( -0.6801582343750282034, 1.432291667008027458, 1.178068619123810334 ) ) ;
#103040=CARTESIAN_POINT ( 'NONE',  ( 1.963753466588878283, 3.754052640047455647, 0.4000000000000453748 ) ) ;
#103059=ORIENTED_EDGE ( 'NONE', *, *, #204467, .T. ) ;
#103122=DIRECTION ( 'NONE',  ( -5.662137425588289679E-15, 4.419671232041788924E-16, 1.000000000000000000 ) ) ;
#103159=CARTESIAN_POINT ( 'NONE',  ( -0.6125000000000019318, 0.5208333340161186431, -1.060881119635944891 ) ) ;
#103270=CARTESIAN_POINT ( 'NONE',  ( -0.6125000000000175859, 2.104166667349471886, 1.060881119635908476 ) ) ;
#103316=FACE_OUTER_BOUND ( 'NONE', #70640, .T. ) ;
#103355=EDGE_CURVE ( 'NONE', #62036, #43349, #44142, .T. ) ;
#103424=CARTESIAN_POINT ( 'NONE',  ( -1.743066579297358008E-15, 1.875000000682791379, 1.224999999999958566 ) ) ;
#103478=CARTESIAN_POINT ( 'NONE',  ( 1.360316468750005559, 1.567708333674729282, -0.7853790794158981292 ) ) ;
#103503=CARTESIAN_POINT ( 'NONE',  ( 0.6124999999999880540, 0.1666666666666899443, -1.060881119635979530 ) ) ;
#103529=ORIENTED_EDGE ( 'NONE', *, *, #205827, .F. ) ;
#103570=( BOUNDED_CURVE ( )  B_SPLINE_CURVE ( 2, ( #201704, #53348, #147667, #39233, #139964, #189740, #4560, #138887, #123780 ),
 .UNSPECIFIED., .F., .T. ) 
 B_SPLINE_CURVE_WITH_KNOTS ( ( 3, 2, 2, 2, 3 ),
 ( 0.6406250000000002220, 0.6458333333333333703, 0.6562500000000000000, 0.6666666666666666297, 0.6718749999999998890 ),
 .UNSPECIFIED. ) 
 CURVE ( )  GEOMETRIC_REPRESENTATION_ITEM ( )  RATIONAL_B_SPLINE_CURVE ( ( 0.9330127018922194093, 0.9330127018922221849, 1.000000000000000000, 0.8660254037844387076, 1.000000000000000000, 0.8660254037844387076, 1.000000000000000000, 0.9330127018922207416, 0.9330127018922192983 ) ) 
 REPRESENTATION_ITEM ( '' )  );
#103612=ORIENTED_EDGE ( 'NONE', *, *, #205827, .T. ) ;
#103615=CIRCLE ( 'NONE', #107078, 1.224999999999996980 ) ;
#103661=CARTESIAN_POINT ( 'NONE',  ( 0.6801582343749744686, 0.3385416670080923507, -1.178068619123886718 ) ) ;
#103671=LINE ( 'NONE', #121063, #140420 ) ;
#103767=EDGE_LOOP ( 'NONE', ( #203184, #6673, #73057, #121641, #3503, #150935, #178992 ) ) ;
#103807=CARTESIAN_POINT ( 'NONE',  ( 1.360316468749983576, 0.9947916670081107249, 0.7853790794158601596 ) ) ;
#103809=DIRECTION ( 'NONE',  ( 0.000000000000000000, 1.000000000000000000, -3.330669073875479482E-16 ) ) ;
#103876=CARTESIAN_POINT ( 'NONE',  ( -0.6125000000000262457, 2.791666666666692276, 1.060881119635882497 ) ) ;
#103912=CARTESIAN_POINT ( 'NONE',  ( -1.902112725515587632, 3.289212146679059146, 0.4096023912811905809 ) ) ;
#103939=EDGE_CURVE ( 'NONE', #40528, #3320, #172210, .T. ) ;
#103971=CARTESIAN_POINT ( 'NONE',  ( 1.224999999999949241, -0.2916666659838533793, -0.7072540797573176885 ) ) ;
#104005=CARTESIAN_POINT ( 'NONE',  ( 1.360316468749957597, -0.2239583329919110355, 0.7853790794158921340 ) ) ;
#104013=VERTEX_POINT ( 'NONE', #101149 ) ;
#104036=CARTESIAN_POINT ( 'NONE',  ( 1.360316468749957597, 1.265625000341379147, -5.030698080332740574E-14 ) ) ;
#104234=PLANE ( 'NONE',  #73571 ) ;
#104334=EDGE_CURVE ( 'NONE', #6267, #31530, #106549, .T. ) ;
#104343=CARTESIAN_POINT ( 'NONE',  ( -1.225000000000033396, 2.062500000682796042, -2.949029909160572061E-14 ) ) ;
#104344=CARTESIAN_POINT ( 'NONE',  ( -0.3878679656440350842, 4.000000000000003553, -1.007084189318380618 ) ) ;
#104368=FACE_OUTER_BOUND ( 'NONE', #97565, .T. ) ;
#104399=CARTESIAN_POINT ( 'NONE',  ( 0.4499999999999975131, 3.999999999999961808, -0.9353126743251579667 ) ) ;
#104485=B_SPLINE_CURVE_WITH_KNOTS ( 'NONE', 3,
 ( #85493, #15150, #81236, #214381, #150517, #165684, #31432, #2078, #132160, #134285, #200290, #181913, #114862, #149434, #51941, #35669, #101748, #167815, #19415, #97509, #180862, #32484 ),
 .UNSPECIFIED., .F., .F.,
 ( 4, 3, 3, 3, 3, 3, 3, 4 ),
 ( 0.000000000000000000, 1.209865308640392985E-05, 2.418763075657826564E-05, 3.626888754243231552E-05, 5.481069466191479497E-05, 8.058589917395160660E-05, 0.0001081451638904113897, 0.0001095998438940794050 ),
 .UNSPECIFIED. ) ;
#104505=CARTESIAN_POINT ( 'NONE',  ( -0.6125000000000019318, 2.291666666666664298, 1.060881119635910252 ) ) ;
#104557=CARTESIAN_POINT ( 'NONE',  ( 1.360316468749957597, 1.276041667008120051, 0.7853790794158580502 ) ) ;
#104580=CARTESIAN_POINT ( 'NONE',  ( -0.6125000000000262457, 1.208333333333311277, -1.060881119635962211 ) ) ;
#104667=DIRECTION ( 'NONE',  ( -1.000000000000000000, 7.771561172376094797E-16, -3.330669073875481454E-16 ) ) ;
#104723=CARTESIAN_POINT ( 'NONE',  ( 0.3769810270647707684, 3.049942316455285685, -0.4288785890453113980 ) ) ;
#104738=FACE_OUTER_BOUND ( 'NONE', #86058, .T. ) ;
#104778=CARTESIAN_POINT ( 'NONE',  ( -0.4000000000000305533, 3.099999999999943245, 0.3423093779009872550 ) ) ;
#104798=CIRCLE ( 'NONE', #11537, 0.05000000000000008604 ) ;
#104879=CARTESIAN_POINT ( 'NONE',  ( -4.757329562667670667E-14, 0.5781250003414447614, -1.570758158831812246 ) ) ;
#104954=CARTESIAN_POINT ( 'NONE',  ( 1.224999999999953015, 1.854166666666720698, 0.7072540797572656190 ) ) ;
#105048=CARTESIAN_POINT ( 'NONE',  ( -1.225000000000004086, -0.9166666659838483833, 0.7072540797572737237 ) ) ;
#105114=CARTESIAN_POINT ( 'NONE',  ( 1.360316468749981800, 1.744791667008098290, 0.7853790794158680422 ) ) ;
#105123=CARTESIAN_POINT ( 'NONE',  ( 1.224999999999948797, 2.895833333333310389, -0.7072540797573237947 ) ) ;
#105137=CARTESIAN_POINT ( 'NONE',  ( -1.162044386198238738E-15, 2.937500000000009326, -1.225000000000010525 ) ) ;
#105187=FACE_OUTER_BOUND ( 'NONE', #110857, .T. ) ;
#105251=ORIENTED_EDGE ( 'NONE', *, *, #112850, .F. ) ;
#105264=ADVANCED_FACE ( 'NONE', ( #73530 ), #65038, .T. ) ;
#105323=DIRECTION ( 'NONE',  ( 0.000000000000000000, 1.000000000000000000, -3.330669073875479482E-16 ) ) ;
#105347=CARTESIAN_POINT ( 'NONE',  ( -1.360316468750018659, 2.401041667008069425, -0.7853790794159061228 ) ) ;
#105430=CARTESIAN_POINT ( 'NONE',  ( 1.224999999999959233, 1.166666667349521624, 0.7072540797572417492 ) ) ;
#105630=AXIS2_PLACEMENT_3D ( 'NONE', #18136, #84225, #150313 ) ;
#105643=CARTESIAN_POINT ( 'NONE',  ( -1.360316468750036645, 2.151041667008108060, -0.7853790794159301036 ) ) ;
#105666=CARTESIAN_POINT ( 'NONE',  ( -2.954552044183079750E-14, 2.734375000341430884, 1.570758158831788265 ) ) ;
#105738=B_SPLINE_CURVE_WITH_KNOTS ( 'NONE', 3,
 ( #171137, #191634, #189519, #204680 ),
 .UNSPECIFIED., .F., .F.,
 ( 4, 4 ),
 ( 0.000000000000000000, 0.0006799945003891862041 ),
 .UNSPECIFIED. ) ;
#105741=FACE_OUTER_BOUND ( 'NONE', #142693, .T. ) ;
#105749=VERTEX_POINT ( 'NONE', #166514 ) ;
#105830=DIRECTION ( 'NONE',  ( -1.000000000000000000, 7.771561172376094797E-16, -3.330669073875481454E-16 ) ) ;
#105887=LINE ( 'NONE', #190278, #181740 ) ;
#105982=CARTESIAN_POINT ( 'NONE',  ( -1.360316468750030650, 0.8697916670080861890, -0.7853790794159041244 ) ) ;
#106053=CARTESIAN_POINT ( 'NONE',  ( -1.225000000000058042, 1.520833333333367232, 0.7072540797572596238 ) ) ;
#106212=CARTESIAN_POINT ( 'NONE',  ( -5.758872628492444169E-14, 2.203125000341452200, 1.570758158831754070 ) ) ;
#106292=DIRECTION ( 'NONE',  ( -3.330669073875479482E-16, 3.330669073875479482E-16, 1.000000000000000000 ) ) ;
#106411=CARTESIAN_POINT ( 'NONE',  ( -1.225000000000044276, 0.5416666673494865414, -0.7072540797573158011 ) ) ;
#106436=DIRECTION ( 'NONE',  ( 1.276756478318932585E-15, -1.000000000000000000, 1.665334536937738262E-16 ) ) ;
#106444=CARTESIAN_POINT ( 'NONE',  ( -3.755786496842897795E-14, 2.109375000341444206, -1.570758158831810247 ) ) ;
#106454=ORIENTED_EDGE ( 'NONE', *, *, #84254, .T. ) ;
#106520=CARTESIAN_POINT ( 'NONE',  ( -2.754243431018125239E-14, 0.8750000006828161370, 1.414508159514559438 ) ) ;
#106549=CIRCLE ( 'NONE', #6118, 1.224999999999996980 ) ;
#106635=CARTESIAN_POINT ( 'NONE',  ( -1.225000000000045386, 1.312500000682802259, -4.336808689942017736E-14 ) ) ;
#106653=CARTESIAN_POINT ( 'NONE',  ( 1.772826578343081660, 3.950000000000036593, -0.4000000000000478728 ) ) ;
#106734=CARTESIAN_POINT ( 'NONE',  ( 0.6801582343749813520, 0.005208333674754095366, 1.178068619123793015 ) ) ;
#106756=CARTESIAN_POINT ( 'NONE',  ( -1.225000000000005640, 1.387778780781445676E-14, -1.387778780781445676E-14 ) ) ;
#106769=CARTESIAN_POINT ( 'NONE',  ( 0.6311622855796321652, 3.199999999999987743, 0.3999999999999646061 ) ) ;
#106774=VERTEX_POINT ( 'NONE', #88340 ) ;
#106981=CARTESIAN_POINT ( 'NONE',  ( 1.907519672996849103, 3.236073672982398008, 0.4612874649729346022 ) ) ;
#107055=CARTESIAN_POINT ( 'NONE',  ( -5.758872628492444169E-14, 0.4531250003414521998, 1.570758158831760287 ) ) ;
#107078=AXIS2_PLACEMENT_3D ( 'NONE', #209593, #176069, #78547 ) ;
#107116=CIRCLE ( 'NONE', #131236, 0.05000000000000002359 ) ;
#107132=CARTESIAN_POINT ( 'NONE',  ( -0.6124999999999967137, 1.541666666666677177, 1.060881119635903147 ) ) ;
#107190=CARTESIAN_POINT ( 'NONE',  ( -0.4288785890452923022, 3.049942316455306113, -0.4000000000000062395 ) ) ;
#107290=CARTESIAN_POINT ( 'NONE',  ( -0.6801582343750125492, 2.182291667008062763, 1.178068619123824323 ) ) ;
#107298=CARTESIAN_POINT ( 'NONE',  ( 1.360316468749980023, 0.01562500034139879812, -2.255140518769849223E-14 ) ) ;
#107360=CARTESIAN_POINT ( 'NONE',  ( 0.4288785890452437299, 3.049942316455264812, -0.4196807566835009662 ) ) ;
#107403=FACE_OUTER_BOUND ( 'NONE', #176188, .T. ) ;
#107456=EDGE_CURVE ( 'NONE', #126346, #137780, #167451, .T. ) ;
#107494=CARTESIAN_POINT ( 'NONE',  ( -1.874158809982213958, 3.299964346911606228, -0.4000000000000374922 ) ) ;
#107522=CARTESIAN_POINT ( 'NONE',  ( -1.360316468750026875, 2.671875000341383810, -2.602085213965210642E-14 ) ) ;
#107567=VERTEX_POINT ( 'NONE', #153891 ) ;
#107604=CARTESIAN_POINT ( 'NONE',  ( -1.225000000000005640, 0.5625000006828015930, -1.734723475976807094E-15 ) ) ;
#107629=ORIENTED_EDGE ( 'NONE', *, *, #145579, .T. ) ;
#107650=B_SPLINE_CURVE_WITH_KNOTS ( 'NONE', 3,
 ( #15489, #161780, #78374, #145562, #179091, #30713, #98906 ),
 .UNSPECIFIED., .F., .F.,
 ( 4, 3, 4 ),
 ( -2.180065393121582080E-06, 0.000000000000000000, 4.270488675893448704E-05 ),
 .UNSPECIFIED. ) ;
#107681=CARTESIAN_POINT ( 'NONE',  ( -0.4307572970103041854, 3.041534709929983205, 0.4240169840791090383 ) ) ;
#107817=CARTESIAN_POINT ( 'NONE',  ( 1.360316468749965590, 1.067708333674703081, -0.7853790794159082322 ) ) ;
#107838=CARTESIAN_POINT ( 'NONE',  ( -0.6125000000000279110, -0.7083333333333247106, 1.060881119635904923 ) ) ;
#107873=EDGE_LOOP ( 'NONE', ( #155945, #70031, #78055 ) ) ;
#107948=VERTEX_POINT ( 'NONE', #210027 ) ;
#108010=EDGE_CURVE ( 'NONE', #56038, #140828, #42242, .T. ) ;
#108034=CYLINDRICAL_SURFACE ( 'NONE', #44311, 0.09999999999999971412 ) ;
#108048=CARTESIAN_POINT ( 'NONE',  ( 0.3282377607281221632, 2.676335450315374676, -1.225000000000002753 ) ) ;
#108091=ORIENTED_EDGE ( 'NONE', *, *, #209517, .F. ) ;
#108104=CIRCLE ( 'NONE', #69962, 0.04999999999999985706 ) ;
#108115=VERTEX_POINT ( 'NONE', #206839 ) ;
#108133=CARTESIAN_POINT ( 'NONE',  ( 0.6801582343750038895, 0.3072916670080680368, -1.178068619123848526 ) ) ;
#108177=DIRECTION ( 'NONE',  ( 1.276756478318932585E-15, -1.000000000000000000, 1.665334536937738262E-16 ) ) ;
#108207=CARTESIAN_POINT ( 'NONE',  ( -4.757329562667670667E-14, 2.062499999999985789, 1.414508159514559438 ) ) ;
#108240=CARTESIAN_POINT ( 'NONE',  ( -2.954552044183079750E-14, 2.734375000341431772, 1.570758158831788265 ) ) ;
#108276=LINE ( 'NONE', #93045, #32939 ) ;
#108284=EDGE_CURVE ( 'NONE', #75994, #211791, #22225, .T. ) ;
#108342=ORIENTED_EDGE ( 'NONE', *, *, #141897, .F. ) ;
#108355=DIRECTION ( 'NONE',  ( -1.000000000000000000, 7.771561172376097755E-16, 4.440892098500627148E-16 ) ) ;
#108360=CARTESIAN_POINT ( 'NONE',  ( -1.360316468750021768, 0.6406250003414132310, -3.469446951953614189E-14 ) ) ;
#108410=AXIS2_PLACEMENT_3D ( 'NONE', #131985, #195879, #16028 ) ;
#108528=VERTEX_POINT ( 'NONE', #159205 ) ;
#108566=CARTESIAN_POINT ( 'NONE',  ( 1.772826578343066117, 3.950000000000009059, 0.4499999999999590994 ) ) ;
#108590=CARTESIAN_POINT ( 'NONE',  ( -1.360316468750002672, 1.921875000341424666, -3.642919299551294898E-14 ) ) ;
#108600=PLANE ( 'NONE',  #101520 ) ;
#108667=CARTESIAN_POINT ( 'NONE',  ( -1.225000000000044276, 0.5416666673494865414, -0.7072540797573158011 ) ) ;
#108747=CARTESIAN_POINT ( 'NONE',  ( -0.3405876332338036439, 3.079852035184873049, 0.4461735512527613690 ) ) ;
#108765=DIRECTION ( 'NONE',  ( 9.436895709313856232E-16, -0.8656921114426506803, -0.5005768354468324022 ) ) ;
#108767=CARTESIAN_POINT ( 'NONE',  ( 1.224999999999979661, 0.6249999999999866773, -2.775557561562891351E-14 ) ) ;
#108780=CARTESIAN_POINT ( 'NONE',  ( 0.3999999999999792610, 4.000000000000008882, 0.8338124244295505028 ) ) ;
#108801=CARTESIAN_POINT ( 'NONE',  ( 0.3282377607281153908, 1.926335450315390885, -1.225000000000010525 ) ) ;
#108887=CARTESIAN_POINT ( 'NONE',  ( 0.6801582343750056658, 0.5885416670080856338, -1.178068619123862515 ) ) ;
#108907=CARTESIAN_POINT ( 'NONE',  ( 1.224999999999996980, -0.3750000000000211497, -2.428612866367529932E-14 ) ) ;
#108997=SPHERICAL_SURFACE ( 'NONE', #100154, 0.05000000000000000278 ) ;
#109061=CARTESIAN_POINT ( 'NONE',  ( 0.4304495291404202839, 3.052659083096553871, -0.4198826858263793871 ) ) ;
#109116=LINE ( 'NONE', #92819, #167852 ) ;
#109123=CARTESIAN_POINT ( 'NONE',  ( -0.5000000000000455191, 3.999999999999955147, 0.4499999999999521605 ) ) ;
#109205=CARTESIAN_POINT ( 'NONE',  ( 1.224999999999994982, 2.666666667349464781, 0.7072540797572857141 ) ) ;
#109208=DIRECTION ( 'NONE',  ( 3.330669073875478989E-16, -3.330669073875478989E-16, -1.000000000000000000 ) ) ;
#109308=CARTESIAN_POINT ( 'NONE',  ( 1.360316468749975805, 2.776041667008103175, 0.7853790794158820310 ) ) ;
#109408=( BOUNDED_CURVE ( )  B_SPLINE_CURVE ( 3, ( #193911, #78031, #74847, #160355 ),
 .UNSPECIFIED., .F., .T. ) 
 B_SPLINE_CURVE_WITH_KNOTS ( ( 4, 4 ),
 ( 4.148111545443840420, 4.712388980384622172 ),
 .UNSPECIFIED. ) 
 CURVE ( )  GEOMETRIC_REPRESENTATION_ITEM ( )  RATIONAL_B_SPLINE_CURVE ( ( 1.000000000000000000, 0.9736414627471743355, 0.9736414627471743355, 1.000000000000000000 ) ) 
 REPRESENTATION_ITEM ( '' )  );
#109433=CARTESIAN_POINT ( 'NONE',  ( 0.6801582343749900117, 0.05729166700808169255, -1.178068619123848526 ) ) ;
#109478=VERTEX_POINT ( 'NONE', #18007 ) ;
#109534=EDGE_CURVE ( 'NONE', #39288, #109538, #179518, .T. ) ;
#109538=VERTEX_POINT ( 'NONE', #79834 ) ;
#109606=( BOUNDED_CURVE ( )  B_SPLINE_CURVE ( 3, ( #72222, #56003, #10436, #208627 ),
 .UNSPECIFIED., .F., .T. ) 
 B_SPLINE_CURVE_WITH_KNOTS ( ( 4, 4 ),
 ( 1.570796326794897668, 2.415429946053228250 ),
 .UNSPECIFIED. ) 
 CURVE ( )  GEOMETRIC_REPRESENTATION_ITEM ( )  RATIONAL_B_SPLINE_CURVE ( ( 1.000000000000000000, 0.9414278581755111119, 0.9414278581755111119, 1.000000000000000000 ) ) 
 REPRESENTATION_ITEM ( '' )  );
#109610=EDGE_LOOP ( 'NONE', ( #154860, #198781, #203207, #84593 ) ) ;
#109668=CARTESIAN_POINT ( 'NONE',  ( -1.360316468750062846, 1.401041667008104508, -0.7853790794158941324 ) ) ;
#109700=CARTESIAN_POINT ( 'NONE',  ( 0.6801582343749865700, 2.307291667008083635, -1.178068619123879834 ) ) ;
#109742=CARTESIAN_POINT ( 'NONE',  ( 1.224999999999949241, 0.4583333340161501734, -0.7072540797573277915 ) ) ;
#109956=CARTESIAN_POINT ( 'NONE',  ( 1.360316468750004448, 0.2968750003413955785, -6.938893903907228378E-15 ) ) ;
#109978=CARTESIAN_POINT ( 'NONE',  ( -3.355169270512988773E-14, -0.4375000000000020539, 1.414508159514561436 ) ) ;
#109998=CARTESIAN_POINT ( 'NONE',  ( -0.3000000000000155320, 3.999999999999955147, 1.007084189318345757 ) ) ;
#110071=AXIS2_PLACEMENT_3D ( 'NONE', #62917, #96524, #129085 ) ;
#110079=ORIENTED_EDGE ( 'NONE', *, *, #83031, .T. ) ;
#110162=ORIENTED_EDGE ( 'NONE', *, *, #160909, .T. ) ;
#110165=AXIS2_PLACEMENT_3D ( 'NONE', #79852, #211971, #18028 ) ;
#110167=FACE_OUTER_BOUND ( 'NONE', #208265, .T. ) ;
#110168=FACE_OUTER_BOUND ( 'NONE', #131043, .T. ) ;
#110237=DIRECTION ( 'NONE',  ( -1.276756478318932585E-15, 1.000000000000000000, -1.665334536937738262E-16 ) ) ;
#110266=CARTESIAN_POINT ( 'NONE',  ( -1.360316468750032870, -1.088541666325267165, 0.7853790794158641564 ) ) ;
#110268=CARTESIAN_POINT ( 'NONE',  ( -0.8666125166525048273, -3.171907292983330183E-14, 0.9704771928531863434 ) ) ;
#110339=DIRECTION ( 'NONE',  ( -1.276756478318932585E-15, 1.000000000000000000, -1.665334536937738262E-16 ) ) ;
#110361=ORIENTED_EDGE ( 'NONE', *, *, #140329, .F. ) ;
#110371=CARTESIAN_POINT ( 'NONE',  ( -1.360316468750048857, 2.651041667008094294, -0.7853790794159161148 ) ) ;
#110416=FACE_OUTER_BOUND ( 'NONE', #210072, .T. ) ;
#110495=CARTESIAN_POINT ( 'NONE',  ( 1.360316468749953600, 0.4947916670081083934, 0.7853790794158861388 ) ) ;
#110597=CYLINDRICAL_SURFACE ( 'NONE', #78664, 0.04999999999999991257 ) ;
#110682=( BOUNDED_CURVE ( )  B_SPLINE_CURVE ( 2, ( #113829, #177700, #94335, #95405, #129028, #161457, #114878, #93270, #78052 ),
 .UNSPECIFIED., .F., .T. ) 
 B_SPLINE_CURVE_WITH_KNOTS ( ( 3, 2, 2, 2, 3 ),
 ( 0.5156250000000002220, 0.5208333333333333703, 0.5312500000000000000, 0.5416666666666666297, 0.5468749999999997780 ),
 .UNSPECIFIED. ) 
 CURVE ( )  GEOMETRIC_REPRESENTATION_ITEM ( )  RATIONAL_B_SPLINE_CURVE ( ( 0.9330127018922194093, 0.9330127018922221849, 1.000000000000000000, 0.8660254037844387076, 1.000000000000000000, 0.8660254037844387076, 1.000000000000000000, 0.9330127018922221849, 0.9330127018922194093 ) ) 
 REPRESENTATION_ITEM ( '' )  );
#110722=DIRECTION ( 'NONE',  ( 4.440892098500637009E-16, 0.8656921114426514574, 0.5005768354468314030 ) ) ;
#110724=CARTESIAN_POINT ( 'NONE',  ( 1.360316468749971808, 1.026041667008142921, 0.7853790794158540534 ) ) ;
#110758=CARTESIAN_POINT ( 'NONE',  ( -0.4170821662629227156, 3.033599471985643170, 0.4170821662629036752 ) ) ;
#110826=EDGE_CURVE ( 'NONE', #146356, #42660, #52348, .T. ) ;
#110857=EDGE_LOOP ( 'NONE', ( #106454, #198691, #179313, #7811 ) ) ;
#110866=( BOUNDED_CURVE ( )  B_SPLINE_CURVE ( 3, ( #9706, #191639, #73645, #172227 ),
 .UNSPECIFIED., .F., .T. ) 
 B_SPLINE_CURVE_WITH_KNOTS ( ( 4, 4 ),
 ( 4.712388980384771386, 5.718907872238673029 ),
 .UNSPECIFIED. ) 
 CURVE ( )  GEOMETRIC_REPRESENTATION_ITEM ( )  RATIONAL_B_SPLINE_CURVE ( ( 1.000000000000000000, 0.9173434942194497177, 0.9173434942194497177, 1.000000000000000000 ) ) 
 REPRESENTATION_ITEM ( '' )  );
#110930=DIRECTION ( 'NONE',  ( 3.330669073875478989E-16, -3.540251991789410786E-16, -1.000000000000000000 ) ) ;
#111002=B_SPLINE_CURVE_WITH_KNOTS ( 'NONE', 3,
 ( #158048, #159093, #207828, #12817 ),
 .UNSPECIFIED., .F., .F.,
 ( 4, 4 ),
 ( 0.000000000000000000, 0.0006799945003891866378 ),
 .UNSPECIFIED. ) ;
#111017=CARTESIAN_POINT ( 'NONE',  ( 0.6801582343749900117, -0.6614583329919085930, -1.178068619123883165 ) ) ;
#111075=CARTESIAN_POINT ( 'NONE',  ( -0.6125000000000279110, 2.520833334016120197, -1.060881119635969094 ) ) ;
#111109=ADVANCED_FACE ( 'NONE', ( #105187 ), #204765, .T. ) ;
#111135=CARTESIAN_POINT ( 'NONE',  ( -0.3914079065636231203, 3.043201908700346792, -0.4248930002255434379 ) ) ;
#111173=ORIENTED_EDGE ( 'NONE', *, *, #158482, .T. ) ;
#111284=CARTESIAN_POINT ( 'NONE',  ( -1.992711204631002198E-15, 2.999999999999989342, 1.224999999999989875 ) ) ;
#111304=CARTESIAN_POINT ( 'NONE',  ( 1.278248824818062671E-15, 1.062499999999996003, 1.224999999999968781 ) ) ;
#111320=ORIENTED_EDGE ( 'NONE', *, *, #137088, .F. ) ;
#111332=CARTESIAN_POINT ( 'NONE',  ( 0.6124999999999793943, 2.479166667349472331, -1.060881119635965764 ) ) ;
#111443=CARTESIAN_POINT ( 'NONE',  ( 1.772826578343088544, 3.950000000000001954, -0.4500000000000284883 ) ) ;
#111556=CARTESIAN_POINT ( 'NONE',  ( 1.360316468749968033, 1.015625000341371820, -4.163336342344337027E-14 ) ) ;
#111591=CARTESIAN_POINT ( 'NONE',  ( 1.882262909678001916, 3.299172163371817401, -0.4004916885353014266 ) ) ;
#111714=DIRECTION ( 'NONE',  ( -1.276756478318932585E-15, 1.000000000000000000, -1.665334536937738262E-16 ) ) ;
#111715=CARTESIAN_POINT ( 'NONE',  ( 1.224999999999992983, 1.458333334016139071, -0.7072540797572817173 ) ) ;
#111770=DIRECTION ( 'NONE',  ( -1.000000000000000000, 7.771561172376097755E-16, 4.440892098500627148E-16 ) ) ;
#111777=DIRECTION ( 'NONE',  ( -3.330669073875477510E-16, 2.265265487380573707E-16, 1.000000000000000000 ) ) ;
#111790=VECTOR ( 'NONE', #212628, 1000.000000000000000 ) ;
#111793=CARTESIAN_POINT ( 'NONE',  ( -1.360316468750042862, 0.1510416670080827195, -0.7853790794159282163 ) ) ;
#111821=ADVANCED_FACE ( 'NONE', ( #164441 ), #165503, .T. ) ;
#111832=PLANE ( 'NONE',  #207600 ) ;
#111834=CARTESIAN_POINT ( 'NONE',  ( -0.6801582343750004478, 2.348958333674739052, -1.178068619123869398 ) ) ;
#111844=CARTESIAN_POINT ( 'NONE',  ( 0.4000000000000045186, 3.950000000000022826, -1.561251128379126385E-14 ) ) ;
#111892=( BOUNDED_CURVE ( )  B_SPLINE_CURVE ( 2, ( #90133, #138885, #204903, #56557, #122717, #205985, #213433, #60812, #96545 ),
 .UNSPECIFIED., .F., .T. ) 
 B_SPLINE_CURVE_WITH_KNOTS ( ( 3, 2, 2, 2, 3 ),
 ( 0.3906250000000001665, 0.3958333333333333148, 0.4062500000000000000, 0.4166666666666666852, 0.4218749999999998335 ),
 .UNSPECIFIED. ) 
 CURVE ( )  GEOMETRIC_REPRESENTATION_ITEM ( )  RATIONAL_B_SPLINE_CURVE ( ( 0.9330127018922194093, 0.9330127018922215187, 1.000000000000000000, 0.8660254037844387076, 1.000000000000000000, 0.8660254037844387076, 1.000000000000000000, 0.9330127018922215187, 0.9330127018922194093 ) ) 
 REPRESENTATION_ITEM ( '' )  );
#112009=CARTESIAN_POINT ( 'NONE',  ( -0.6125000000000175859, 2.104166667349471886, 1.060881119635908476 ) ) ;
#112094=CARTESIAN_POINT ( 'NONE',  ( -0.6801582343750074422, -0.1197916663252529546, -1.178068619123865846 ) ) ;
#112241=EDGE_LOOP ( 'NONE', ( #103612, #190570, #2540, #181906, #123890, #8673, #76440 ) ) ;
#112309=ORIENTED_EDGE ( 'NONE', *, *, #82886, .T. ) ;
#112319=ORIENTED_EDGE ( 'NONE', *, *, #196992, .T. ) ;
#112395=CARTESIAN_POINT ( 'NONE',  ( 1.360316468750001784, -0.7552083329919376808, 0.7853790794158941324 ) ) ;
#112433=LINE ( 'NONE', #195754, #199201 ) ;
#112484=LINE ( 'NONE', #27970, #42593 ) ;
#112494=CARTESIAN_POINT ( 'NONE',  ( -1.360316468750044638, 1.151041667008095404, -0.7853790794159261068 ) ) ;
#112498=ORIENTED_EDGE ( 'NONE', *, *, #61376, .T. ) ;
#112515=DIRECTION ( 'NONE',  ( -3.330669073875485398E-16, 1.665334536937734071E-16, 1.000000000000000000 ) ) ;
#112518=EDGE_CURVE ( 'NONE', #50089, #139477, #132647, .T. ) ;
#112544=CARTESIAN_POINT ( 'NONE',  ( 1.913843478179610536, 3.256154753185164452, 0.4414708703499702902 ) ) ;
#112603=ORIENTED_EDGE ( 'NONE', *, *, #90038, .F. ) ;
#112625=CARTESIAN_POINT ( 'NONE',  ( -2.754243431018125239E-14, 0.2031250003414269978, 1.570758158831750295 ) ) ;
#112648=CARTESIAN_POINT ( 'NONE',  ( -1.360316468750034868, 2.619791667008062319, -0.7853790794159261068 ) ) ;
#112659=CARTESIAN_POINT ( 'NONE',  ( 1.874158809982179319, 3.299964346911585356, -0.3999999999999993006 ) ) ;
#112727=CARTESIAN_POINT ( 'NONE',  ( 0.3999999999999941380, 3.949999999999995293, 0.4999999999999501510 ) ) ;
#112745=( BOUNDED_CURVE ( )  B_SPLINE_CURVE ( 2, ( #198712, #180361, #82847, #68707, #164121, #66564, #3696, #48252, #16763 ),
 .UNSPECIFIED., .F., .T. ) 
 B_SPLINE_CURVE_WITH_KNOTS ( ( 3, 2, 2, 2, 3 ),
 ( 0.1093749999999997641, 0.1145833333333333287, 0.1250000000000000000, 0.1354166666666666574, 0.1406250000000002776 ),
 .UNSPECIFIED. ) 
 CURVE ( )  GEOMETRIC_REPRESENTATION_ITEM ( )  RATIONAL_B_SPLINE_CURVE ( ( 0.9330127018922194093, 0.9330127018922163007, 1.000000000000000000, 0.8660254037844387076, 1.000000000000000000, 0.8660254037844387076, 1.000000000000000000, 0.9330127018922158566, 0.9330127018922194093 ) ) 
 REPRESENTATION_ITEM ( '' )  );
#112781=DIRECTION ( 'NONE',  ( -2.126226658603517140E-31, 1.665334536937738015E-16, 1.000000000000000000 ) ) ;
#112792=CARTESIAN_POINT ( 'NONE',  ( -0.9782388782689013240, 3.999999999999989786, -0.3999999999999993006 ) ) ;
#112800=VERTEX_POINT ( 'NONE', #121987 ) ;
#112850=EDGE_CURVE ( 'NONE', #13808, #108528, #153333, .T. ) ;
#112856=CARTESIAN_POINT ( 'NONE',  ( -1.360316468750032204, 0.6718750003414097893, -2.081668171172168513E-14 ) ) ;
#112893=ORIENTED_EDGE ( 'NONE', *, *, #206691, .T. ) ;
#113060=DIRECTION ( 'NONE',  ( -3.330669073875481947E-16, 4.742150360713068815E-16, 1.000000000000000000 ) ) ;
#113076=CIRCLE ( 'NONE', #144139, 0.04999999999999989869 ) ;
#113120=ORIENTED_EDGE ( 'NONE', *, *, #174390, .T. ) ;
#113156=CARTESIAN_POINT ( 'NONE',  ( -3.355169270512988773E-14, -0.6406249996585449136, -1.570758158831794260 ) ) ;
#113293=ADVANCED_FACE ( 'NONE', ( #142357 ), #26423, .T. ) ;
#113364=CARTESIAN_POINT ( 'NONE',  ( -0.6311622855796755749, 3.299999999999955858, -0.4000000000000444311 ) ) ;
#113467=CARTESIAN_POINT ( 'NONE',  ( -1.225000000000050271, 2.583333334016200578, 0.7072540797572757221 ) ) ;
#113567=CARTESIAN_POINT ( 'NONE',  ( -1.360316468750002672, 1.921875000341424666, -3.642919299551294898E-14 ) ) ;
#113590=CARTESIAN_POINT ( 'NONE',  ( 0.9782388782688926643, 3.999999999999968914, 0.3999999999999576672 ) ) ;
#113610=DIRECTION ( 'NONE',  ( 0.5005768354468328463, 0.8656921114426504582, -5.551115123125790098E-17 ) ) ;
#113615=CARTESIAN_POINT ( 'NONE',  ( 1.907713928855335972, 3.283019769909846897, 0.4154771360143372783 ) ) ;
#113697=CARTESIAN_POINT ( 'NONE',  ( -1.360316468750026653, -0.1302083329919105914, -0.7853790794159422051 ) ) ;
#113716=CARTESIAN_POINT ( 'NONE',  ( -1.162044386198238837E-16, 2.062499999999991562, 1.224999999999974332 ) ) ;
#113751=FACE_OUTER_BOUND ( 'NONE', #141990, .T. ) ;
#113815=CARTESIAN_POINT ( 'NONE',  ( -1.772826578343177140, 3.950000000000023714, 0.3999999999999835354 ) ) ;
#113829=CARTESIAN_POINT ( 'NONE',  ( 6.856061878569608298E-15, 0.9375000000000238698, -1.225000000000010303 ) ) ;
#113835=CARTESIAN_POINT ( 'NONE',  ( -1.878188943807090672, 3.299815425349210685, 0.3999999999999993006 ) ) ;
#113929=CARTESIAN_POINT ( 'NONE',  ( -1.360316468750019991, 0.4218750003414165062, -4.336808689942017736E-14 ) ) ;
#113968=CARTESIAN_POINT ( 'NONE',  ( 0.6801582343749952297, 2.807291667008070313, -1.178068619123883165 ) ) ;
#113992=CARTESIAN_POINT ( 'NONE',  ( -0.3282377607281447562, 0.3638354509981936991, 1.224999999999983658 ) ) ;
#114036=CARTESIAN_POINT ( 'NONE',  ( -1.926047848156435149, 3.520667328686782671, 0.3999999999999993006 ) ) ;
#114138=CIRCLE ( 'NONE', #145178, 1.962502847949850526 ) ;
#114145=CARTESIAN_POINT ( 'NONE',  ( -0.4499999960735077686, 3.999999999999980904, -0.9281957781481916525 ) ) ;
#114225=CARTESIAN_POINT ( 'NONE',  ( -1.752700365193352367E-14, -0.2656249996585993145, 1.570758158831780271 ) ) ;
#114422=DIRECTION ( 'NONE',  ( 3.497202527569253358E-15, -0.000000000000000000, 1.000000000000000000 ) ) ;
#114460=ADVANCED_FACE ( 'NONE', ( #137817 ), #175649, .T. ) ;
#114471=CARTESIAN_POINT ( 'NONE',  ( -1.360316468750038643, 2.901041667008071645, -0.7853790794159161148 ) ) ;
#114562=PLANE ( 'NONE',  #110165 ) ;
#114630=CARTESIAN_POINT ( 'NONE',  ( -0.6801582343750177673, 0.9635416670080582113, 1.178068619123796568 ) ) ;
#114636=AXIS2_PLACEMENT_3D ( 'NONE', #56495, #73802, #40248 ) ;
#114638=EDGE_CURVE ( 'NONE', #153954, #112800, #111892, .T. ) ;
#114742=CARTESIAN_POINT ( 'NONE',  ( -0.4307572970102932497, 3.041534709929986313, -0.4240169840791543354 ) ) ;
#114754=CARTESIAN_POINT ( 'NONE',  ( -1.360316468750032870, -1.088541666325267165, 0.7853790794158641564 ) ) ;
#114774=CARTESIAN_POINT ( 'NONE',  ( 1.360316468749965590, 2.494791667008093849, 0.7853790794158861388 ) ) ;
#114805=CARTESIAN_POINT ( 'NONE',  ( 1.997523430356448193, 3.481192892629490832, -0.3999999999998126721 ) ) ;
#114845=FACE_OUTER_BOUND ( 'NONE', #167037, .T. ) ;
#114862=CARTESIAN_POINT ( 'NONE',  ( -1.911686719268524293, 3.274494700676914949, -0.4236673858377688062 ) ) ;
#114878=CARTESIAN_POINT ( 'NONE',  ( 0.6124999999999776179, 0.8333333333333594606, 1.060881119635894487 ) ) ;
#114918=FACE_OUTER_BOUND ( 'NONE', #27738, .T. ) ;
#114919=ORIENTED_EDGE ( 'NONE', *, *, #197493, .F. ) ;
#114975=CARTESIAN_POINT ( 'NONE',  ( -1.360316468750018659, 0.6927083336747492659, 0.7853790794158961308 ) ) ;
#114977=ADVANCED_FACE ( 'NONE', ( #41426 ), #108600, .F. ) ;
#115015=EDGE_CURVE ( 'NONE', #209652, #164105, #82699, .T. ) ;
#115019=CARTESIAN_POINT ( 'NONE',  ( -1.360316468750021768, 0.6406250003414132310, -3.469446951953614189E-14 ) ) ;
#115027=CARTESIAN_POINT ( 'NONE',  ( -1.225000000000032063, 1.833333334016213012, 0.7072540797572777205 ) ) ;
#115040=ORIENTED_EDGE ( 'NONE', *, *, #100912, .F. ) ;
#115044=CARTESIAN_POINT ( 'NONE',  ( 4.067155351693835485E-15, 0.2500000006828133059, -1.225000000000014300 ) ) ;
#115061=AXIS2_PLACEMENT_3D ( 'NONE', #202345, #150448, #19345 ) ;
#115163=DIRECTION ( 'NONE',  ( -5.421010862427537947E-16, 0.000000000000000000, 1.000000000000000000 ) ) ;
#115278=CARTESIAN_POINT ( 'NONE',  ( 1.360316468749955598, -0.9739583329918906074, 0.7853790794158580502 ) ) ;
#115402=ORIENTED_EDGE ( 'NONE', *, *, #177464, .F. ) ;
#115413=CARTESIAN_POINT ( 'NONE',  ( -0.4000000000000322742, 4.000000000000017764, 0.9782388782688753448 ) ) ;
#115425=DIRECTION ( 'NONE',  ( 1.276756478318932585E-15, -1.000000000000000000, 1.665334536937738262E-16 ) ) ;
#115524=CARTESIAN_POINT ( 'NONE',  ( -3.755786496842897795E-14, 2.609375000341406459, -1.570758158831778273 ) ) ;
#115609=CARTESIAN_POINT ( 'NONE',  ( -8.673617379884035472E-15, 3.975067388631681187, -1.561251128379126385E-14 ) ) ;
#115624=CARTESIAN_POINT ( 'NONE',  ( -1.975475456537005874E-15, 2.812500000000000888, 1.224999999999953904 ) ) ;
#115680=CARTESIAN_POINT ( 'NONE',  ( 1.360316468750007779, 1.296875000341410455, -2.602085213965210642E-14 ) ) ;
#115690=CYLINDRICAL_SURFACE ( 'NONE', #15430, 1.224999999999996980 ) ;
#115796=CARTESIAN_POINT ( 'NONE',  ( 0.3282377607281172782, 0.9888354509981792662, -1.225000000000007860 ) ) ;
#115802=FACE_OUTER_BOUND ( 'NONE', #190322, .T. ) ;
#115815=CARTESIAN_POINT ( 'NONE',  ( 1.360316468749964480, -0.2343749996585806072, -5.204170427930421283E-15 ) ) ;
#115838=CARTESIAN_POINT ( 'NONE',  ( -1.360316468750072838, 1.661458333674769694, 0.7853790794158601596 ) ) ;
#115854=EDGE_CURVE ( 'NONE', #175466, #169074, #153639, .T. ) ;
#115995=LINE ( 'NONE', #130143, #119227 ) ;
#116010=CIRCLE ( 'NONE', #188624, 0.05000000000000009298 ) ;
#116015=ORIENTED_EDGE ( 'NONE', *, *, #108010, .T. ) ;
#116021=ORIENTED_EDGE ( 'NONE', *, *, #212155, .F. ) ;
#116038=CARTESIAN_POINT ( 'NONE',  ( -1.360316468750028651, -1.078124999658591765, -4.510281037539698445E-14 ) ) ;
#116074=CARTESIAN_POINT ( 'NONE',  ( -1.360316468750013108, 1.390625000341414008, -3.469446951953614189E-15 ) ) ;
#116085=LINE ( 'NONE', #111844, #21497 ) ;
#116145=CARTESIAN_POINT ( 'NONE',  ( -8.673617379884035472E-15, 3.975067388631681187, -1.561251128379126385E-14 ) ) ;
#116284=CARTESIAN_POINT ( 'NONE',  ( -0.6124999999999984901, 2.770833334016134408, -1.060881119635941339 ) ) ;
#116336=CARTESIAN_POINT ( 'NONE',  ( 1.360316468749949825, 1.994791667008131597, 0.7853790794158701516 ) ) ;
#116498=CARTESIAN_POINT ( 'NONE',  ( 0.3868389748197207378, 3.100956225802571797, -0.4583768147623590861 ) ) ;
#116506=CARTESIAN_POINT ( 'NONE',  ( -1.225000000000014300, 0.7500000000000145439, -2.602085213965210642E-14 ) ) ;
#116581=CARTESIAN_POINT ( 'NONE',  ( -1.772826578342764359, 3.950000000000574385, -0.4000000000000286660 ) ) ;
#116608=CARTESIAN_POINT ( 'NONE',  ( -0.6125000000000262457, 0.4583333333333244886, -1.060881119635996850 ) ) ;
#116655=DIRECTION ( 'NONE',  ( 3.330669073875479482E-16, -3.330669073875479482E-16, -1.000000000000000000 ) ) ;
#116750=CARTESIAN_POINT ( 'NONE',  ( 1.360316468749957597, 1.276041667008120051, 0.7853790794158581612 ) ) ;
#116778=VERTEX_POINT ( 'NONE', #174827 ) ;
#116876=ORIENTED_EDGE ( 'NONE', *, *, #168793, .T. ) ;
#116880=CARTESIAN_POINT ( 'NONE',  ( -3.355169270512988773E-14, -0.7968749996585455797, 1.570758158831762286 ) ) ;
#116900=CARTESIAN_POINT ( 'NONE',  ( 1.224999999999955014, 2.145833333333346360, -0.7072540797573136917 ) ) ;
#116903=CARTESIAN_POINT ( 'NONE',  ( -0.6801582343750403048, 1.598958333674738164, -1.178068619123869398 ) ) ;
#116977=DIRECTION ( 'NONE',  ( 0.000000000000000000, 0.000000000000000000, -1.000000000000000000 ) ) ;
#116999=EDGE_CURVE ( 'NONE', #109538, #107567, #149128, .T. ) ;
#117016=AXIS2_PLACEMENT_3D ( 'NONE', #59971, #126125, #96776 ) ;
#117061=CARTESIAN_POINT ( 'NONE',  ( 0.4499999999999922395, 3.999999999999974243, -0.8338124244296039045 ) ) ;
#117079=CARTESIAN_POINT ( 'NONE',  ( 1.772826578343048798, 4.000000000000045297, -0.4500000000000284883 ) ) ;
#117086=DIRECTION ( 'NONE',  ( 1.276756478318932585E-15, -1.000000000000000000, 1.665334536937738262E-16 ) ) ;
#117105=CARTESIAN_POINT ( 'NONE',  ( -1.360316468750000674, -0.3489583329919356824, -0.7853790794158941324 ) ) ;
#117118=ADVANCED_FACE ( 'NONE', ( #91438 ), #127208, .T. ) ;
#117145=CARTESIAN_POINT ( 'NONE',  ( 1.360316468750000896, 0.7656250003413994643, 0.000000000000000000 ) ) ;
#117171=AXIS2_PLACEMENT_3D ( 'NONE', #79965, #47501, #113610 ) ;
#117177=EDGE_CURVE ( 'NONE', #116778, #86803, #142218, .T. ) ;
#117220=AXIS2_PLACEMENT_3D ( 'NONE', #139521, #140609, #109208 ) ;
#117278=ORIENTED_EDGE ( 'NONE', *, *, #80620, .F. ) ;
#117324=LINE ( 'NONE', #97835, #174538 ) ;
#117376=ORIENTED_EDGE ( 'NONE', *, *, #112850, .T. ) ;
#117402=EDGE_CURVE ( 'NONE', #140322, #28319, #117324, .T. ) ;
#117424=EDGE_CURVE ( 'NONE', #15383, #177247, #14984, .T. ) ;
#117448=CARTESIAN_POINT ( 'NONE',  ( -0.6125000000000019318, 1.270833334016133076, -1.060881119635938008 ) ) ;
#117453=ADVANCED_FACE ( 'NONE', ( #133550 ), #37152, .T. ) ;
#117540=( BOUNDED_CURVE ( )  B_SPLINE_CURVE ( 2, ( #11998, #127997, #161481, #111715, #79139, #50904, #134320, #34643, #17310 ),
 .UNSPECIFIED., .F., .T. ) 
 B_SPLINE_CURVE_WITH_KNOTS ( ( 3, 2, 2, 2, 3 ),
 ( 0.3281250000000001665, 0.3333333333333333148, 0.3437500000000000000, 0.3541666666666666852, 0.3593749999999997224 ),
 .UNSPECIFIED. ) 
 CURVE ( )  GEOMETRIC_REPRESENTATION_ITEM ( )  RATIONAL_B_SPLINE_CURVE ( ( 0.9330127018922194093, 0.9330127018922215187, 1.000000000000000000, 0.8660254037844387076, 1.000000000000000000, 0.8660254037844387076, 1.000000000000000000, 0.9330127018922229620, 0.9330127018922194093 ) ) 
 REPRESENTATION_ITEM ( '' )  );
#117577=CARTESIAN_POINT ( 'NONE',  ( -0.3282377607281493637, 0.8013354503153625741, 1.224999999999967004 ) ) ;
#117580=CARTESIAN_POINT ( 'NONE',  ( -1.225000000000024736, 1.062500000682836676, -3.122502256758252770E-14 ) ) ;
#117659=CARTESIAN_POINT ( 'NONE',  ( -1.898855744251342514, 3.739179606816304346, -0.4000000000000286104 ) ) ;
#117662=CARTESIAN_POINT ( 'NONE',  ( -1.360316468750006669, 2.442708333674733723, 0.7853790794158861388 ) ) ;
#117686=CARTESIAN_POINT ( 'NONE',  ( -4.156403723172807449E-14, 0.8124999999999957812, 1.414508159514549446 ) ) ;
#117723=EDGE_LOOP ( 'NONE', ( #161696, #33044, #20201, #157103 ) ) ;
#117749=ADVANCED_FACE ( 'NONE', ( #183322 ), #69547, .F. ) ;
#117768=CARTESIAN_POINT ( 'NONE',  ( -1.992711204631002198E-15, 2.999999999999989342, 1.224999999999989875 ) ) ;
#117792=LINE ( 'NONE', #63646, #127585 ) ;
#117806=( BOUNDED_CURVE ( )  B_SPLINE_CURVE ( 2, ( #99719, #132257, #84530, #198264, #148482, #167919, #101850, #52040, #51 ),
 .UNSPECIFIED., .F., .T. ) 
 B_SPLINE_CURVE_WITH_KNOTS ( ( 3, 2, 2, 2, 3 ),
 ( 0.3906250000000002220, 0.3958333333333333148, 0.4062500000000000000, 0.4166666666666666852, 0.4218749999999998890 ),
 .UNSPECIFIED. ) 
 CURVE ( )  GEOMETRIC_REPRESENTATION_ITEM ( )  RATIONAL_B_SPLINE_CURVE ( ( 0.9330127018922194093, 0.9330127018922221849, 1.000000000000000000, 0.8660254037844387076, 1.000000000000000000, 0.8660254037844387076, 1.000000000000000000, 0.9330127018922207416, 0.9330127018922192983 ) ) 
 REPRESENTATION_ITEM ( '' )  );
#117831=CARTESIAN_POINT ( 'NONE',  ( -1.360316468750042862, 0.1510416670080827195, -0.7853790794159281052 ) ) ;
#117945=CARTESIAN_POINT ( 'NONE',  ( -0.4288785890452732064, 3.049942316455313218, 0.4196807566830707548 ) ) ;
#117976=CARTESIAN_POINT ( 'NONE',  ( -0.6801582343750282034, 2.432291667008048996, 1.178068619123807004 ) ) ;
#118078=ORIENTED_EDGE ( 'NONE', *, *, #173979, .F. ) ;
#118137=FACE_OUTER_BOUND ( 'NONE', #138580, .T. ) ;
#118139=CARTESIAN_POINT ( 'NONE',  ( -1.225000000000016298, 0.2708333333333532988, 0.7072540797572717253 ) ) ;
#118142=CARTESIAN_POINT ( 'NONE',  ( -0.6125000000000314637, -0.2291666659838820230, -1.060881119635976200 ) ) ;
#118158=CARTESIAN_POINT ( 'NONE',  ( 1.224999999999986988, 1.645833333333327486, -0.7072540797572998139 ) ) ;
#118177=CARTESIAN_POINT ( 'NONE',  ( -1.360316468750013108, -0.3281249996585910989, -3.469446951953614189E-14 ) ) ;
#118216=CARTESIAN_POINT ( 'NONE',  ( 1.360316468749981578, 1.744791667008098290, 0.7853790794158680422 ) ) ;
#118396=EDGE_CURVE ( 'NONE', #53788, #59826, #36110, .T. ) ;
#118513=CARTESIAN_POINT ( 'NONE',  ( -1.225000000000035172, 1.562500000682809365, -4.510281037539698445E-14 ) ) ;
#118523=ORIENTED_EDGE ( 'NONE', *, *, #122827, .F. ) ;
#118576=CARTESIAN_POINT ( 'NONE',  ( -1.326716514427061987E-15, 2.999999999999988454, -1.225000000000003864 ) ) ;
#118718=CARTESIAN_POINT ( 'NONE',  ( -1.360316468750038643, 1.651041667008089853, -0.7853790794159041244 ) ) ;
#118730=AXIS2_PLACEMENT_3D ( 'NONE', #200801, #137979, #38332 ) ;
#118741=CARTESIAN_POINT ( 'NONE',  ( 1.224999999999963896, 1.374999999999987343, -4.857225732735059864E-14 ) ) ;
#118779=VERTEX_POINT ( 'NONE', #149511 ) ;
#118790=CARTESIAN_POINT ( 'NONE',  ( 0.8281745818101267087, -6.790584702349180379E-15, 1.093811874046688892 ) ) ;
#118824=( BOUNDED_SURFACE ( )  B_SPLINE_SURFACE ( 3, 2, ( 
 ( #2741, #50462, #116581 ),
 ( #167414, #182576, #117659 ),
 ( #35256, #19005, #85086 ),
 ( #140280, #39539, #40628 ) ),
 .UNSPECIFIED., .F., .F., .F. ) 
 B_SPLINE_SURFACE_WITH_KNOTS ( ( 4, 4 ),
 ( 3, 3 ),
 ( 0.0002736160683302315730, 0.001000278046670501726 ),
 ( 0.000000000000000000, 1.000000000000000000 ),
 .UNSPECIFIED. ) 
 GEOMETRIC_REPRESENTATION_ITEM ( )  RATIONAL_B_SPLINE_SURFACE ( (
 ( 1.000000000000000000, 0.6273451206645928035, 1.000000000000000000),
 ( 1.000000000000000000, 0.6198151287834093859, 1.000000000000000000),
 ( 1.000000000000000000, 0.6183718462548107864, 1.000000000000000000),
 ( 1.000000000000000000, 0.6222643257228465119, 1.000000000000000000) ) ) 
 REPRESENTATION_ITEM ( '' )  SURFACE ( )  );
#118839=AXIS2_PLACEMENT_3D ( 'NONE', #28921, #110237, #95006 ) ;
#118886=EDGE_CURVE ( 'NONE', #53408, #61933, #43116, .T. ) ;
#118893=CARTESIAN_POINT ( 'NONE',  ( -0.6801582343750438575, 0.7135416670080579893, 1.178068619123810334 ) ) ;
#118912=EDGE_CURVE ( 'NONE', #184258, #74569, #30200, .T. ) ;
#119040=CARTESIAN_POINT ( 'NONE',  ( 1.360316468749955598, 1.536458333674721288, -0.7853790794159342115 ) ) ;
#119056=CYLINDRICAL_SURFACE ( 'NONE', #115061, 1.224999999999996980 ) ;
#119114=AXIS2_PLACEMENT_3D ( 'NONE', #195942, #162381, #129954 ) ;
#119143=DIRECTION ( 'NONE',  ( -1.000000000000000000, 7.771561172376097755E-16, 4.440892098500627148E-16 ) ) ;
#119156=FACE_OUTER_BOUND ( 'NONE', #174961, .T. ) ;
#119201=CARTESIAN_POINT ( 'NONE',  ( 0.6124999999999932720, -0.6041666659838615949, 1.060881119635929348 ) ) ;
#119219=CARTESIAN_POINT ( 'NONE',  ( 0.3282377607281223852, 1.573664549684625769, 1.224999999999981659 ) ) ;
#119227=VECTOR ( 'NONE', #165756, 1000.000000000000000 ) ;
#119280=CARTESIAN_POINT ( 'NONE',  ( 1.360316468749983798, 0.9947916670081107249, 0.7853790794158600486 ) ) ;
#119346=CARTESIAN_POINT ( 'NONE',  ( 6.972266317189433020E-16, 0.5000000006828014820, -1.225000000000012745 ) ) ;
#119472=CARTESIAN_POINT ( 'NONE',  ( -1.872228381520322449, 3.300000000000011369, -0.3999999999999993006 ) ) ;
#119576=AXIS2_PLACEMENT_3D ( 'NONE', #175593, #111714, #112781 ) ;
#119581=CARTESIAN_POINT ( 'NONE',  ( 0.6124999999999776179, 1.479166667349464337, -1.060881119635962211 ) ) ;
#119593=CYLINDRICAL_SURFACE ( 'NONE', #60855, 0.09999999999999971412 ) ;
#119671=DIRECTION ( 'NONE',  ( -3.497202527569253358E-15, 0.000000000000000000, -1.000000000000000000 ) ) ;
#119676=ORIENTED_EDGE ( 'NONE', *, *, #124581, .F. ) ;
#119687=APPLICATION_CONTEXT ( 'automotive_design' ) ;
#119715=ADVANCED_FACE ( 'NONE', ( #13891 ), #131968, .T. ) ;
#119719=CIRCLE ( 'NONE', #171597, 0.05000000000000007910 ) ;
#119787=CARTESIAN_POINT ( 'NONE',  ( -0.4169036860910567133, 3.145283463680806246, 0.4342470185719313203 ) ) ;
#119790=CARTESIAN_POINT ( 'NONE',  ( 1.360316468749971808, 2.567708333674758148, -0.7853790794159301036 ) ) ;
#119792=PRODUCT_CONTEXT ( 'NONE', #119687, 'mechanical' ) ;
#119813=CARTESIAN_POINT ( 'NONE',  ( -0.6125000000000331291, 0.7916666666666558605, 1.060881119635891157 ) ) ;
#119819=EDGE_CURVE ( 'NONE', #142570, #191858, #99563, .T. ) ;
#119884=EDGE_CURVE ( 'NONE', #6089, #30915, #74494, .T. ) ;
#119945=ORIENTED_EDGE ( 'NONE', *, *, #100518, .F. ) ;
#119959=DIRECTION ( 'NONE',  ( 1.276756478318932585E-15, -1.000000000000000000, 1.665334536937738262E-16 ) ) ;
#120118=CARTESIAN_POINT ( 'NONE',  ( -1.360316468750008667, 0.1197916670080665519, -0.7853790794159001276 ) ) ;
#120136=CARTESIAN_POINT ( 'NONE',  ( 1.813763795902412879, 3.950000000000016165, 0.3999999999999576672 ) ) ;
#120166=DIRECTION ( 'NONE',  ( -3.330669073875479482E-16, 3.330669073875479482E-16, 1.000000000000000000 ) ) ;
#120169=CARTESIAN_POINT ( 'NONE',  ( -1.872228381520320672, 3.299999999999962519, 0.3999999999999628852 ) ) ;
#120193=FACE_OUTER_BOUND ( 'NONE', #121844, .T. ) ;
#120238=CARTESIAN_POINT ( 'NONE',  ( 0.7119062752653980697, -6.995223886616102449E-15, -1.051716123837681760 ) ) ;
#120245=CARTESIAN_POINT ( 'NONE',  ( 0.4320269763654895345, 3.055387103097206847, -0.4199383792806877236 ) ) ;
#120266=DIRECTION ( 'NONE',  ( 3.330669073875478989E-16, -3.540251991789410786E-16, -1.000000000000000000 ) ) ;
#120277=CARTESIAN_POINT ( 'NONE',  ( 0.6124999999999707345, 1.895833334016133742, 1.060881119635880721 ) ) ;
#120284=CARTESIAN_POINT ( 'NONE',  ( -1.225000000000022293, -1.166666665983833617, 0.7072540797572477445 ) ) ;
#120293=CARTESIAN_POINT ( 'NONE',  ( 0.2999999999999669598, 4.050057683544661558, -0.8916696671246847616 ) ) ;
#120352=CARTESIAN_POINT ( 'NONE',  ( -3.956095110007852622E-14, 2.328125000341396689, -1.570758158831800255 ) ) ;
#120385=CARTESIAN_POINT ( 'NONE',  ( 1.910130646976073043, 3.278792710263286114, -0.4195261609911307144 ) ) ;
#120453=FACE_OUTER_BOUND ( 'NONE', #21941, .T. ) ;
#120457=AXIS2_PLACEMENT_3D ( 'NONE', #120293, #153787, #23768 ) ;
#120458=AXIS2_PLACEMENT_3D ( 'NONE', #210785, #62408, #124306 ) ;
#120595=ORIENTED_EDGE ( 'NONE', *, *, #180391, .T. ) ;
#120661=CARTESIAN_POINT ( 'NONE',  ( 0.6124999999999707345, 1.395833334016133298, 1.060881119635904923 ) ) ;
#120874=CARTESIAN_POINT ( 'NONE',  ( -0.6801582343750125492, 2.213541667008059211, 1.178068619123818994 ) ) ;
#120884=CARTESIAN_POINT ( 'NONE',  ( 1.872228381520312013, 3.299999999999997158, -0.4000000000000131783 ) ) ;
#120897=CARTESIAN_POINT ( 'NONE',  ( 1.224999999999951017, 0.1458333333333527160, -0.7072540797573076965 ) ) ;
#120971=DIRECTION ( 'NONE',  ( -3.219646771412963434E-15, -1.665334536937739741E-16, -1.000000000000000000 ) ) ;
#120986=( BOUNDED_CURVE ( )  B_SPLINE_CURVE ( 2, ( #34680, #166831, #102890, #118139, #200364, #18426, #82366, #136471, #84500 ),
 .UNSPECIFIED., .F., .T. ) 
 B_SPLINE_CURVE_WITH_KNOTS ( ( 3, 2, 2, 2, 3 ),
 ( 0.6718749999999998890, 0.6770833333333333703, 0.6875000000000000000, 0.6979166666666666297, 0.7031250000000002220 ),
 .UNSPECIFIED. ) 
 CURVE ( )  GEOMETRIC_REPRESENTATION_ITEM ( )  RATIONAL_B_SPLINE_CURVE ( ( 0.9330127018922192983, 0.9330127018922178550, 1.000000000000000000, 0.8660254037844387076, 1.000000000000000000, 0.8660254037844387076, 1.000000000000000000, 0.9330127018922165227, 0.9330127018922194093 ) ) 
 REPRESENTATION_ITEM ( '' )  );
#120991=FACE_OUTER_BOUND ( 'NONE', #62935, .T. ) ;
#121054=CARTESIAN_POINT ( 'NONE',  ( -0.6801582343750334214, 0.3802083336747336118, -1.178068619123869398 ) ) ;
#121063=CARTESIAN_POINT ( 'NONE',  ( -0.3000000000000432876, 3.999999999999940936, 0.9782388782688614670 ) ) ;
#121170=CARTESIAN_POINT ( 'NONE',  ( -1.045839947578414805E-15, 1.812499999999992673, 1.224999999999988987 ) ) ;
#121200=CARTESIAN_POINT ( 'NONE',  ( 0.6801582343749970061, 0.5572916670080683144, -1.178068619123862515 ) ) ;
#121262=ORIENTED_EDGE ( 'NONE', *, *, #170740, .F. ) ;
#121268=CARTESIAN_POINT ( 'NONE',  ( -1.225000000000004086, 1.979166666666657193, -0.7072540797572898219 ) ) ;
#121313=DIRECTION ( 'NONE',  ( 1.276756478318932585E-15, -1.000000000000000000, 1.665334536937738262E-16 ) ) ;
#121327=EDGE_CURVE ( 'NONE', #210405, #74826, #193411, .T. ) ;
#121333=ORIENTED_EDGE ( 'NONE', *, *, #76048, .F. ) ;
#121359=CARTESIAN_POINT ( 'NONE',  ( 0.6124999999999811706, -0.2708333326505441008, -1.060881119635955327 ) ) ;
#121428=CARTESIAN_POINT ( 'NONE',  ( 1.360316468749966257, 1.765625000341414230, -3.642919299551294898E-14 ) ) ;
#121438=CARTESIAN_POINT ( 'NONE',  ( -0.6801582343750074422, 0.5989583336747372755, -1.178068619123841643 ) ) ;
#121461=ORIENTED_EDGE ( 'NONE', *, *, #166426, .T. ) ;
#121500=CARTESIAN_POINT ( 'NONE',  ( -1.734723475976807094E-15, 2.999999999999988898, -6.938893903907228378E-15 ) ) ;
#121506=ADVANCED_FACE ( 'NONE', ( #51534 ), #118824, .T. ) ;
#121616=CARTESIAN_POINT ( 'NONE',  ( -0.4000000000000201172, 4.000000000000003553, -0.9782388782689169782 ) ) ;
#121641=ORIENTED_EDGE ( 'NONE', *, *, #22519, .T. ) ;
#121652=DIRECTION ( 'NONE',  ( 1.000000000000000000, -7.771561172376097755E-16, -4.440892098500627148E-16 ) ) ;
#121659=CARTESIAN_POINT ( 'NONE',  ( -2.754243431018125239E-14, 1.984375000341467299, 1.570758158831788265 ) ) ;
#121717=CYLINDRICAL_SURFACE ( 'NONE', #50498, 0.09999999999999982514 ) ;
#121738=CARTESIAN_POINT ( 'NONE',  ( 1.224999999999979217, 1.208333334016137739, -0.7072540797573076965 ) ) ;
#121761=AXIS2_PLACEMENT_3D ( 'NONE', #135300, #204516, #172056 ) ;
#121844=EDGE_LOOP ( 'NONE', ( #101853, #66172, #58606, #142099, #182125 ) ) ;
#121875=CARTESIAN_POINT ( 'NONE',  ( 0.4170821662628915183, 3.033599471985643170, 0.4170821662628724225 ) ) ;
#121946=CARTESIAN_POINT ( 'NONE',  ( 1.360316468749987573, 1.817708333674738608, -0.7853790794158981292 ) ) ;
#121968=CARTESIAN_POINT ( 'NONE',  ( -4.757329562667670667E-14, -0.1874999999999768518, 1.414508159514551444 ) ) ;
#121983=SHAPE_REPRESENTATION ( 'screw coil', ( #200407 ), #141734 ) ;
#121987=CARTESIAN_POINT ( 'NONE',  ( -2.440293211016301606E-15, 1.312499999999991118, 1.224999999999973888 ) ) ;
#121995=CARTESIAN_POINT ( 'NONE',  ( -0.4000000000000131783, 3.372708439410149417, -0.5000000000000160982 ) ) ;
#122001=ORIENTED_EDGE ( 'NONE', *, *, #71255, .F. ) ;
#122036=VECTOR ( 'NONE', #5802, 1000.000000000000000 ) ;
#122072=( BOUNDED_CURVE ( )  B_SPLINE_CURVE ( 3, ( #133490, #198429, #97776, #16477 ),
 .UNSPECIFIED., .F., .T. ) 
 B_SPLINE_CURVE_WITH_KNOTS ( ( 4, 4 ),
 ( 3.705870088530484718, 4.712388980384521808 ),
 .UNSPECIFIED. ) 
 CURVE ( )  GEOMETRIC_REPRESENTATION_ITEM ( )  RATIONAL_B_SPLINE_CURVE ( ( 1.000000000000000000, 0.9173434942194278463, 0.9173434942194278463, 1.000000000000000000 ) ) 
 REPRESENTATION_ITEM ( '' )  );
#122076=VERTEX_POINT ( 'NONE', #2114 ) ;
#122115=DIRECTION ( 'NONE',  ( 1.276756478318932585E-15, -1.000000000000000000, 1.665334536937738262E-16 ) ) ;
#122123=CARTESIAN_POINT ( 'NONE',  ( -0.6801582343750438575, 0.6302083336747199560, -1.178068619123869398 ) ) ;
#122158=ADVANCED_FACE ( 'NONE', ( #8275 ), #135369, .T. ) ;
#122236=ORIENTED_EDGE ( 'NONE', *, *, #54770, .F. ) ;
#122273=ORIENTED_EDGE ( 'NONE', *, *, #153089, .T. ) ;
#122275=CARTESIAN_POINT ( 'NONE',  ( 1.360316468749983576, 0.5156250003414062366, -5.204170427930421283E-15 ) ) ;
#122297=LINE ( 'NONE', #172024, #192296 ) ;
#122349=CARTESIAN_POINT ( 'NONE',  ( -5.157946788997579689E-14, 2.437500000000003553, -1.414508159514605401 ) ) ;
#122383=CARTESIAN_POINT ( 'NONE',  ( -1.913843809498108950, 3.268536626279731738, 0.4294081188992993070 ) ) ;
#122439=CARTESIAN_POINT ( 'NONE',  ( 1.224999999999989209, -1.083333332650529224, 0.7072540797572777205 ) ) ;
#122508=CARTESIAN_POINT ( 'NONE',  ( 0.6801582343749865700, 2.307291667008083635, -1.178068619123879834 ) ) ;
#122582=CARTESIAN_POINT ( 'NONE',  ( 0.2999999999999842792, 3.975028841772351829, 0.9637995837462106641 ) ) ;
#122708=CARTESIAN_POINT ( 'NONE',  ( -1.225000000000040057, 0.5833333340161186431, 0.7072540797572817173 ) ) ;
#122717=CARTESIAN_POINT ( 'NONE',  ( 1.224999999999963896, 1.374999999999987343, -4.857225732735059864E-14 ) ) ;
#122739=CARTESIAN_POINT ( 'NONE',  ( 0.6801582343749674742, 1.755208333674734833, 1.178068619123803451 ) ) ;
#122751=CARTESIAN_POINT ( 'NONE',  ( 0.6124999999999793943, 2.479166667349472331, -1.060881119635965764 ) ) ;
#122793=ADVANCED_FACE ( 'NONE', ( #162929 ), #27576, .T. ) ;
#122820=CARTESIAN_POINT ( 'NONE',  ( -1.225000000000016076, 0.8333333340161279690, 0.7072540797572857141 ) ) ;
#122827=EDGE_CURVE ( 'NONE', #55688, #23953, #9018, .T. ) ;
#122942=DIRECTION ( 'NONE',  ( 3.330669073875479482E-16, -3.330669073875479482E-16, -1.000000000000000000 ) ) ;
#123036=CARTESIAN_POINT ( 'NONE',  ( 0.6801582343749865700, 0.08854166700808518975, -1.178068619123869398 ) ) ;
#123058=CARTESIAN_POINT ( 'NONE',  ( -0.6801582343750420812, 2.713541667008087632, 1.178068619123787908 ) ) ;
#123185=ORIENTED_EDGE ( 'NONE', *, *, #7576, .F. ) ;
#123328=AXIS2_PLACEMENT_3D ( 'NONE', #182264, #146614, #16554 ) ;
#123345=CARTESIAN_POINT ( 'NONE',  ( 1.360316468749973584, 0.7864583336747016373, -0.7853790794159161148 ) ) ;
#123416=CARTESIAN_POINT ( 'NONE',  ( 1.224999999999955014, 1.895833333333312831, -0.7072540797573217963 ) ) ;
#123454=CARTESIAN_POINT ( 'NONE',  ( 0.6801582343749831283, 2.755208333674742605, 1.178068619123796568 ) ) ;
#123476=CARTESIAN_POINT ( 'NONE',  ( 0.4999999999999848455, 3.949999999999953548, -0.4500000000000250466 ) ) ;
#123496=CARTESIAN_POINT ( 'NONE',  ( 0.4809368265653533037, 3.139971263792666445, -0.4000000000000023537 ) ) ;
#123573=CARTESIAN_POINT ( 'NONE',  ( -0.6801582343750213200, 1.348958333674710186, -1.178068619123886718 ) ) ;
#123604=CARTESIAN_POINT ( 'NONE',  ( 1.907692715643306114, 3.236394383240543959, -0.4609675857477724681 ) ) ;
#123620=CARTESIAN_POINT ( 'NONE',  ( 1.224999999999947020, 2.354166666666674512, 0.7072540797573039217 ) ) ;
#123645=ADVANCED_FACE ( 'NONE', ( #156275 ), #121717, .F. ) ;
#123704=CARTESIAN_POINT ( 'NONE',  ( -0.3000000000000051514, 3.322650755865477645, -0.5865692111443002732 ) ) ;
#123709=ORIENTED_EDGE ( 'NONE', *, *, #103355, .T. ) ;
#123768=EDGE_CURVE ( 'NONE', #127784, #144032, #907, .T. ) ;
#123780=CARTESIAN_POINT ( 'NONE',  ( -1.162044386198238935E-15, 0.3125000000000180411, 1.224999999999967004 ) ) ;
#123801=CARTESIAN_POINT ( 'NONE',  ( 1.224999999999969225, 0.6875000006828015930, -3.642919299551294898E-14 ) ) ;
#123803=CARTESIAN_POINT ( 'NONE',  ( -1.360316468750048635, 2.651041667008094738, -0.7853790794159161148 ) ) ;
#123855=CARTESIAN_POINT ( 'NONE',  ( -0.4254946254921331272, 3.044090126849021694, -0.4192457809173989469 ) ) ;
#123859=AXIS2_PLACEMENT_3D ( 'NONE', #208094, #139937, #125880 ) ;
#123880=CARTESIAN_POINT ( 'NONE',  ( 0.6124999999999759526, 0.8958333340161606095, 1.060881119635896264 ) ) ;
#123890=ORIENTED_EDGE ( 'NONE', *, *, #200423, .F. ) ;
#123953=FACE_OUTER_BOUND ( 'NONE', #201379, .T. ) ;
#123995=ADVANCED_FACE ( 'NONE', ( #44956 ), #179209, .T. ) ;
#124005=CARTESIAN_POINT ( 'NONE',  ( 2.672702088255949078E-15, 1.937500000000013323, -1.225000000000018074 ) ) ;
#124015=VECTOR ( 'NONE', #117086, 1000.000000000000000 ) ;
#124092=CARTESIAN_POINT ( 'NONE',  ( -1.360316468750014884, 0.1927083336747308917, 0.7853790794158901356 ) ) ;
#124114=CARTESIAN_POINT ( 'NONE',  ( 1.224999999999943023, -0.8541666666666519747, -0.7072540797573197979 ) ) ;
#124142=VERTEX_POINT ( 'NONE', #18803 ) ;
#124225=ADVANCED_FACE ( 'NONE', ( #1473 ), #119593, .T. ) ;
#124306=DIRECTION ( 'NONE',  ( 1.000000000000000000, 0.000000000000000000, -4.336808689942017736E-15 ) ) ;
#124319=CARTESIAN_POINT ( 'NONE',  ( -2.091679895156829610E-15, 2.562499999999987121, 1.224999999999973888 ) ) ;
#124326=ORIENTED_EDGE ( 'NONE', *, *, #72117, .F. ) ;
#124334=LINE ( 'NONE', #174088, #96039 ) ;
#124404=CARTESIAN_POINT ( 'NONE',  ( 1.360316468749977581, 0.5364583336746844289, -0.7853790794159001276 ) ) ;
#124476=CARTESIAN_POINT ( 'NONE',  ( -1.225000000000019407, 2.500000000000009326, -1.387778780781445676E-14 ) ) ;
#124535=EDGE_CURVE ( 'NONE', #30915, #99612, #112433, .T. ) ;
#124537=CARTESIAN_POINT ( 'NONE',  ( -0.6125000000000279110, 1.291666666666656305, 1.060881119635892933 ) ) ;
#124552=ORIENTED_EDGE ( 'NONE', *, *, #165324, .F. ) ;
#124581=EDGE_CURVE ( 'NONE', #171576, #102576, #16249, .T. ) ;
#124632=CARTESIAN_POINT ( 'NONE',  ( 5.007715329123863766E-16, 0.8281250003414059035, -1.570758158831786266 ) ) ;
#124641=CARTESIAN_POINT ( 'NONE',  ( 0.6125000000000123679, 2.916666666666671404, -1.060881119635948444 ) ) ;
#124664=CARTESIAN_POINT ( 'NONE',  ( 1.913843809498031012, 3.268536626279791690, -0.4294081188993625342 ) ) ;
#124699=CARTESIAN_POINT ( 'NONE',  ( 7.320879633048903241E-15, 0.3750000006828252408, 1.224999999999981659 ) ) ;
#124783=CYLINDRICAL_SURFACE ( 'NONE', #95427, 1.224999999999996980 ) ;
#124803=EDGE_LOOP ( 'NONE', ( #39362, #67931, #177736, #170658 ) ) ;
#124836=ORIENTED_EDGE ( 'NONE', *, *, #122827, .T. ) ;
#124856=CARTESIAN_POINT ( 'NONE',  ( -1.360316468750026653, 2.192708333674788346, 0.7853790794158680422 ) ) ;
#124938=CARTESIAN_POINT ( 'NONE',  ( -0.6125000000000019318, 0.5208333340161186431, -1.060881119635944891 ) ) ;
#124980=EDGE_CURVE ( 'NONE', #149597, #211791, #162041, .T. ) ;
#125050=CARTESIAN_POINT ( 'NONE',  ( 0.3999999999999825917, 3.963633530850413145, 0.9046180958550574802 ) ) ;
#125071=CARTESIAN_POINT ( 'NONE',  ( -1.734723475976807094E-15, 2.999999999999988898, -6.938893903907228378E-15 ) ) ;
#125153=CARTESIAN_POINT ( 'NONE',  ( -5.558564015327489343E-14, 0.4843750003414603600, 1.570758158831762286 ) ) ;
#125172=CARTESIAN_POINT ( 'NONE',  ( -0.6801582343750108839, 2.880208333674722176, -1.178068619123848526 ) ) ;
#125199=ORIENTED_EDGE ( 'NONE', *, *, #138892, .F. ) ;
#125205=B_SPLINE_CURVE_WITH_KNOTS ( 'NONE', 3,
 ( #45781, #114036, #129239, #127095 ),
 .UNSPECIFIED., .F., .F.,
 ( 4, 4 ),
 ( -3.662496629072134259E-08, 0.0006801242851315165375 ),
 .UNSPECIFIED. ) ;
#125290=CARTESIAN_POINT ( 'NONE',  ( -0.4000000000000218936, 3.949999999999960654, 0.8627243683429972609 ) ) ;
#125436=TOROIDAL_SURFACE ( 'NONE', #87313, 1.052419468952678239, 0.9475805310473219834 ) ;
#125461=DIRECTION ( 'NONE',  ( 1.000000000000000000, -7.771561172376097755E-16, -4.440892098500627148E-16 ) ) ;
#125464=CARTESIAN_POINT ( 'NONE',  ( 1.360316468749975582, -0.4635416663252802660, -0.7853790794159301036 ) ) ;
#125472=ADVANCED_FACE ( 'NONE', ( #120453 ), #201596, .T. ) ;
#125570=CARTESIAN_POINT ( 'NONE',  ( -1.360316468750038865, 2.901041667008071645, -0.7853790794159161148 ) ) ;
#125691=CARTESIAN_POINT ( 'NONE',  ( 0.6801582343749813520, 0.2239583336747300035, 1.178068619123796568 ) ) ;
#125724=EDGE_LOOP ( 'NONE', ( #206617, #10354, #123185 ) ) ;
#125736=VERTEX_POINT ( 'NONE', #74834 ) ;
#125798=ORIENTED_EDGE ( 'NONE', *, *, #174533, .F. ) ;
#125880=DIRECTION ( 'NONE',  ( 0.000000000000000000, 0.000000000000000000, 1.000000000000000000 ) ) ;
#125927=CARTESIAN_POINT ( 'NONE',  ( -0.6801582343750265380, 1.463541667008072533, 1.178068619123799898 ) ) ;
#125996=VERTEX_POINT ( 'NONE', #22846 ) ;
#126001=CARTESIAN_POINT ( 'NONE',  ( -3.555477883677943599E-14, 6.828200129012236763E-10, -1.414508159514579644 ) ) ;
#126017=DIRECTION ( 'NONE',  ( -1.000000000000000000, 0.000000000000000000, 4.440892098500751393E-16 ) ) ;
#126044=CARTESIAN_POINT ( 'NONE',  ( -1.224999999999741851, 0.02083333333336212859, 0.7072540797574373705 ) ) ;
#126066=CARTESIAN_POINT ( 'NONE',  ( -0.3999999999999993006, 3.949999999999967315, 0.4999999999999674705 ) ) ;
#126077=CARTESIAN_POINT ( 'NONE',  ( -0.3000000002818530298, 3.198312376128904067, 0.5146719259195894347 ) ) ;
#126125=DIRECTION ( 'NONE',  ( 1.276756478318932585E-15, -1.000000000000000000, 1.665334536937738262E-16 ) ) ;
#126131=CARTESIAN_POINT ( 'NONE',  ( -0.3282377607281391496, 2.011164550367436465, -1.225000000000030287 ) ) ;
#126138=CARTESIAN_POINT ( 'NONE',  ( 1.907519672996875082, 3.236073672982398008, -0.4612874649729831744 ) ) ;
#126151=CARTESIAN_POINT ( 'NONE',  ( -1.734723475976807094E-15, 2.999999999999988898, -6.938893903907228378E-15 ) ) ;
#126218=CARTESIAN_POINT ( 'NONE',  ( -1.360316468750038643, 1.192708333674735721, 0.7853790794158880262 ) ) ;
#126221=ORIENTED_EDGE ( 'NONE', *, *, #167761, .T. ) ;
#126238=CARTESIAN_POINT ( 'NONE',  ( 0.6801582343750022241, 2.838541667008094738, -1.178068619123834759 ) ) ;
#126346=VERTEX_POINT ( 'NONE', #112727 ) ;
#126371=EDGE_LOOP ( 'NONE', ( #196372, #53279, #11974, #130091, #13202, #126221, #41612, #158033 ) ) ;
#126443=CARTESIAN_POINT ( 'NONE',  ( -3.486133158594716510E-16, 2.687500000000001332, -1.225000000000008749 ) ) ;
#126532=CARTESIAN_POINT ( 'NONE',  ( 1.360316468749978469, -0.4843749996586016460, -3.816391647148975608E-14 ) ) ;
#126600=CARTESIAN_POINT ( 'NONE',  ( -1.734723475976807094E-15, 2.999999999999988898, -6.938893903907228378E-15 ) ) ;
#126635=VERTEX_POINT ( 'NONE', #139473 ) ;
#126758=CARTESIAN_POINT ( 'NONE',  ( 0.6801582343749831283, 1.057291667008075642, -1.178068619123862515 ) ) ;
#126766=PLANE ( 'NONE',  #16024 ) ;
#126809=ORIENTED_EDGE ( 'NONE', *, *, #35863, .T. ) ;
#126889=CARTESIAN_POINT ( 'NONE',  ( 0.4999999999999900080, 3.949999999999995293, -0.4000000000000339950 ) ) ;
#126963=TOROIDAL_SURFACE ( 'NONE', #95830, 0.05000000000000000278, 0.05000000000000000278 ) ;
#126975=DIRECTION ( 'NONE',  ( 0.000000000000000000, 1.000000000000000000, -3.330669073875479482E-16 ) ) ;
#126997=CARTESIAN_POINT ( 'NONE',  ( -1.360316468750038643, 1.192708333674735721, 0.7853790794158880262 ) ) ;
#127036=CARTESIAN_POINT ( 'NONE',  ( 0.4999999999999987232, 3.999999999999996447, -0.4499999999999972911 ) ) ;
#127058=ORIENTED_EDGE ( 'NONE', *, *, #103355, .F. ) ;
#127068=CARTESIAN_POINT ( 'NONE',  ( -0.3000000000000085931, 3.372708439410163184, 0.4999999999999657496 ) ) ;
#127095=CARTESIAN_POINT ( 'NONE',  ( -1.772826578343097204, 3.950000000000001954, 0.3999999999999941380 ) ) ;
#127124=ORIENTED_EDGE ( 'NONE', *, *, #145579, .F. ) ;
#127177=CIRCLE ( 'NONE', #165121, 0.04999999999999985706 ) ;
#127192=ORIENTED_EDGE ( 'NONE', *, *, #86559, .F. ) ;
#127195=CARTESIAN_POINT ( 'NONE',  ( -0.3282377607281372622, 1.261164550367456672, -1.225000000000019851 ) ) ;
#127208=CYLINDRICAL_SURFACE ( 'NONE', #15389, 1.224999999999996980 ) ;
#127291=CARTESIAN_POINT ( 'NONE',  ( -1.953008978358306879E-14, 0.2343750003414031002, 1.570758158831794260 ) ) ;
#127454=ORIENTED_EDGE ( 'NONE', *, *, #79113, .F. ) ;
#127561=CARTESIAN_POINT ( 'NONE',  ( -0.4000000000000513700, 3.949999999999967315, 0.8338124244295243015 ) ) ;
#127585=VECTOR ( 'NONE', #83073, 1000.000000000000000 ) ;
#127609=CARTESIAN_POINT ( 'NONE',  ( 0.6124999999999741762, 2.729166667349444797, -1.060881119635955327 ) ) ;
#127646=CARTESIAN_POINT ( 'NONE',  ( -1.981037863234370811, 3.482875600935725569, 0.4617754461038545699 ) ) ;
#127711=CARTESIAN_POINT ( 'NONE',  ( -0.6801582343750420812, 2.713541667008087632, 1.178068619123787908 ) ) ;
#127784=VERTEX_POINT ( 'NONE', #173300 ) ;
#127841=CARTESIAN_POINT ( 'NONE',  ( 1.360316468749980023, 0.01562500034139879812, -2.255140518769849223E-14 ) ) ;
#127856=CARTESIAN_POINT ( 'NONE',  ( 0.3769810270647707684, 3.049942316455285685, -0.4288785890453113980 ) ) ;
#127862=EDGE_LOOP ( 'NONE', ( #179979, #158784, #97647, #131558 ) ) ;
#127956=EDGE_CURVE ( 'NONE', #108115, #184329, #110866, .T. ) ;
#127964=CARTESIAN_POINT ( 'NONE',  ( -1.814759087650030356, 3.975067388631713161, 0.4606438099578192280 ) ) ;
#127997=CARTESIAN_POINT ( 'NONE',  ( 0.3282377607281167786, 1.488835450998188259, -1.225000000000016298 ) ) ;
#128019=CARTESIAN_POINT ( 'NONE',  ( -1.225000000000005640, 2.812500000682796486, -1.734723475976807094E-15 ) ) ;
#128070=CARTESIAN_POINT ( 'NONE',  ( -0.6801582343750282034, 0.4635416670080716450, 1.178068619123793015 ) ) ;
#128105=CARTESIAN_POINT ( 'NONE',  ( 0.6801582343750004478, 2.057291667008069425, -1.178068619123876282 ) ) ;
#128228=EDGE_CURVE ( 'NONE', #138011, #189127, #4902, .T. ) ;
#128232=ORIENTED_EDGE ( 'NONE', *, *, #205195, .T. ) ;
#128235=CYLINDRICAL_SURFACE ( 'NONE', #35670, 0.09999999999999999167 ) ;
#128250=ADVANCED_FACE ( 'NONE', ( #40667 ), #141398, .T. ) ;
#128282=CARTESIAN_POINT ( 'NONE',  ( 0.6124999999999898304, 1.916666666666677621, -1.060881119635962211 ) ) ;
#128364=CARTESIAN_POINT ( 'NONE',  ( -4.757329562667670667E-14, -0.8906249996585621220, -1.570758158831818241 ) ) ;
#128422=CARTESIAN_POINT ( 'NONE',  ( -1.225000000000050271, 2.583333334016200133, 0.7072540797572757221 ) ) ;
#128554=EDGE_LOOP ( 'NONE', ( #91829, #187394, #116021, #177469 ) ) ;
#128560=DIRECTION ( 'NONE',  ( -1.000000000000000000, 7.771561172376094797E-16, -3.330669073875481454E-16 ) ) ;
#128604=SURFACE_STYLE_FILL_AREA ( #129669 ) ;
#128613=CARTESIAN_POINT ( 'NONE',  ( -0.6801582343750108839, 2.880208333674722176, -1.178068619123848526 ) ) ;
#128669=CARTESIAN_POINT ( 'NONE',  ( -1.360316468750002894, -0.6302083329919370147, -0.7853790794158941324 ) ) ;
#128728=ORIENTED_EDGE ( 'NONE', *, *, #35454, .T. ) ;
#128764=CARTESIAN_POINT ( 'NONE',  ( -1.360316468750007779, 2.171875000341411344, -4.336808689942017736E-14 ) ) ;
#128887=CARTESIAN_POINT ( 'NONE',  ( -5.157946788997579689E-14, 1.203125000341463746, 1.570758158831762286 ) ) ;
#128919=DIRECTION ( 'NONE',  ( 3.330669073875478989E-16, -3.540251991789410786E-16, -1.000000000000000000 ) ) ;
#128934=DIRECTION ( 'NONE',  ( -1.276756478318932585E-15, 1.000000000000000000, -1.665334536937738262E-16 ) ) ;
#128936=( BOUNDED_CURVE ( )  B_SPLINE_CURVE ( 2, ( #56821, #75211, #143450, #60021, #174868 ),
 .UNSPECIFIED., .F., .T. ) 
 B_SPLINE_CURVE_WITH_KNOTS ( ( 3, 2, 3 ),
 ( 0.000000000000000000, 0.01041666666666666609, 0.01562500000000013531 ),
 .UNSPECIFIED. ) 
 CURVE ( )  GEOMETRIC_REPRESENTATION_ITEM ( )  RATIONAL_B_SPLINE_CURVE ( ( 1.000000000000000000, 0.8660254037844387076, 1.000000000000000000, 0.9330127018922176330, 0.9330127018922194093 ) ) 
 REPRESENTATION_ITEM ( '' )  );
#129028=CARTESIAN_POINT ( 'NONE',  ( 1.224999999999982991, 0.8749999999999937828, -4.163336342344337027E-14 ) ) ;
#129085=DIRECTION ( 'NONE',  ( 1.276756478318909314E-15, -1.000000000000000000, 0.000000000000000000 ) ) ;
#129131=CARTESIAN_POINT ( 'NONE',  ( 1.360316468749963592, 1.317708333674712184, -0.7853790794158981292 ) ) ;
#129225=EDGE_CURVE ( 'NONE', #62493, #22081, #83831, .T. ) ;
#129239=CARTESIAN_POINT ( 'NONE',  ( -1.889151116980601453, 3.755413325228997401, 0.3999999999999940270 ) ) ;
#129254=LINE ( 'NONE', #96689, #70848 ) ;
#129307=ORIENTED_EDGE ( 'NONE', *, *, #157223, .T. ) ;
#129346=CARTESIAN_POINT ( 'NONE',  ( -0.3282377607281349308, 1.511164550367446235, -1.225000000000023848 ) ) ;
#129416=CARTESIAN_POINT ( 'NONE',  ( -0.4499999960735147075, 3.999999999999974243, 0.9281957781481157133 ) ) ;
#129427=CARTESIAN_POINT ( 'NONE',  ( 1.360316468749959373, -0.4531249996586189654, -4.163336342344337027E-14 ) ) ;
#129633=CARTESIAN_POINT ( 'NONE',  ( 0.6124999999999949374, 1.645833334016133520, 1.060881119635922243 ) ) ;
#129669=FILL_AREA_STYLE ('',( #48350 ) ) ;
#129733=CARTESIAN_POINT ( 'NONE',  ( -0.6801582343750213200, -0.4010416663252705516, -1.178068619123886718 ) ) ;
#129736=CARTESIAN_POINT ( 'NONE',  ( -0.9782388782689256379, 3.999999999999989786, 0.3999999999999559464 ) ) ;
#129832=CARTESIAN_POINT ( 'NONE',  ( 1.360316468749997565, 2.067708333674723953, -0.7853790794159001276 ) ) ;
#129837=EDGE_CURVE ( 'NONE', #5098, #124142, #117806, .T. ) ;
#129878=PLANE ( 'NONE',  #117171 ) ;
#129937=ORIENTED_EDGE ( 'NONE', *, *, #100401, .F. ) ;
#129954=DIRECTION ( 'NONE',  ( -3.330669073875478989E-16, 3.330669073875478989E-16, 1.000000000000000000 ) ) ;
#129959=CARTESIAN_POINT ( 'NONE',  ( 0.6801582343749744686, -0.2760416663252704406, 1.178068619123780802 ) ) ;
#129975=CARTESIAN_POINT ( 'NONE',  ( 0.3782569160206594727, 3.049340702855413365, -0.4285286083246188649 ) ) ;
#130055=DIRECTION ( 'NONE',  ( 0.9692622846690297500, 0.000000000000000000, -0.2460297208025335747 ) ) ;
#130091=ORIENTED_EDGE ( 'NONE', *, *, #82844, .T. ) ;
#130143=CARTESIAN_POINT ( 'NONE',  ( -1.326716514427061987E-15, 2.999999999999988454, -1.225000000000003864 ) ) ;
#130183=CARTESIAN_POINT ( 'NONE',  ( 0.6801582343749917881, 1.255208333674727506, 1.178068619123834759 ) ) ;
#130191=ORIENTED_EDGE ( 'NONE', *, *, #9020, .T. ) ;
#130221=CARTESIAN_POINT ( 'NONE',  ( -0.6801582343750282034, 2.682291667008049441, 1.178068619123805227 ) ) ;
#130396=VECTOR ( 'NONE', #119959, 1000.000000000000000 ) ;
#130401=EDGE_CURVE ( 'NONE', #132173, #78057, #175852, .T. ) ;
#130481=CARTESIAN_POINT ( 'NONE',  ( -1.360316468750034868, 2.619791667008062319, -0.7853790794159261068 ) ) ;
#130571=CIRCLE ( 'NONE', #213486, 0.05000000000000012768 ) ;
#130611=LINE ( 'NONE', #195541, #41921 ) ;
#130707=VERTEX_POINT ( 'NONE', #84541 ) ;
#130780=CARTESIAN_POINT ( 'NONE',  ( -0.6125000000000105915, 1.604166667349450570, 1.060881119635899816 ) ) ;
#130794=CIRCLE ( 'NONE', #123859, 0.09999999999999971412 ) ;
#130813=DIRECTION ( 'NONE',  ( -3.330669073875478989E-16, 3.330669073875478989E-16, 1.000000000000000000 ) ) ;
#130866=ORIENTED_EDGE ( 'NONE', *, *, #35714, .T. ) ;
#130879=CARTESIAN_POINT ( 'NONE',  ( -3.755786496842899057E-14, 1.109375000341423112, -1.570758158831814466 ) ) ;
#130928=CARTESIAN_POINT ( 'NONE',  ( 1.907862554904949492, 3.236716050607333361, 0.4606469147255249919 ) ) ;
#130999=CARTESIAN_POINT ( 'NONE',  ( -0.4032277238576692513, 3.019957635004392404, -0.4115402804778547363 ) ) ;
#131009=CARTESIAN_POINT ( 'NONE',  ( -1.360316468750040642, -0.3802083329919277999, -0.7853790794159161148 ) ) ;
#131043=EDGE_LOOP ( 'NONE', ( #61669, #91288, #197103, #97766, #186324 ) ) ;
#131134=ORIENTED_EDGE ( 'NONE', *, *, #198698, .F. ) ;
#131230=( LENGTH_UNIT ( ) NAMED_UNIT ( * ) SI_UNIT ( .MILLI., .METRE. ) );
#131232=CARTESIAN_POINT ( 'NONE',  ( -0.6801582343750316451, 0.2135416670080853008, 1.178068619123807004 ) ) ;
#131236=AXIS2_PLACEMENT_3D ( 'NONE', #213188, #178587, #194818 ) ;
#131271=CARTESIAN_POINT ( 'NONE',  ( -3.956095110007851991E-14, 2.328125000341396689, -1.570758158831800255 ) ) ;
#131294=CARTESIAN_POINT ( 'NONE',  ( -0.4500000000000302647, 3.949999999999953548, 0.4999999999999553690 ) ) ;
#131350=ORIENTED_EDGE ( 'NONE', *, *, #79132, .F. ) ;
#131390=ORIENTED_EDGE ( 'NONE', *, *, #70626, .F. ) ;
#131434=CARTESIAN_POINT ( 'NONE',  ( -1.225000000000008304, 1.583333334016155503, 0.7072540797572817173 ) ) ;
#131514=CARTESIAN_POINT ( 'NONE',  ( -1.151774525698488676E-14, -0.7656249996585936524, 1.570758158831776052 ) ) ;
#131558=ORIENTED_EDGE ( 'NONE', *, *, #195142, .T. ) ;
#131762=CARTESIAN_POINT ( 'NONE',  ( -1.360316468750026875, 2.671875000341383810, -2.602085213965210642E-14 ) ) ;
#131918=CARTESIAN_POINT ( 'NONE',  ( -1.360316468750021768, 1.421875000341424222, -4.510281037539698445E-14 ) ) ;
#131923=EDGE_LOOP ( 'NONE', ( #165510, #175850, #70452, #168529 ) ) ;
#131963=CARTESIAN_POINT ( 'NONE',  ( 1.224999999999995204, 1.125000000000000888, -2.949029909160572061E-14 ) ) ;
#131968=CYLINDRICAL_SURFACE ( 'NONE', #77851, 1.224999999999996980 ) ;
#131985=CARTESIAN_POINT ( 'NONE',  ( -2.449742653233043743, 3.949999999999981526, -0.4500000000000354272 ) ) ;
#132002=DIRECTION ( 'NONE',  ( 0.000000000000000000, 0.000000000000000000, 1.000000000000000000 ) ) ;
#132048=CARTESIAN_POINT ( 'NONE',  ( -1.360316468750002894, -0.6302083329919370147, -0.7853790794158941324 ) ) ;
#132071=CARTESIAN_POINT ( 'NONE',  ( -3.755786496842897795E-14, 1.703125000341434214, 1.570758158831776052 ) ) ;
#132101=CARTESIAN_POINT ( 'NONE',  ( 1.859587702710796542, 3.245828361968115860, -0.4000000000000271672 ) ) ;
#132160=CARTESIAN_POINT ( 'NONE',  ( -1.902112725515572755, 3.289212146679091120, -0.4096023912812309375 ) ) ;
#132173=VERTEX_POINT ( 'NONE', #40678 ) ;
#132257=CARTESIAN_POINT ( 'NONE',  ( 0.3282377607281153908, 1.238835450998194920, -1.225000000000006972 ) ) ;
#132264=DIRECTION ( 'NONE',  ( -1.000000000000000000, 0.000000000000000000, 2.168404344971007685E-15 ) ) ;
#132267=CARTESIAN_POINT ( 'NONE',  ( -0.6801582343750091075, -1.036458332991943454, 1.178068619123817218 ) ) ;
#132308=CARTESIAN_POINT ( 'NONE',  ( -1.360316468750030650, 0.8697916670080860779, -0.7853790794159041244 ) ) ;
#132370=ORIENTED_EDGE ( 'NONE', *, *, #165324, .T. ) ;
#132379=CARTESIAN_POINT ( 'NONE',  ( 0.3000000000000016542, 4.000000000000003553, -1.007084189318387502 ) ) ;
#132409=VERTEX_POINT ( 'NONE', #155818 ) ;
#132567=CARTESIAN_POINT ( 'NONE',  ( -0.6801582343750004478, 2.598958333674746157, -1.178068619123848526 ) ) ;
#132586=TOROIDAL_SURFACE ( 'NONE', #21814, 1.914481421317583587, 0.05000000000000000278 ) ;
#132607=DIRECTION ( 'NONE',  ( 0.000000000000000000, 0.000000000000000000, -1.000000000000000000 ) ) ;
#132647=CIRCLE ( 'NONE', #42654, 0.05000000000000002359 ) ;
#132754=ORIENTED_EDGE ( 'NONE', *, *, #74123, .F. ) ;
#132790=ORIENTED_EDGE ( 'NONE', *, *, #109534, .F. ) ;
#132874=FACE_OUTER_BOUND ( 'NONE', #147528, .T. ) ;
#132977=CARTESIAN_POINT ( 'NONE',  ( -0.6801582343750265380, 1.463541667008072533, 1.178068619123799898 ) ) ;
#132984=ADVANCED_FACE ( 'NONE', ( #158508 ), #167264, .T. ) ;
#132988=AXIS2_PLACEMENT_3D ( 'NONE', #202602, #171194, #21708 ) ;
#133053=ADVANCED_FACE ( 'NONE', ( #174779 ), #128235, .F. ) ;
#133087=VERTEX_POINT ( 'NONE', #78311 ) ;
#133131=CARTESIAN_POINT ( 'NONE',  ( -1.360316468750004448, 1.640625000341400241, -2.602085213965210642E-14 ) ) ;
#133160=CARTESIAN_POINT ( 'NONE',  ( 1.963827086952127710, 3.753930767994603457, -0.3999999999999195310 ) ) ;
#133203=CARTESIAN_POINT ( 'NONE',  ( 0.6124999999999793943, 2.833333333333354354, 1.060881119635899816 ) ) ;
#133233=DIRECTION ( 'NONE',  ( -1.000000000000000000, 7.771561172376097755E-16, 4.440892098500627148E-16 ) ) ;
#133292=CARTESIAN_POINT ( 'NONE',  ( -1.225000000000011857, 2.770833333333349024, 0.7072540797572636206 ) ) ;
#133312=CARTESIAN_POINT ( 'NONE',  ( -2.324088772396477673E-16, 1.562500000000000666, 1.224999999999980549 ) ) ;
#133333=CARTESIAN_POINT ( 'NONE',  ( -1.360316468750024876, -0.8072916663252578395, 0.7853790794158560518 ) ) ;
#133341=ORIENTED_EDGE ( 'NONE', *, *, #200423, .T. ) ;
#133372=CARTESIAN_POINT ( 'NONE',  ( -0.6801582343750143256, 1.848958333674724397, -1.178068619123862515 ) ) ;
#133490=CARTESIAN_POINT ( 'NONE',  ( 0.4465194593917843902, 3.080450244942134486, 0.4155024747329351120 ) ) ;
#133550=FACE_OUTER_BOUND ( 'NONE', #137740, .T. ) ;
#133570=CYLINDRICAL_SURFACE ( 'NONE', #123328, 1.224999999999996980 ) ;
#133637=CARTESIAN_POINT ( 'NONE',  ( -1.360316468750013108, 1.390625000341414008, -3.469446951953614189E-15 ) ) ;
#133673=CARTESIAN_POINT ( 'NONE',  ( -0.3000000000000241918, 4.000000000000003553, -1.007084189318394385 ) ) ;
#133717=AXIS2_PLACEMENT_3D ( 'NONE', #66257, #17515, #83602 ) ;
#133740=LINE ( 'NONE', #34060, #214106 ) ;
#133780=CARTESIAN_POINT ( 'NONE',  ( -0.4000000000000357714, 3.949999999999981526, -0.5000000000000299760 ) ) ;
#133783=ORIENTED_EDGE ( 'NONE', *, *, #10768, .F. ) ;
#133884=CARTESIAN_POINT ( 'NONE',  ( 1.360316468749961816, 2.026041667008099179, 0.7853790794158520550 ) ) ;
#133908=CARTESIAN_POINT ( 'NONE',  ( 1.224999999999982991, 0.8749999999999937828, -4.163336342344337027E-14 ) ) ;
#133952=CARTESIAN_POINT ( 'NONE',  ( 0.9782388782688978823, 3.999999999999989786, -0.4000000000000097367 ) ) ;
#134050=( BOUNDED_CURVE ( )  B_SPLINE_CURVE ( 3, ( #34383, #66851, #198996, #210991 ),
 .UNSPECIFIED., .F., .T. ) 
 B_SPLINE_CURVE_WITH_KNOTS ( ( 4, 4 ),
 ( 4.712388980384737636, 5.276666415325541593 ),
 .UNSPECIFIED. ) 
 CURVE ( )  GEOMETRIC_REPRESENTATION_ITEM ( )  RATIONAL_B_SPLINE_CURVE ( ( 1.000000000000000000, 0.9736414627471723371, 0.9736414627471723371, 1.000000000000000000 ) ) 
 REPRESENTATION_ITEM ( '' )  );
#134052=CARTESIAN_POINT ( 'NONE',  ( 1.360316468749945606, 0.06770833367471427999, -0.7853790794159161148 ) ) ;
#134076=ORIENTED_EDGE ( 'NONE', *, *, #21017, .F. ) ;
#134087=EDGE_CURVE ( 'NONE', #77834, #160775, #173773, .T. ) ;
#134194=CARTESIAN_POINT ( 'NONE',  ( -1.360316468750042862, 1.869791667008058988, -0.7853790794158961308 ) ) ;
#134267=CYLINDRICAL_SURFACE ( 'NONE', #96489, 0.09999999999999971412 ) ;
#134285=CARTESIAN_POINT ( 'NONE',  ( -1.904329973710263246, 3.286760881231379106, -0.4119279214153201973 ) ) ;
#134303=CARTESIAN_POINT ( 'NONE',  ( -1.907519672996887294, 3.236073672982363369, 0.4612874649729363785 ) ) ;
#134320=CARTESIAN_POINT ( 'NONE',  ( 0.6124999999999707345, 1.395833334016133298, 1.060881119635904923 ) ) ;
#134333=LINE ( 'NONE', #112792, #55216 ) ;
#134360=CARTESIAN_POINT ( 'NONE',  ( 0.4408745273426888933, 3.070687961115777131, 0.4190752896376094827 ) ) ;
#134364=CARTESIAN_POINT ( 'NONE',  ( -3.755786496842897795E-14, -0.3749999993171817536, 1.414508159514569430 ) ) ;
#134400=CARTESIAN_POINT ( 'NONE',  ( 0.6801582343749970061, -0.1614583329919219712, -1.178068619123852079 ) ) ;
#134440=CARTESIAN_POINT ( 'NONE',  ( 1.360316468749969365, 1.036458333674742827, -0.7853790794158820310 ) ) ;
#134464=CARTESIAN_POINT ( 'NONE',  ( -0.3282377607281344867, 0.2611645503674426827, -1.225000000000015410 ) ) ;
#134606=ORIENTED_EDGE ( 'NONE', *, *, #146195, .F. ) ;
#134728=CARTESIAN_POINT ( 'NONE',  ( -0.6125000000000053735, 2.020833334016133964, -1.060881119635941339 ) ) ;
#134733=VERTEX_POINT ( 'NONE', #128019 ) ;
#134847=CARTESIAN_POINT ( 'NONE',  ( 0.4205683736966537856, 3.129384673317387122, -0.4296503687815898531 ) ) ;
#134860=CARTESIAN_POINT ( 'NONE',  ( -0.6125000000000279110, 1.104166667349484765, 1.060881119635904923 ) ) ;
#134936=CARTESIAN_POINT ( 'NONE',  ( -0.6801582343750177673, 1.713541667008065872, 1.178068619123799898 ) ) ;
#134957=CARTESIAN_POINT ( 'NONE',  ( -1.225000000000026068, 1.020833333333308834, 0.7072540797572558491 ) ) ;
#135061=ORIENTED_EDGE ( 'NONE', *, *, #130401, .F. ) ;
#135103=CARTESIAN_POINT ( 'NONE',  ( -1.360316468750018659, 0.6927083336747492659, 0.7853790794158961308 ) ) ;
#135147=CARTESIAN_POINT ( 'NONE',  ( 0.3999999999999923617, 0.6284510210556870646, 1.086836331270357281 ) ) ;
#135224=CARTESIAN_POINT ( 'NONE',  ( -1.225000000000044276, 1.729166666666672292, -0.7072540797572957061 ) ) ;
#135253=CARTESIAN_POINT ( 'NONE',  ( -1.360316468750062846, 1.619791667008073643, -0.7853790794159301036 ) ) ;
#135260=DIRECTION ( 'NONE',  ( -1.276756478318932585E-15, 1.000000000000000000, -1.665334536937738262E-16 ) ) ;
#135300=CARTESIAN_POINT ( 'NONE',  ( -1.387778780781445676E-14, 3.949999999999946443, -1.007084189318404821 ) ) ;
#135320=ORIENTED_EDGE ( 'NONE', *, *, #183389, .T. ) ;
#135325=DIRECTION ( 'NONE',  ( -3.330669073875485398E-16, 1.665334536937734071E-16, 1.000000000000000000 ) ) ;
#135369=PLANE ( 'NONE',  #150711 ) ;
#135401=CARTESIAN_POINT ( 'NONE',  ( -0.4500000000000198286, 3.950000000000009059, 0.8338124244295502807 ) ) ;
#135405=CARTESIAN_POINT ( 'NONE',  ( 0.6124999999999949374, -0.7708333326505306671, -1.060881119635962211 ) ) ;
#135441=CARTESIAN_POINT ( 'NONE',  ( -1.360316468750042862, -0.8489583329918899413, -0.7853790794159322131 ) ) ;
#135470=ADVANCED_FACE ( 'NONE', ( #150576 ), #185169, .T. ) ;
#135482=CARTESIAN_POINT ( 'NONE',  ( 1.360316468749968033, 1.015625000341371820, -4.163336342344337027E-14 ) ) ;
#135548=CARTESIAN_POINT ( 'NONE',  ( 1.814759087649559177, 3.975067388632245624, 0.4606438099578184509 ) ) ;
#135660=AXIS2_PLACEMENT_3D ( 'NONE', #210385, #75070, #95618 ) ;
#135690=DIRECTION ( 'NONE',  ( -5.421010862427532031E-16, 0.5005768354468324022, 0.8656921114426507913 ) ) ;
#135736=DIRECTION ( 'NONE',  ( 1.000000000000000000, 0.000000000000000000, 0.000000000000000000 ) ) ;
#135778=CARTESIAN_POINT ( 'NONE',  ( -1.225000000000008082, 1.583333334016155503, 0.7072540797572817173 ) ) ;
#135803=CARTESIAN_POINT ( 'NONE',  ( -2.449742653233033085, 3.949999999999988187, 0.4499999999999608757 ) ) ;
#135842=DIRECTION ( 'NONE',  ( -1.000000000000000000, 7.771561172376097755E-16, 4.440892098500627148E-16 ) ) ;
#135908=CARTESIAN_POINT ( 'NONE',  ( -0.6125000000000296874, 1.020833334016133076, -1.060881119635955327 ) ) ;
#135923=EDGE_CURVE ( 'NONE', #126346, #72572, #108276, .T. ) ;
#135985=CARTESIAN_POINT ( 'NONE',  ( 0.6801582343749674742, 1.755208333674734833, 1.178068619123803451 ) ) ;
#136009=CARTESIAN_POINT ( 'NONE',  ( -2.954552044183079750E-14, 1.312499999999982236, 1.414508159514555441 ) ) ;
#136043=ORIENTED_EDGE ( 'NONE', *, *, #81270, .F. ) ;
#136051=DIRECTION ( 'NONE',  ( 1.276756478318931402E-15, -1.000000000000000000, 0.000000000000000000 ) ) ;
#136152=ORIENTED_EDGE ( 'NONE', *, *, #35341, .T. ) ;
#136190=ORIENTED_EDGE ( 'NONE', *, *, #207277, .F. ) ;
#136209=CARTESIAN_POINT ( 'NONE',  ( 0.3282377607281186660, 1.176335450315366460, -1.225000000000014522 ) ) ;
#136279=CARTESIAN_POINT ( 'NONE',  ( -1.734723475976807094E-15, 2.999999999999988898, -6.938893903907228378E-15 ) ) ;
#136310=CARTESIAN_POINT ( 'NONE',  ( -0.6801582343750143256, 1.848958333674724397, -1.178068619123862515 ) ) ;
#136377=ORIENTED_EDGE ( 'NONE', *, *, #83031, .F. ) ;
#136471=CARTESIAN_POINT ( 'NONE',  ( -0.3282377607281363741, 0.1986645496846400905, -1.225000000000038725 ) ) ;
#136474=CARTESIAN_POINT ( 'NONE',  ( -0.6125000000000089262, -0.1458333326505162342, 1.060881119635894487 ) ) ;
#136485=ORIENTED_EDGE ( 'NONE', *, *, #209073, .T. ) ;
#136510=CARTESIAN_POINT ( 'NONE',  ( 0.6801582343749970061, -0.4947916663252532876, 1.178068619123832983 ) ) ;
#136550=CARTESIAN_POINT ( 'NONE',  ( 0.6801582343749744686, 0.4739583336747441034, 1.178068619123803451 ) ) ;
#136576=( BOUNDED_CURVE ( )  B_SPLINE_CURVE ( 3, ( #181866, #81192, #163516, #48703 ),
 .UNSPECIFIED., .F., .T. ) 
 B_SPLINE_CURVE_WITH_KNOTS ( ( 4, 4 ),
 ( 1.570796326795016462, 3.141592653589631468 ),
 .UNSPECIFIED. ) 
 CURVE ( )  GEOMETRIC_REPRESENTATION_ITEM ( )  RATIONAL_B_SPLINE_CURVE ( ( 1.000000000000000000, 0.8047378541244312178, 0.8047378541244312178, 1.000000000000000000 ) ) 
 REPRESENTATION_ITEM ( '' )  );
#136758=CYLINDRICAL_SURFACE ( 'NONE', #67673, 1.224999999999996980 ) ;
#136759=EDGE_CURVE ( 'NONE', #195016, #86803, #167615, .T. ) ;
#136837=CARTESIAN_POINT ( 'NONE',  ( -1.225000000000042277, 0.9791666666666766217, -0.7072540797572898219 ) ) ;
#136844=CARTESIAN_POINT ( 'NONE',  ( 1.224999999999976996, 1.666666667349515851, 0.7072540797572517413 ) ) ;
#136850=ORIENTED_EDGE ( 'NONE', *, *, #159917, .T. ) ;
#136874=ORIENTED_EDGE ( 'NONE', *, *, #83130, .T. ) ;
#136893=DIRECTION ( 'NONE',  ( 3.330669073875478989E-16, -3.540251991789410786E-16, -1.000000000000000000 ) ) ;
#136922=DIRECTION ( 'NONE',  ( 1.000000000000000000, -7.771561172376097755E-16, -4.440892098500627148E-16 ) ) ;
#136948=ADVANCED_FACE ( 'NONE', ( #34401 ), #100473, .T. ) ;
#137003=CARTESIAN_POINT ( 'NONE',  ( -1.225000000000038058, 2.270833333333395210, 0.7072540797572858251 ) ) ;
#137055=CARTESIAN_POINT ( 'NONE',  ( -0.6801582343750229853, 1.380208333674720622, -1.178068619123855409 ) ) ;
#137077=CARTESIAN_POINT ( 'NONE',  ( 1.224999999999974998, 0.6041666666666989371, 0.7072540797572456350 ) ) ;
#137088=EDGE_CURVE ( 'NONE', #56038, #141384, #109606, .T. ) ;
#137195=CARTESIAN_POINT ( 'NONE',  ( 0.4999999999999605316, 3.999999999999989786, 0.3999999999999611644 ) ) ;
#137236=CARTESIAN_POINT ( 'NONE',  ( 0.6801582343749726922, 0.7552083336747339448, 1.178068619123784355 ) ) ;
#137381=CARTESIAN_POINT ( 'NONE',  ( 1.360316468749988683, 0.2656250003413990202, -1.387778780781445676E-14 ) ) ;
#137399=AXIS2_PLACEMENT_3D ( 'NONE', #170722, #8216, #154487 ) ;
#137445=ORIENTED_EDGE ( 'NONE', *, *, #159917, .F. ) ;
#137453=CARTESIAN_POINT ( 'NONE',  ( -1.225000000000026512, 1.750000000000015543, -1.734723475976807094E-14 ) ) ;
#137460=ADVANCED_FACE ( 'NONE', ( #51224 ), #198510, .T. ) ;
#137543=CARTESIAN_POINT ( 'NONE',  ( -0.6125000000000105915, -0.4791666659838753062, -1.060881119635955327 ) ) ;
#137562=ORIENTED_EDGE ( 'NONE', *, *, #118912, .T. ) ;
#137612=CARTESIAN_POINT ( 'NONE',  ( 0.6801582343749761339, 1.973958333674710630, 1.178068619123801675 ) ) ;
#137620=CARTESIAN_POINT ( 'NONE',  ( -2.754243431018125239E-14, 0.2031250003414269978, 1.570758158831750295 ) ) ;
#137664=EDGE_LOOP ( 'NONE', ( #211411, #107629, #44805, #89076, #209103, #15992, #188091 ) ) ;
#137685=CARTESIAN_POINT ( 'NONE',  ( -0.3000000000000051514, 3.322650755865477645, -0.5865692111443002732 ) ) ;
#137740=EDGE_LOOP ( 'NONE', ( #130866, #84408, #99103, #80360 ) ) ;
#137780=VERTEX_POINT ( 'NONE', #93869 ) ;
#137817=FACE_OUTER_BOUND ( 'NONE', #125724, .T. ) ;
#137875=EDGE_LOOP ( 'NONE', ( #121461, #145915, #3409, #23916 ) ) ;
#137888=DIRECTION ( 'NONE',  ( -4.440892098500630106E-16, -3.330669073875473073E-16, -1.000000000000000000 ) ) ;
#137915=CARTESIAN_POINT ( 'NONE',  ( -1.225000000000056044, 1.291666667349482100, -0.7072540797573317883 ) ) ;
#137969=DIRECTION ( 'NONE',  ( -3.330669073875478989E-16, 3.330669073875478989E-16, 1.000000000000000000 ) ) ;
#137977=DIRECTION ( 'NONE',  ( 0.000000000000000000, 0.000000000000000000, -1.000000000000000000 ) ) ;
#137979=DIRECTION ( 'NONE',  ( 4.440892098500630106E-16, 3.330669073875473073E-16, 1.000000000000000000 ) ) ;
#138011=VERTEX_POINT ( 'NONE', #113364 ) ;
#138027=CARTESIAN_POINT ( 'NONE',  ( -0.3782569160207209791, 3.049340702855438234, 0.4285286083245324895 ) ) ;
#138056=CARTESIAN_POINT ( 'NONE',  ( 0.3978093821460517154, 3.011896635411783762, 0.3978093821460513824 ) ) ;
#138069=CARTESIAN_POINT ( 'NONE',  ( -1.292658234375014592, 2.960937500170686576, -3.295974604355933479E-14 ) ) ;
#138098=EDGE_CURVE ( 'NONE', #140828, #62036, #80795, .T. ) ;
#138102=ORIENTED_EDGE ( 'NONE', *, *, #140329, .T. ) ;
#138127=CARTESIAN_POINT ( 'NONE',  ( 1.360316468749987129, 1.796875000341410900, -3.295974604355933479E-14 ) ) ;
#138149=CARTESIAN_POINT ( 'NONE',  ( 1.225000000000010747, 0.3749999999999864553, -2.081668171172168513E-14 ) ) ;
#138244=CARTESIAN_POINT ( 'NONE',  ( 0.3282377607281227738, 2.636164550367435133, 1.224999999999981659 ) ) ;
#138295=MECHANICAL_DESIGN_GEOMETRIC_PRESENTATION_REPRESENTATION('',(#210933),#72549);
#138298=CARTESIAN_POINT ( 'NONE',  ( 1.360316468749973140, 0.5468750003413819227, -2.081668171172168513E-14 ) ) ;
#138357=CARTESIAN_POINT ( 'NONE',  ( 0.6124999999999655165, 0.08333333333334497217, 1.060881119635885828 ) ) ;
#138414=CARTESIAN_POINT ( 'NONE',  ( -0.4379653042624916948, 3.065656782498161537, 0.4195809500673950421 ) ) ;
#138446=CARTESIAN_POINT ( 'NONE',  ( -0.6801582343750161019, 0.6822916670080614310, 1.178068619123810334 ) ) ;
#138515=CARTESIAN_POINT ( 'NONE',  ( -0.6125000000000349054, 2.208333333333325932, -1.060881119635983083 ) ) ;
#138561=CARTESIAN_POINT ( 'NONE',  ( 0.9630212455657579662, -7.887518224194900737E-15, -0.8538729164882093992 ) ) ;
#138580=EDGE_LOOP ( 'NONE', ( #103059, #72594, #115040, #2616 ) ) ;
#138594=EDGE_CURVE ( 'NONE', #21883, #87431, #141213, .T. ) ;
#138606=CARTESIAN_POINT ( 'NONE',  ( 1.224999999999974998, -0.3333333326504774874, 0.7072540797572697269 ) ) ;
#138610=CARTESIAN_POINT ( 'NONE',  ( -0.3000000000000097589, 3.214163249644239606, 0.5238375172406791735 ) ) ;
#138667=( GEOMETRIC_REPRESENTATION_CONTEXT ( 3 ) GLOBAL_UNCERTAINTY_ASSIGNED_CONTEXT ( ( #147173 ) ) GLOBAL_UNIT_ASSIGNED_CONTEXT ( ( #131230, #68265, #33653 ) ) REPRESENTATION_CONTEXT ( 'NONE', 'WORKASPACE' ) );
#138677=CARTESIAN_POINT ( 'NONE',  ( 1.360316468749943608, 1.494791667008105174, 0.7853790794158439503 ) ) ;
#138706=AXIS2_PLACEMENT_3D ( 'NONE', #115413, #51419, #99109 ) ;
#138750=CARTESIAN_POINT ( 'NONE',  ( 1.981451431469405389, 3.479816182765795851, 0.4617787996151190288 ) ) ;
#138823=EDGE_CURVE ( 'NONE', #34023, #75994, #86100, .T. ) ;
#138885=CARTESIAN_POINT ( 'NONE',  ( 0.3282377607281121712, 1.426335450315397102, -1.225000000000027400 ) ) ;
#138887=CARTESIAN_POINT ( 'NONE',  ( 0.3282377607281144472, 0.3236645496846485281, 1.224999999999966116 ) ) ;
#138892=EDGE_CURVE ( 'NONE', #15383, #170783, #83718, .T. ) ;
#138909=CARTESIAN_POINT ( 'NONE',  ( -0.6801582343750125492, 2.213541667008059211, 1.178068619123818994 ) ) ;
#138989=CARTESIAN_POINT ( 'NONE',  ( 1.224999999999989875, 0.4375000006828014265, -4.510281037539698445E-14 ) ) ;
#139105=CARTESIAN_POINT ( 'NONE',  ( -3.035961785846409301E-14, 2.999999999999988454, -1.857347330825986687 ) ) ;
#139190=CARTESIAN_POINT ( 'NONE',  ( 1.360316468749980023, 0.7968750003414099004, -3.122502256758252770E-14 ) ) ;
#139211=CARTESIAN_POINT ( 'NONE',  ( -7.761958760141988650E-14, -0.3124999999999614197, -1.414508159514597407 ) ) ;
#139250=ORIENTED_EDGE ( 'NONE', *, *, #79113, .T. ) ;
#139305=DIRECTION ( 'NONE',  ( -1.276756478318932585E-15, 1.000000000000000000, -1.665334536937738262E-16 ) ) ;
#139427=CARTESIAN_POINT ( 'NONE',  ( 1.224999999999943023, 2.645833333333332593, -0.7072540797573158011 ) ) ;
#139443=CARTESIAN_POINT ( 'NONE',  ( 6.972266317189433020E-16, 0.5000000006828014820, -1.225000000000012745 ) ) ;
#139473=CARTESIAN_POINT ( 'NONE',  ( 2.324088772396477673E-16, 0.6875000000000069944, -1.225000000000008749 ) ) ;
#139477=VERTEX_POINT ( 'NONE', #164978 ) ;
#139519=CARTESIAN_POINT ( 'NONE',  ( 1.360316468749980023, 0.01562500034139879812, -2.255140518769849223E-14 ) ) ;
#139521=CARTESIAN_POINT ( 'NONE',  ( -0.4000000000000218936, 2.999999999999988898, 0.3999999999999819811 ) ) ;
#139585=ORIENTED_EDGE ( 'NONE', *, *, #191715, .T. ) ;
#139593=CARTESIAN_POINT ( 'NONE',  ( -1.225000000000038058, 2.270833333333394766, 0.7072540797572857141 ) ) ;
#139653=EDGE_CURVE ( 'NONE', #104013, #211691, #201718, .T. ) ;
#139703=DIRECTION ( 'NONE',  ( -1.000000000000000000, 7.771561172376097755E-16, 4.440892098500627148E-16 ) ) ;
#139719=ADVANCED_FACE ( 'NONE', ( #21891 ), #136758, .T. ) ;
#139755=CARTESIAN_POINT ( 'NONE',  ( 1.360316468749953600, 1.786458333674746601, -0.7853790794159161148 ) ) ;
#139883=EDGE_CURVE ( 'NONE', #190021, #44750, #206001, .T. ) ;
#139923=AXIS2_PLACEMENT_3D ( 'NONE', #88040, #166087, #135736 ) ;
#139927=DIRECTION ( 'NONE',  ( -5.828670879282089587E-16, 0.8656921114426507913, -0.5005768354468322912 ) ) ;
#139937=DIRECTION ( 'NONE',  ( 1.276756478318932585E-15, -1.000000000000000000, 1.665334536937738262E-16 ) ) ;
#139964=CARTESIAN_POINT ( 'NONE',  ( 1.225000000000010747, 0.3749999999999864553, -2.081668171172168513E-14 ) ) ;
#139987=CARTESIAN_POINT ( 'NONE',  ( -1.360316468750036645, 2.151041667008108060, -0.7853790794159301036 ) ) ;
#140019=ORIENTED_EDGE ( 'NONE', *, *, #67872, .T. ) ;
#140065=CARTESIAN_POINT ( 'NONE',  ( -0.6125000000000296874, 1.020833334016133076, -1.060881119635955327 ) ) ;
#140121=CARTESIAN_POINT ( 'NONE',  ( -0.3282377607281349308, 1.448664549684643310, -1.225000000000014522 ) ) ;
#140280=CARTESIAN_POINT ( 'NONE',  ( -1.906201616980850222, 3.231688558335370054, -0.4612787108932971392 ) ) ;
#140283=CARTESIAN_POINT ( 'NONE',  ( -1.360316468750032204, 0.6718750003414097893, -2.081668171172168513E-14 ) ) ;
#140306=CARTESIAN_POINT ( 'NONE',  ( -0.6125000000000262457, -0.7916666666666349883, -1.060881119635962211 ) ) ;
#140322=VERTEX_POINT ( 'NONE', #54387 ) ;
#140329=EDGE_CURVE ( 'NONE', #75836, #140322, #188643, .T. ) ;
#140420=VECTOR ( 'NONE', #70059, 1000.000000000000114 ) ;
#140607=CARTESIAN_POINT ( 'NONE',  ( 1.360316468749969809, 0.7447916670080856338, 0.7853790794158741484 ) ) ;
#140609=DIRECTION ( 'NONE',  ( 1.276756478318932191E-15, -1.000000000000000000, 3.330669073875483426E-16 ) ) ;
#140673=ORIENTED_EDGE ( 'NONE', *, *, #192933, .T. ) ;
#140675=CARTESIAN_POINT ( 'NONE',  ( 1.224999999999974332, 2.374999999999988454, -3.295974604355933479E-14 ) ) ;
#140711=CARTESIAN_POINT ( 'NONE',  ( -4.356712336337761644E-14, 2.859375000341351392, -1.570758158831810247 ) ) ;
#140828=VERTEX_POINT ( 'NONE', #205954 ) ;
#140832=CARTESIAN_POINT ( 'NONE',  ( -0.6801582343750282034, 1.432291667008027458, 1.178068619123810334 ) ) ;
#140841=CARTESIAN_POINT ( 'NONE',  ( -0.6801582343750334214, 0.1822916670080609869, 1.178068619123799898 ) ) ;
#140848=CARTESIAN_POINT ( 'NONE',  ( -1.907519672996887294, 3.236073672982363369, 0.4612874649729363785 ) ) ;
#140864=CARTESIAN_POINT ( 'NONE',  ( 1.911175648939841265, 3.243131119507678850, -0.4542559028653492814 ) ) ;
#140890=CARTESIAN_POINT ( 'NONE',  ( 0.3000000000000016542, 3.322650755865477645, 0.5865692111442620815 ) ) ;
#141010=VERTEX_POINT ( 'NONE', #196621 ) ;
#141051=ORIENTED_EDGE ( 'NONE', *, *, #213886, .F. ) ;
#141066=CARTESIAN_POINT ( 'NONE',  ( 4.996790860652426159E-15, 0.6250000006827882704, 1.224999999999976330 ) ) ;
#141068=CARTESIAN_POINT ( 'NONE',  ( -0.6801582343750438575, 1.630208333674734611, -1.178068619123879834 ) ) ;
#141152=CARTESIAN_POINT ( 'NONE',  ( 1.224999999999969225, 0.6875000006828015930, -3.642919299551294898E-14 ) ) ;
#141213=( BOUNDED_CURVE ( )  B_SPLINE_CURVE ( 2, ( #206250, #190004, #104505, #137003, #57876, #8045, #22133, #88246, #41654 ),
 .UNSPECIFIED., .F., .T. ) 
 B_SPLINE_CURVE_WITH_KNOTS ( ( 3, 2, 2, 2, 3 ),
 ( 0.1718749999999998335, 0.1770833333333333426, 0.1875000000000000000, 0.1979166666666666574, 0.2031250000000001388 ),
 .UNSPECIFIED. ) 
 CURVE ( )  GEOMETRIC_REPRESENTATION_ITEM ( )  RATIONAL_B_SPLINE_CURVE ( ( 0.9330127018922194093, 0.9330127018922171889, 1.000000000000000000, 0.8660254037844387076, 1.000000000000000000, 0.8660254037844387076, 1.000000000000000000, 0.9330127018922176330, 0.9330127018922194093 ) ) 
 REPRESENTATION_ITEM ( '' )  );
#141226=CARTESIAN_POINT ( 'NONE',  ( -0.4000000000000343836, 3.372708439410141867, 0.4999999999999770184 ) ) ;
#141244=CARTESIAN_POINT ( 'NONE',  ( 2.324088772396477673E-16, 0.6875000000000069944, -1.225000000000008749 ) ) ;
#141258=CARTESIAN_POINT ( 'NONE',  ( 0.3544712801348807729, 3.975028838742734383, 0.9637995819944042974 ) ) ;
#141364=CARTESIAN_POINT ( 'NONE',  ( -7.511572993685796537E-15, 0.3593750003414036831, -1.570758158831792262 ) ) ;
#141384=VERTEX_POINT ( 'NONE', #188374 ) ;
#141387=CARTESIAN_POINT ( 'NONE',  ( 0.6124999999999862776, -0.6666666666666556385, 1.060881119635903147 ) ) ;
#141398=CYLINDRICAL_SURFACE ( 'NONE', #52841, 0.1000000000000000472 ) ;
#141435=AXIS2_PLACEMENT_3D ( 'NONE', #46182, #175116, #97071 ) ;
#141646=DIRECTION ( 'NONE',  ( 0.5131086435338283458, 0.8583236685137343169, -5.551115123125796507E-16 ) ) ;
#141675=CARTESIAN_POINT ( 'NONE',  ( -1.360316468749999119, 0.3906250003414130090, -8.673617379884035472E-15 ) ) ;
#141734=( GEOMETRIC_REPRESENTATION_CONTEXT ( 3 ) GLOBAL_UNCERTAINTY_ASSIGNED_CONTEXT ( ( #33171 ) ) GLOBAL_UNIT_ASSIGNED_CONTEXT ( ( #177270, #63515, #14741 ) ) REPRESENTATION_CONTEXT ( 'NONE', 'WORKASPACE' ) );
#141746=CARTESIAN_POINT ( 'NONE',  ( 0.6124999999999914957, 2.083333333333339699, 1.060881119635884051 ) ) ;
#141808=( BOUNDED_CURVE ( )  B_SPLINE_CURVE ( 2, ( #166567, #51760, #67956, #149246, #148194, #34419, #35485, #66888, #819 ),
 .UNSPECIFIED., .F., .T. ) 
 B_SPLINE_CURVE_WITH_KNOTS ( ( 3, 2, 2, 2, 3 ),
 ( 0.4843749999999997780, 0.4895833333333333148, 0.5000000000000000000, 0.5104166666666666297, 0.5156250000000002220 ),
 .UNSPECIFIED. ) 
 CURVE ( )  GEOMETRIC_REPRESENTATION_ITEM ( )  RATIONAL_B_SPLINE_CURVE ( ( 0.9330127018922194093, 0.9330127018922165227, 1.000000000000000000, 0.8660254037844387076, 1.000000000000000000, 0.8660254037844387076, 1.000000000000000000, 0.9330127018922165227, 0.9330127018922194093 ) ) 
 REPRESENTATION_ITEM ( '' )  );
#141897=EDGE_CURVE ( 'NONE', #144032, #201878, #49285, .T. ) ;
#141900=CARTESIAN_POINT ( 'NONE',  ( 1.360316468749985575, 0.2864583336747233422, -0.7853790794158961308 ) ) ;
#141931=CARTESIAN_POINT ( 'NONE',  ( 1.907519672996875082, 3.236073672982398008, -0.4612874649729831744 ) ) ;
#141972=DIRECTION ( 'NONE',  ( 1.000000000000000000, -7.771561172376097755E-16, -4.440892098500627148E-16 ) ) ;
#141990=EDGE_LOOP ( 'NONE', ( #68405, #131390, #69494, #176639 ) ) ;
#142028=DIRECTION ( 'NONE',  ( -3.330669073875479482E-16, 3.330669073875479482E-16, 1.000000000000000000 ) ) ;
#142099=ORIENTED_EDGE ( 'NONE', *, *, #174390, .F. ) ;
#142109=ORIENTED_EDGE ( 'NONE', *, *, #158235, .T. ) ;
#142125=CARTESIAN_POINT ( 'NONE',  ( -3.755786496842897795E-14, 2.609375000341406459, -1.570758158831778273 ) ) ;
#142202=CARTESIAN_POINT ( 'NONE',  ( 0.6124999999999707345, 0.7291666673494984208, -1.060881119635972647 ) ) ;
#142218=( BOUNDED_CURVE ( )  B_SPLINE_CURVE ( 2, ( #124005, #108801, #128282, #192091, #27474, #93572, #159617, #156425, #11214 ),
 .UNSPECIFIED., .F., .T. ) 
 B_SPLINE_CURVE_WITH_KNOTS ( ( 3, 2, 2, 2, 3 ),
 ( 0.2656250000000002220, 0.2708333333333333148, 0.2812500000000000000, 0.2916666666666666852, 0.2968749999999998335 ),
 .UNSPECIFIED. ) 
 CURVE ( )  GEOMETRIC_REPRESENTATION_ITEM ( )  RATIONAL_B_SPLINE_CURVE ( ( 0.9330127018922194093, 0.9330127018922221849, 1.000000000000000000, 0.8660254037844387076, 1.000000000000000000, 0.8660254037844387076, 1.000000000000000000, 0.9330127018922215187, 0.9330127018922194093 ) ) 
 REPRESENTATION_ITEM ( '' )  );
#142307=ADVANCED_FACE ( 'NONE', ( #97854 ), #133570, .T. ) ;
#142315=CARTESIAN_POINT ( 'NONE',  ( 0.3645075752534430724, 4.000000000000008882, 0.9782388703846671696 ) ) ;
#142329=FACE_OUTER_BOUND ( 'NONE', #131923, .T. ) ;
#142336=DIRECTION ( 'NONE',  ( 1.276756478318932585E-15, -1.000000000000000000, 1.665334536937738262E-16 ) ) ;
#142357=FACE_OUTER_BOUND ( 'NONE', #170186, .T. ) ;
#142419=CARTESIAN_POINT ( 'NONE',  ( -1.360316468750056851, 0.6510416670080609869, -0.7853790794158981292 ) ) ;
#142441=CARTESIAN_POINT ( 'NONE',  ( -1.225000000000042277, -0.9791666666666447583, 0.7072540797572656190 ) ) ;
#142530=AXIS2_PLACEMENT_3D ( 'NONE', #211779, #115425, #98070 ) ;
#142570=VERTEX_POINT ( 'NONE', #106981 ) ;
#142613=ORIENTED_EDGE ( 'NONE', *, *, #158235, .F. ) ;
#142693=EDGE_LOOP ( 'NONE', ( #67795, #62503, #212497, #158810 ) ) ;
#142733=CARTESIAN_POINT ( 'NONE',  ( 0.6801582343749674742, -0.4427083329919187515, -1.178068619123886718 ) ) ;
#142742=DIRECTION ( 'NONE',  ( 1.000000000000000000, -7.771561172376097755E-16, -4.440892098500627148E-16 ) ) ;
#142838=CARTESIAN_POINT ( 'NONE',  ( -1.360316468750006669, 2.442708333674733723, 0.7853790794158861388 ) ) ;
#142841=ORIENTED_EDGE ( 'NONE', *, *, #177464, .T. ) ;
#142964=CARTESIAN_POINT ( 'NONE',  ( 1.360316468750000896, 0.7656250003413994643, 0.000000000000000000 ) ) ;
#142985=CARTESIAN_POINT ( 'NONE',  ( 1.360316468749997565, 2.744791667008062763, 0.7853790794158921340 ) ) ;
#143002=ORIENTED_EDGE ( 'NONE', *, *, #88639, .T. ) ;
#143043=CARTESIAN_POINT ( 'NONE',  ( 1.224999999999979217, 0.2083333340161329650, -0.7072540797572937077 ) ) ;
#143067=CARTESIAN_POINT ( 'NONE',  ( 1.772826578343088544, 3.950000000000001954, -0.4500000000000284883 ) ) ;
#143124=FACE_OUTER_BOUND ( 'NONE', #79520, .T. ) ;
#143206=CARTESIAN_POINT ( 'NONE',  ( -0.6801582343750420812, 1.880208333674727950, -1.178068619123883165 ) ) ;
#143216=CARTESIAN_POINT ( 'NONE',  ( -5.810221930991193690E-16, 2.500000000682804036, -1.225000000000023626 ) ) ;
#143239=CARTESIAN_POINT ( 'NONE',  ( -1.360316468750010666, 2.869791667008063207, -0.7853790794158961308 ) ) ;
#143294=VERTEX_POINT ( 'NONE', #168453 ) ;
#143360=CARTESIAN_POINT ( 'NONE',  ( -5.204170427930421283E-14, 3.949999999999960654, -4.683753385137379155E-14 ) ) ;
#143369=DIRECTION ( 'NONE',  ( -1.000000000000000000, 7.771561172376097755E-16, 4.440892098500627148E-16 ) ) ;
#143450=CARTESIAN_POINT ( 'NONE',  ( -0.6125000000000123679, 2.958333333333326820, -1.060881119635965764 ) ) ;
#143457=ORIENTED_EDGE ( 'NONE', *, *, #13041, .F. ) ;
#143494=CARTESIAN_POINT ( 'NONE',  ( 0.6801582343749726922, 0.7552083336747339448, 1.178068619123784355 ) ) ;
#143539=CARTESIAN_POINT ( 'NONE',  ( 2.007420792093927986E-08, -6.938893903907228378E-15, -1.225000000000033396 ) ) ;
#143712=CYLINDRICAL_SURFACE ( 'NONE', #141435, 0.09999999999999971412 ) ;
#143810=CARTESIAN_POINT ( 'NONE',  ( -5.758872628492444169E-14, -0.1718749996585747786, -1.570758158831818241 ) ) ;
#143824=ORIENTED_EDGE ( 'NONE', *, *, #39783, .F. ) ;
#143913=CARTESIAN_POINT ( 'NONE',  ( -6.760415694317216410E-14, 2.234375000341476625, 1.570758158831744300 ) ) ;
#143962=CARTESIAN_POINT ( 'NONE',  ( 1.913201741516640464, 3.249623237789940333, 0.4478572873796038967 ) ) ;
#144032=VERTEX_POINT ( 'NONE', #159677 ) ;
#144036=CARTESIAN_POINT ( 'NONE',  ( -3.355169270512988773E-14, 0.9531250003414385441, 1.570758158831740303 ) ) ;
#144052=B_SPLINE_CURVE_WITH_KNOTS ( 'NONE', 3,
 ( #107360, #59606, #8717, #42318 ),
 .UNSPECIFIED., .F., .F.,
 ( 4, 4 ),
 ( 0.000000000000000000, 2.032232339065676875E-05 ),
 .UNSPECIFIED. ) ;
#144113=DIRECTION ( 'NONE',  ( -1.276756478318932585E-15, 1.000000000000000000, -1.665334536937738262E-16 ) ) ;
#144139=AXIS2_PLACEMENT_3D ( 'NONE', #68042, #85392, #31326 ) ;
#144161=CARTESIAN_POINT ( 'NONE',  ( -1.963827086952256051, 3.753930767994497764, 0.3999999999999835909 ) ) ;
#144277=CARTESIAN_POINT ( 'NONE',  ( 1.360316468749989793, 0.8177083336747339448, -0.7853790794159001276 ) ) ;
#144312=CARTESIAN_POINT ( 'NONE',  ( -1.360316468750008667, 2.369791667008076974, -0.7853790794159001276 ) ) ;
#144432=ORIENTED_EDGE ( 'NONE', *, *, #119884, .F. ) ;
#144462=EDGE_LOOP ( 'NONE', ( #144758, #136874, #37097, #23067 ) ) ;
#144563=CARTESIAN_POINT ( 'NONE',  ( -3.956095110007852622E-14, -0.1406249996585586248, -1.570758158831808249 ) ) ;
#144578=CARTESIAN_POINT ( 'NONE',  ( 0.4170821662628915183, 3.033599471985643170, 0.4170821662628724225 ) ) ;
#144758=ORIENTED_EDGE ( 'NONE', *, *, #171547, .F. ) ;
#144776=CARTESIAN_POINT ( 'NONE',  ( 0.6124999999999707345, 1.729166667349485431, -1.060881119635955327 ) ) ;
#144822=CYLINDRICAL_SURFACE ( 'NONE', #33603, 1.224999999999996980 ) ;
#144872=CARTESIAN_POINT ( 'NONE',  ( 0.6801582343749865700, -1.026041666325229418, 1.178068619123805227 ) ) ;
#144876=ADVANCED_FACE ( 'NONE', ( #98654 ), #164710, .T. ) ;
#144905=EDGE_CURVE ( 'NONE', #140322, #62112, #130571, .T. ) ;
#144967=CARTESIAN_POINT ( 'NONE',  ( -2.353626204688216217E-14, 0.9843750003414547534, 1.570758158831764062 ) ) ;
#144969=EDGE_CURVE ( 'NONE', #45585, #16624, #94411, .T. ) ;
#144993=EDGE_CURVE ( 'NONE', #55379, #160775, #127177, .T. ) ;
#145020=CARTESIAN_POINT ( 'NONE',  ( 1.899436509991797584, 3.291494839451057253, 0.4074537448169641696 ) ) ;
#145048=EDGE_CURVE ( 'NONE', #211691, #170783, #159498, .T. ) ;
#145098=CARTESIAN_POINT ( 'NONE',  ( -1.552391752028397856E-14, -0.04687499965855816686, 1.570758158831750295 ) ) ;
#145118=CARTESIAN_POINT ( 'NONE',  ( 1.360316468749992236, 2.765625000341414896, -4.683753385137379155E-14 ) ) ;
#145132=AXIS2_PLACEMENT_3D ( 'NONE', #99715, #13125, #111777 ) ;
#145178=AXIS2_PLACEMENT_3D ( 'NONE', #196813, #96146, #30056 ) ;
#145218=CARTESIAN_POINT ( 'NONE',  ( -1.826099658463393061, 3.981846818257626541, 0.3999999999999835354 ) ) ;
#145336=CARTESIAN_POINT ( 'NONE',  ( -2.353626204688216217E-14, 0.1093750003414345612, -1.570758158831782270 ) ) ;
#145361=( BOUNDED_CURVE ( )  B_SPLINE_CURVE ( 3, ( #207829, #123496, #172157, #56270 ),
 .UNSPECIFIED., .F., .T. ) 
 B_SPLINE_CURVE_WITH_KNOTS ( ( 4, 4 ),
 ( 4.712388980384695003, 5.276666415325903969 ),
 .UNSPECIFIED. ) 
 CURVE ( )  GEOMETRIC_REPRESENTATION_ITEM ( )  RATIONAL_B_SPLINE_CURVE ( ( 1.000000000000000000, 0.9736414627471347005, 0.9736414627471347005, 1.000000000000000000 ) ) 
 REPRESENTATION_ITEM ( '' )  );
#145377=CARTESIAN_POINT ( 'NONE',  ( -1.360316468749998675, 2.411458333674740828, 0.7853790794158941324 ) ) ;
#145549=CARTESIAN_POINT ( 'NONE',  ( -0.3817069231124953776, 3.999999999999980904, -1.007084182327226296 ) ) ;
#145562=CARTESIAN_POINT ( 'NONE',  ( 0.3788956605885618889, 3.049042541176487209, 0.4283520265745445199 ) ) ;
#145579=EDGE_CURVE ( 'NONE', #60914, #64456, #6448, .T. ) ;
#145634=CARTESIAN_POINT ( 'NONE',  ( 1.360316468749979801, -0.9322916663252904801, -0.7853790794159041244 ) ) ;
#145692=CARTESIAN_POINT ( 'NONE',  ( -0.6125000000000105915, 0.5416666666666625218, 1.060881119635880721 ) ) ;
#145814=ADVANCED_FACE ( 'NONE', ( #170029 ), #72526, .T. ) ;
#145837=CARTESIAN_POINT ( 'NONE',  ( 2.672702088255949078E-15, 1.625000000682787160, 1.224999999999980549 ) ) ;
#145877=CARTESIAN_POINT ( 'NONE',  ( 0.6801582343749883464, 2.588541667008101399, -1.178068619123865846 ) ) ;
#145915=ORIENTED_EDGE ( 'NONE', *, *, #43786, .T. ) ;
#145930=CARTESIAN_POINT ( 'NONE',  ( -1.552391752028397856E-14, 2.750000000682808921, -1.414508159514587415 ) ) ;
#145932=LINE ( 'NONE', #129736, #10142 ) ;
#145994=CARTESIAN_POINT ( 'NONE',  ( -1.734723475976807094E-14, 4.000000000000003553, -1.734723475976807094E-14 ) ) ;
#146027=CARTESIAN_POINT ( 'NONE',  ( 1.360316468749971586, 1.026041667008143143, 0.7853790794158540534 ) ) ;
#146074=CARTESIAN_POINT ( 'NONE',  ( 1.882262909678013463, 3.299172163371834277, 0.4004916885352222677 ) ) ;
#146151=CARTESIAN_POINT ( 'NONE',  ( 1.360316468749975582, -0.4635416663252802660, -0.7853790794159301036 ) ) ;
#146165=FACE_OUTER_BOUND ( 'NONE', #117723, .T. ) ;
#146173=CARTESIAN_POINT ( 'NONE',  ( -1.360316468750010666, 2.869791667008063651, -0.7853790794158961308 ) ) ;
#146195=EDGE_CURVE ( 'NONE', #28319, #41218, #182420, .T. ) ;
#146265=EDGE_CURVE ( 'NONE', #175731, #125736, #124334, .T. ) ;
#146356=VERTEX_POINT ( 'NONE', #139443 ) ;
#146382=CARTESIAN_POINT ( 'NONE',  ( 1.360316468749965590, 1.067708333674703081, -0.7853790794159082322 ) ) ;
#146460=DIRECTION ( 'NONE',  ( -1.054711873393901277E-15, 0.8656921114426510133, 0.5005768354468321801 ) ) ;
#146485=DIRECTION ( 'NONE',  ( 3.330669073875478989E-16, -3.540251991789410786E-16, -1.000000000000000000 ) ) ;
#146559=ORIENTED_EDGE ( 'NONE', *, *, #48267, .F. ) ;
#146562=AXIS2_PLACEMENT_3D ( 'NONE', #12179, #211440, #96673 ) ;
#146614=DIRECTION ( 'NONE',  ( 1.276756478318932585E-15, -1.000000000000000000, 1.665334536937738262E-16 ) ) ;
#146658=CARTESIAN_POINT ( 'NONE',  ( -0.4408745273427117084, 3.070687961115757592, -0.4190752896376583325 ) ) ;
#146682=CARTESIAN_POINT ( 'NONE',  ( -1.360316468750042862, -0.8489583329918899413, -0.7853790794159322131 ) ) ;
#146697=CARTESIAN_POINT ( 'NONE',  ( 0.4214947629262710826, 3.038568440852366770, 0.4183962726258849685 ) ) ;
#146799=CARTESIAN_POINT ( 'NONE',  ( -0.3788956605886382167, 3.049042541176487209, -0.4283520265746191269 ) ) ;
#146933=CARTESIAN_POINT ( 'NONE',  ( -4.356712336337761644E-14, 2.859375000341351392, -1.570758158831810247 ) ) ;
#146986=CARTESIAN_POINT ( 'NONE',  ( -1.225000000000010747, 2.312500000682803147, -2.081668171172168513E-14 ) ) ;
#147018=ADVANCED_FACE ( 'NONE', ( #211109 ), #126766, .T. ) ;
#147082=CARTESIAN_POINT ( 'NONE',  ( -1.360316468750004448, 1.671875000341424666, -8.673617379884035472E-15 ) ) ;
#147173=UNCERTAINTY_MEASURE_WITH_UNIT (LENGTH_MEASURE( 1.000000000000000082E-05 ), #131230, 'distance_accuracy_value', 'NONE');
#147203=ORIENTED_EDGE ( 'NONE', *, *, #117177, .T. ) ;
#147207=CARTESIAN_POINT ( 'NONE',  ( -1.360316468750034868, -0.8802083329919301313, -0.7853790794159242195 ) ) ;
#147230=CARTESIAN_POINT ( 'NONE',  ( 0.6801582343749952297, 2.807291667008070313, -1.178068619123883165 ) ) ;
#147413=EDGE_CURVE ( 'NONE', #143294, #175466, #113076, .T. ) ;
#147430=CARTESIAN_POINT ( 'NONE',  ( 1.360316468749957597, 0.3177083336747154596, -0.7853790794158961308 ) ) ;
#147456=ORIENTED_EDGE ( 'NONE', *, *, #91508, .T. ) ;
#147475=( BOUNDED_CURVE ( )  B_SPLINE_CURVE ( 3, ( #137685, #24971, #72655, #203706 ),
 .UNSPECIFIED., .F., .T. ) 
 B_SPLINE_CURVE_WITH_KNOTS ( ( 4, 4 ),
 ( 1.570796326794821729, 2.479086375274792253 ),
 .UNSPECIFIED. ) 
 CURVE ( )  GEOMETRIC_REPRESENTATION_ITEM ( )  RATIONAL_B_SPLINE_CURVE ( ( 1.000000000000000000, 0.9324242863010213656, 0.9324242863010213656, 1.000000000000000000 ) ) 
 REPRESENTATION_ITEM ( '' )  );
#147528=EDGE_LOOP ( 'NONE', ( #169985, #100709, #90068, #118523, #17325, #92474 ) ) ;
#147584=CARTESIAN_POINT ( 'NONE',  ( 0.3999999999999576672, 3.949999999999981526, 0.8338124244295311849 ) ) ;
#147627=ORIENTED_EDGE ( 'NONE', *, *, #112518, .T. ) ;
#147644=CARTESIAN_POINT ( 'NONE',  ( -0.4000000000000338840, 3.949999999999977973, -0.8338124244295983534 ) ) ;
#147667=CARTESIAN_POINT ( 'NONE',  ( 0.6124999999999707345, 0.4166666666666901664, -1.060881119635969094 ) ) ;
#147679=DIRECTION ( 'NONE',  ( 1.276756478318932585E-15, -1.000000000000000000, 1.665334536937738262E-16 ) ) ;
#147704=CARTESIAN_POINT ( 'NONE',  ( -0.4347878448725298051, 3.060161718936324160, -0.4204403343213366506 ) ) ;
#147719=CARTESIAN_POINT ( 'NONE',  ( -0.3000000000000414002, 3.999999999999974243, 1.007084189318353973 ) ) ;
#147727=CARTESIAN_POINT ( 'NONE',  ( 1.360316468749989793, -0.4322916663252800995, -0.7853790794158961308 ) ) ;
#147771=DIRECTION ( 'NONE',  ( 1.000000000000000000, -7.771561172376097755E-16, -4.440892098500627148E-16 ) ) ;
#148038=CARTESIAN_POINT ( 'NONE',  ( -1.235837185320847853, 1.391320699396851395E-14, 0.2124088322884870594 ) ) ;
#148094=AXIS2_PLACEMENT_3D ( 'NONE', #71379, #72454, #56227 ) ;
#148142=CARTESIAN_POINT ( 'NONE',  ( 1.360316468749964480, 2.046875000341397133, -4.857225732735059864E-14 ) ) ;
#148194=CARTESIAN_POINT ( 'NONE',  ( -1.225000000000003864, 0.8125000006827948207, -3.469446951953614189E-15 ) ) ;
#148259=CARTESIAN_POINT ( 'NONE',  ( -0.3868389748197708644, 3.100956225802684596, -0.4583768147623576428 ) ) ;
#148270=CARTESIAN_POINT ( 'NONE',  ( -1.352083138863443345E-14, -0.9218749996585863249, -1.570758158831792262 ) ) ;
#148292=CARTESIAN_POINT ( 'NONE',  ( -0.6801582343750213200, 1.348958333674710186, -1.178068619123886718 ) ) ;
#148358=ORIENTED_EDGE ( 'NONE', *, *, #77906, .F. ) ;
#148397=DIRECTION ( 'NONE',  ( 1.000000000000000000, 1.276756478318932585E-15, 4.555315873022827019E-16 ) ) ;
#148449=CARTESIAN_POINT ( 'NONE',  ( 0.2999999999999841682, 3.975028841772316301, -0.9637995837462943749 ) ) ;
#148482=CARTESIAN_POINT ( 'NONE',  ( 1.224999999999976108, 1.187500000682802037, -3.469446951953614189E-14 ) ) ;
#148493=CARTESIAN_POINT ( 'NONE',  ( 0.6801582343749917881, 1.005208333674747934, 1.178068619123807004 ) ) ;
#148530=CARTESIAN_POINT ( 'NONE',  ( -5.157946788997579689E-14, 1.203125000341463746, 1.570758158831762286 ) ) ;
#148538=CARTESIAN_POINT ( 'NONE',  ( -0.6125000000000123679, 1.770833334016133520, -1.060881119635941339 ) ) ;
#148554=( BOUNDED_CURVE ( )  B_SPLINE_CURVE ( 2, ( #42295, #58521, #159215, #172283, #28152, #123620, #10815, #207956, #74778 ),
 .UNSPECIFIED., .F., .T. ) 
 B_SPLINE_CURVE_WITH_KNOTS ( ( 3, 2, 2, 2, 3 ),
 ( 0.1406250000000002776, 0.1458333333333333426, 0.1562500000000000000, 0.1666666666666666574, 0.1718749999999998335 ),
 .UNSPECIFIED. ) 
 CURVE ( )  GEOMETRIC_REPRESENTATION_ITEM ( )  RATIONAL_B_SPLINE_CURVE ( ( 0.9330127018922194093, 0.9330127018922229620, 1.000000000000000000, 0.8660254037844387076, 1.000000000000000000, 0.8660254037844387076, 1.000000000000000000, 0.9330127018922215187, 0.9330127018922194093 ) ) 
 REPRESENTATION_ITEM ( '' )  );
#148711=AXIS2_PLACEMENT_3D ( 'NONE', #160092, #193647, #27958 ) ;
#148775=CARTESIAN_POINT ( 'NONE',  ( -0.4000000000000408229, 3.949999999999971756, 0.8338124244295227472 ) ) ;
#148781=CARTESIAN_POINT ( 'NONE',  ( 0.6801582343749952297, 2.807291667008070313, -1.178068619123883165 ) ) ;
#149024=CARTESIAN_POINT ( 'NONE',  ( -0.4000000000000348277, 3.251480759208456917, 0.4649507210924809786 ) ) ;
#149093=CARTESIAN_POINT ( 'NONE',  ( 0.4000000000000045186, 3.950000000000022826, -1.561251128379126385E-14 ) ) ;
#149128=( BOUNDED_CURVE ( )  B_SPLINE_CURVE ( 2, ( #175884, #28552, #112009, #78358, #210485, #173760, #61048, #126131, #94641 ),
 .UNSPECIFIED., .F., .T. ) 
 B_SPLINE_CURVE_WITH_KNOTS ( ( 3, 2, 2, 2, 3 ),
 ( 0.1718749999999998335, 0.1770833333333333426, 0.1875000000000000000, 0.1979166666666666574, 0.2031250000000002220 ),
 .UNSPECIFIED. ) 
 CURVE ( )  GEOMETRIC_REPRESENTATION_ITEM ( )  RATIONAL_B_SPLINE_CURVE ( ( 0.9330127018922194093, 0.9330127018922171889, 1.000000000000000000, 0.8660254037844387076, 1.000000000000000000, 0.8660254037844387076, 1.000000000000000000, 0.9330127018922165227, 0.9330127018922194093 ) ) 
 REPRESENTATION_ITEM ( '' )  );
#149176=B_SPLINE_CURVE_WITH_KNOTS ( 'NONE', 3,
 ( #53064, #98635, #134360, #52013 ),
 .UNSPECIFIED., .F., .F.,
 ( 4, 4 ),
 ( 0.000000000000000000, 3.548791410035703395E-05 ),
 .UNSPECIFIED. ) ;
#149193=CARTESIAN_POINT ( 'NONE',  ( -1.360316468750026653, 2.192708333674788346, 0.7853790794158680422 ) ) ;
#149202=DIRECTION ( 'NONE',  ( 1.276756478318932585E-15, -1.000000000000000000, 1.665334536937738262E-16 ) ) ;
#149246=CARTESIAN_POINT ( 'NONE',  ( -1.225000000000016298, 0.8333333340161279690, 0.7072540797572858251 ) ) ;
#149263=VERTEX_POINT ( 'NONE', #97189 ) ;
#149305=CARTESIAN_POINT ( 'NONE',  ( 0.6124999999999759526, 0.8958333340161606095, 1.060881119635896264 ) ) ;
#149323=CARTESIAN_POINT ( 'NONE',  ( 0.6801582343749865700, -1.026041666325229418, 1.178068619123805227 ) ) ;
#149346=CARTESIAN_POINT ( 'NONE',  ( -1.360316468750056851, 2.119791667008092517, -0.7853790794159082322 ) ) ;
#149389=CARTESIAN_POINT ( 'NONE',  ( 4.067155351693835485E-15, 1.250000000682825130, -1.225000000000013411 ) ) ;
#149401=VECTOR ( 'NONE', #207893, 1000.000000000000000 ) ;
#149434=CARTESIAN_POINT ( 'NONE',  ( -1.913843809498090520, 3.268536626279805013, -0.4294081188993455478 ) ) ;
#149511=CARTESIAN_POINT ( 'NONE',  ( 0.6311622855796339415, 3.299999999999983391, 0.3999999999999593880 ) ) ;
#149531=ORIENTED_EDGE ( 'NONE', *, *, #64709, .T. ) ;
#149590=CARTESIAN_POINT ( 'NONE',  ( -0.6801582343750213200, 1.348958333674710186, -1.178068619123886718 ) ) ;
#149596=CARTESIAN_POINT ( 'NONE',  ( -1.225000000000044276, 1.791666667349484321, -0.7072540797573277915 ) ) ;
#149597=VERTEX_POINT ( 'NONE', #11617 ) ;
#149834=EDGE_CURVE ( 'NONE', #195016, #104013, #203748, .T. ) ;
#149860=CARTESIAN_POINT ( 'NONE',  ( -1.360316468749990459, 1.890625000341386475, -2.428612866367529932E-14 ) ) ;
#149923=CARTESIAN_POINT ( 'NONE',  ( -2.449742653233043743, 3.299999999999976730, -0.4000000000000339950 ) ) ;
#149977=ORIENTED_EDGE ( 'NONE', *, *, #41144, .F. ) ;
#150108=CARTESIAN_POINT ( 'NONE',  ( -3.555477883677943599E-14, 2.484375000341469963, 1.570758158831768281 ) ) ;
#150130=CARTESIAN_POINT ( 'NONE',  ( 1.225000000000001199, 0.6458333333333310389, -0.7072540797572937077 ) ) ;
#150184=CARTESIAN_POINT ( 'NONE',  ( 1.224999999999951017, 2.166666667349502085, 0.7072540797572777205 ) ) ;
#150248=EDGE_CURVE ( 'NONE', #87431, #12920, #101273, .T. ) ;
#150277=CARTESIAN_POINT ( 'NONE',  ( -4.957638175832625493E-14, 0.8593750003414141192, -1.570758158831808249 ) ) ;
#150313=DIRECTION ( 'NONE',  ( 0.000000000000000000, 0.000000000000000000, 1.000000000000000000 ) ) ;
#150346=EDGE_LOOP ( 'NONE', ( #191597, #119676, #154087, #56108 ) ) ;
#150388=CARTESIAN_POINT ( 'NONE',  ( 1.224999999999990985, 0.9166666673494643369, 0.7072540797572697269 ) ) ;
#150403=CARTESIAN_POINT ( 'NONE',  ( -0.6801582343750022241, -0.1510416663252633906, -1.178068619123841643 ) ) ;
#150426=VERTEX_POINT ( 'NONE', #183966 ) ;
#150428=CARTESIAN_POINT ( 'NONE',  ( -1.360316468750026875, 2.140625000341400685, -4.857225732735059864E-14 ) ) ;
#150448=DIRECTION ( 'NONE',  ( 1.276756478318932585E-15, -1.000000000000000000, 1.665334536937738262E-16 ) ) ;
#150460=CARTESIAN_POINT ( 'NONE',  ( 1.919771823249041720, 3.227545531266407419, -0.4000000000000275002 ) ) ;
#150504=CARTESIAN_POINT ( 'NONE',  ( 1.224999999999943023, 2.645833333333332593, -0.7072540797573158011 ) ) ;
#150517=CARTESIAN_POINT ( 'NONE',  ( -1.889772045536145306, 3.296949564223910834, -0.4024211290685451581 ) ) ;
#150576=FACE_OUTER_BOUND ( 'NONE', #189050, .T. ) ;
#150589=CARTESIAN_POINT ( 'NONE',  ( -0.3282377607281322107, 2.698664549684628433, -1.225000000000014744 ) ) ;
#150611=AXIS2_PLACEMENT_3D ( 'NONE', #209694, #128560, #45112 ) ;
#150628=FILL_AREA_STYLE ('',( #183104 ) ) ;
#150630=CARTESIAN_POINT ( 'NONE',  ( -0.6801582343750229853, -0.8697916663252605041, -1.178068619123862515 ) ) ;
#150671=CARTESIAN_POINT ( 'NONE',  ( -1.953008978358306879E-14, 1.828125000341410678, -1.570758158831798257 ) ) ;
#150687=ORIENTED_EDGE ( 'NONE', *, *, #138823, .F. ) ;
#150711=AXIS2_PLACEMENT_3D ( 'NONE', #201387, #33581, #36768 ) ;
#150738=DIRECTION ( 'NONE',  ( 1.276756478318932585E-15, -1.000000000000000000, 1.665334536937738262E-16 ) ) ;
#150935=ORIENTED_EDGE ( 'NONE', *, *, #59473, .F. ) ;
#150965=CARTESIAN_POINT ( 'NONE',  ( -1.225000000000032285, 1.833333334016213012, 0.7072540797572777205 ) ) ;
#151088=CARTESIAN_POINT ( 'NONE',  ( 0.3000000002818084543, 3.198312376128888079, -0.5146719259196330665 ) ) ;
#151173=CARTESIAN_POINT ( 'NONE',  ( 1.360316468749978469, 2.296875000341369599, -4.857225732735059864E-14 ) ) ;
#151195=CARTESIAN_POINT ( 'NONE',  ( 1.224999999999965006, 0.3541666666667217522, 0.7072540797572456350 ) ) ;
#151353=( BOUNDED_CURVE ( )  B_SPLINE_CURVE ( 2, ( #42152, #73557, #124537, #190494, #93036, #91973, #10675, #94105, #9619 ),
 .UNSPECIFIED., .F., .T. ) 
 B_SPLINE_CURVE_WITH_KNOTS ( ( 3, 2, 2, 2, 3 ),
 ( 0.4218749999999998335, 0.4270833333333333148, 0.4375000000000000000, 0.4479166666666666852, 0.4531250000000001665 ),
 .UNSPECIFIED. ) 
 CURVE ( )  GEOMETRIC_REPRESENTATION_ITEM ( )  RATIONAL_B_SPLINE_CURVE ( ( 0.9330127018922194093, 0.9330127018922171889, 1.000000000000000000, 0.8660254037844387076, 1.000000000000000000, 0.8660254037844387076, 1.000000000000000000, 0.9330127018922171889, 0.9330127018922194093 ) ) 
 REPRESENTATION_ITEM ( '' )  );
#151419=DIRECTION ( 'NONE',  ( 1.276756478318932585E-15, -1.000000000000000000, 1.665334536937738262E-16 ) ) ;
#151450=ORIENTED_EDGE ( 'NONE', *, *, #89445, .F. ) ;
#151488=CARTESIAN_POINT ( 'NONE',  ( -1.734723475976807094E-15, 2.999999999999988898, -6.938893903907228378E-15 ) ) ;
#151492=CARTESIAN_POINT ( 'NONE',  ( 1.360316468750001784, 2.286458333674732835, -0.7853790794158941324 ) ) ;
#151541=CYLINDRICAL_SURFACE ( 'NONE', #121761, 0.04999999999999991257 ) ;
#151566=CARTESIAN_POINT ( 'NONE',  ( 1.224999999999957012, 2.854166666666677621, 0.7072540797572558491 ) ) ;
#151568=CARTESIAN_POINT ( 'NONE',  ( -5.204170427930421283E-14, 3.949999999999960654, -4.683753385137379155E-14 ) ) ;
#151621=CARTESIAN_POINT ( 'NONE',  ( 0.4423565646247452077, 3.073250980203122040, -0.4181372721656086977 ) ) ;
#151633=ORIENTED_EDGE ( 'NONE', *, *, #80469, .F. ) ;
#151645=ORIENTED_EDGE ( 'NONE', *, *, #103939, .F. ) ;
#151666=ORIENTED_EDGE ( 'NONE', *, *, #31466, .T. ) ;
#151734=CARTESIAN_POINT ( 'NONE',  ( -3.755786496842899057E-14, 1.078125000341431106, -1.570758158831814466 ) ) ;
#151834=ADVANCED_FACE ( 'NONE', ( #9817 ), #110597, .T. ) ;
#151861=CARTESIAN_POINT ( 'NONE',  ( -0.3000000000000172529, 3.975028841772365595, -0.9637995837462973725 ) ) ;
#151994=VECTOR ( 'NONE', #116655, 1000.000000000000000 ) ;
#152026=CARTESIAN_POINT ( 'NONE',  ( -1.953008978358306879E-14, 2.125000000682797818, 1.414508159514571428 ) ) ;
#152055=COLOUR_RGB ( '', 0.72549020, 0.75294118, 0.79215686) ;
#152097=LINE ( 'NONE', #3668, #122036 ) ;
#152116=LINE ( 'NONE', #201889, #49024 ) ;
#152154=CARTESIAN_POINT ( 'NONE',  ( -0.6125000000000331291, 0.7916666666666558605, 1.060881119635891157 ) ) ;
#152231=CARTESIAN_POINT ( 'NONE',  ( 0.6801582343749952297, 2.255208333674735499, 1.178068619123839866 ) ) ;
#152252=CARTESIAN_POINT ( 'NONE',  ( -1.225000000000042277, 0.2291666666666811181, -0.7072540797573237947 ) ) ;
#152419=CARTESIAN_POINT ( 'NONE',  ( -0.5445930744354052777, 3.250057683544617326, 0.3999999999999455103 ) ) ;
#152543=CARTESIAN_POINT ( 'NONE',  ( -3.755786496842897795E-14, 1.453125000341440876, 1.570758158831776052 ) ) ;
#152615=CARTESIAN_POINT ( 'NONE',  ( 1.224999999999949241, 2.895833333333309501, -0.7072540797573237947 ) ) ;
#152637=EDGE_CURVE ( 'NONE', #99612, #140322, #100029, .T. ) ;
#152662=CARTESIAN_POINT ( 'NONE',  ( 1.350906756270435993, 4.584752781686859626E-14, 0.1093157834398475192 ) ) ;
#152706=CARTESIAN_POINT ( 'NONE',  ( -1.225000000000029843, -0.4374999993171646562, -4.163336342344337027E-14 ) ) ;
#152742=CARTESIAN_POINT ( 'NONE',  ( -1.360316468750012886, -0.05729166632526227348, 0.7853790794158901356 ) ) ;
#152759=AXIS2_PLACEMENT_3D ( 'NONE', #37038, #55434, #103122 ) ;
#152784=CARTESIAN_POINT ( 'NONE',  ( 5.007715329123863766E-16, 0.8281250003414059035, -1.570758158831786266 ) ) ;
#152930=CYLINDRICAL_SURFACE ( 'NONE', #84291, 1.224999999999996980 ) ;
#152973=EDGE_CURVE ( 'NONE', #176198, #42265, #2712, .T. ) ;
#152976=CARTESIAN_POINT ( 'NONE',  ( 6.972266317189433020E-16, 0.5000000006828014820, -1.225000000000012745 ) ) ;
#153083=CARTESIAN_POINT ( 'NONE',  ( 1.224999999999951017, 2.166666667349502529, 0.7072540797572777205 ) ) ;
#153089=EDGE_CURVE ( 'NONE', #164105, #21883, #177704, .T. ) ;
#153132=CARTESIAN_POINT ( 'NONE',  ( -1.734723475976807094E-15, 2.999999999999988898, -6.938893903907228378E-15 ) ) ;
#153140=CARTESIAN_POINT ( 'NONE',  ( -0.6124999999999967137, 1.541666666666677177, 1.060881119635903147 ) ) ;
#153150=PLANE ( 'NONE',  #118730 ) ;
#153196=CARTESIAN_POINT ( 'NONE',  ( -0.3776192402222742217, 3.049641483663600106, 0.4287046358292067039 ) ) ;
#153208=DIRECTION ( 'NONE',  ( -5.828670879282089587E-16, 0.8656921114426507913, -0.5005768354468322912 ) ) ;
#153290=CARTESIAN_POINT ( 'NONE',  ( 0.6801582343749883464, 1.505208333674713739, 1.178068619123805227 ) ) ;
#153314=CARTESIAN_POINT ( 'NONE',  ( 0.6124999999999862776, 1.083333333333352799, 1.060881119635887604 ) ) ;
#153333=LINE ( 'NONE', #89419, #101375 ) ;
#153413=CARTESIAN_POINT ( 'NONE',  ( 0.6124999999999846123, 2.645833334016141514, 1.060881119635910252 ) ) ;
#153418=VECTOR ( 'NONE', #69737, 1000.000000000000000 ) ;
#153471=CARTESIAN_POINT ( 'NONE',  ( -1.360316468750019991, 0.4218750003414165062, -4.336808689942017736E-14 ) ) ;
#153620=CARTESIAN_POINT ( 'NONE',  ( -1.360316468750054852, 0.9114583336747262843, 0.7853790794158720390 ) ) ;
#153638=ORIENTED_EDGE ( 'NONE', *, *, #104334, .T. ) ;
#153639=CIRCLE ( 'NONE', #208956, 1.872309607372811158 ) ;
#153691=CARTESIAN_POINT ( 'NONE',  ( 1.224999999999989875, 2.624999999999995559, -2.255140518769849223E-14 ) ) ;
#153735=CARTESIAN_POINT ( 'NONE',  ( 0.2126227708255458981, -7.873890270133753525E-15, -1.223618500935122366 ) ) ;
#153779=CARTESIAN_POINT ( 'NONE',  ( -1.225000000000004086, -0.7083333326505274474, -0.7072540797572998139 ) ) ;
#153787=DIRECTION ( 'NONE',  ( -5.828670879282089587E-16, 0.8656921114426509023, -0.5005768354468322912 ) ) ;
#153803=( BOUNDED_SURFACE ( )  B_SPLINE_SURFACE ( 3, 2, ( 
 ( #169449, #170512, #184618 ),
 ( #21034, #116498, #134847 ),
 ( #151088, #34116, #17842 ),
 ( #86068, #182487, #54633 ) ),
 .UNSPECIFIED., .F., .F., .F. ) 
 B_SPLINE_SURFACE_WITH_KNOTS ( ( 4, 4 ),
 ( 3, 3 ),
 ( 0.5050616349177523556, 1.570796326794896558 ),
 ( 0.000000000000000000, 1.000000000000000000 ),
 .UNSPECIFIED. ) 
 GEOMETRIC_REPRESENTATION_ITEM ( )  RATIONAL_B_SPLINE_SURFACE ( (
 ( 1.000000000000000000, 0.9374448844494615019, 1.000000000000000000),
 ( 1.000000000000000000, 0.8980788380694217921, 1.000000000000000000),
 ( 1.000000000000000000, 0.8161930835858733913, 1.000000000000000000),
 ( 1.000000000000000000, 0.7071067811866033059, 1.000000000000000000) ) ) 
 REPRESENTATION_ITEM ( '' )  SURFACE ( )  );
#153851=CARTESIAN_POINT ( 'NONE',  ( -0.6801582343750438575, 1.932291667008062541, 1.178068619123787908 ) ) ;
#153860=CARTESIAN_POINT ( 'NONE',  ( 1.360316468749985797, 0.2864583336747233422, -0.7853790794158961308 ) ) ;
#153891=CARTESIAN_POINT ( 'NONE',  ( 8.134310703387671364E-16, 2.000000000682804924, -1.225000000000021849 ) ) ;
#153901=EDGE_CURVE ( 'NONE', #194227, #102576, #2245, .T. ) ;
#153927=CARTESIAN_POINT ( 'NONE',  ( 1.906201616980772950, 3.231688558335350514, 0.4612787108932545066 ) ) ;
#153954=VERTEX_POINT ( 'NONE', #3166 ) ;
#154087=ORIENTED_EDGE ( 'NONE', *, *, #80889, .F. ) ;
#154133=DIRECTION ( 'NONE',  ( -9.436895709313856232E-16, 0.8656921114426507913, 0.5005768354468325132 ) ) ;
#154158=CARTESIAN_POINT ( 'NONE',  ( 0.6124999999999707345, 1.729166667349485431, -1.060881119635955327 ) ) ;
#154185=DIRECTION ( 'NONE',  ( 0.000000000000000000, 0.000000000000000000, 1.000000000000000000 ) ) ;
#154211=CARTESIAN_POINT ( 'NONE',  ( 0.4499999999999677591, 3.999999999999961808, -0.8338124244296144516 ) ) ;
#154231=CARTESIAN_POINT ( 'NONE',  ( -0.3728825314829262716, 3.227879828479837343, 0.5317689764002340169 ) ) ;
#154246=AXIS2_PLACEMENT_3D ( 'NONE', #16670, #46021, #82754 ) ;
#154313=DIRECTION ( 'NONE',  ( -0.8660254037844408170, -0.4999999999999962808, -1.110223024625157526E-16 ) ) ;
#154364=CARTESIAN_POINT ( 'NONE',  ( -1.360316468749998675, 1.442708333674736831, 0.7853790794158961308 ) ) ;
#154388=CARTESIAN_POINT ( 'NONE',  ( 0.6124999999999776179, 0.8333333333333594606, 1.060881119635894487 ) ) ;
#154457=CARTESIAN_POINT ( 'NONE',  ( -0.3000000000000380695, 3.975028841772282107, 0.9637995837462106641 ) ) ;
#154487=DIRECTION ( 'NONE',  ( -1.000000000000000000, 0.000000000000000000, 5.421010862427519212E-16 ) ) ;
#154540=CARTESIAN_POINT ( 'NONE',  ( -7.511572993685796537E-15, 0.3593750003414037386, -1.570758158831792262 ) ) ;
#154542=DIRECTION ( 'NONE',  ( 0.000000000000000000, 0.000000000000000000, 1.000000000000000000 ) ) ;
#154544=VERTEX_POINT ( 'NONE', #79677 ) ;
#154599=ORIENTED_EDGE ( 'NONE', *, *, #128228, .F. ) ;
#154655=CARTESIAN_POINT ( 'NONE',  ( -2.905110965495596944E-15, 1.687500000000013101, -1.225000000000019851 ) ) ;
#154669=CARTESIAN_POINT ( 'NONE',  ( -1.814759087649988833, 3.975067388631688292, -0.4606438099578630818 ) ) ;
#154685=CARTESIAN_POINT ( 'NONE',  ( -1.360316468750042862, -0.08854166632527044056, 0.7853790794158801436 ) ) ;
#154687=FACE_OUTER_BOUND ( 'NONE', #73490, .T. ) ;
#154758=CARTESIAN_POINT ( 'NONE',  ( -2.153317591523261390E-14, 1.562499999999999334, 1.414508159514573427 ) ) ;
#154771=ADVANCED_FACE ( 'NONE', ( #50375 ), #153803, .F. ) ;
#154849=CARTESIAN_POINT ( 'NONE',  ( -2.954552044183079750E-14, -0.1249999993171966028, 1.414508159514565433 ) ) ;
#154860=ORIENTED_EDGE ( 'NONE', *, *, #118886, .T. ) ;
#154917=CARTESIAN_POINT ( 'NONE',  ( 1.360316468749965590, 2.494791667008093849, 0.7853790794158861388 ) ) ;
#154924=CARTESIAN_POINT ( 'NONE',  ( 0.3282377607281097287, 2.823664549684629321, 1.224999999999951239 ) ) ;
#154986=DIRECTION ( 'NONE',  ( 1.276756478318932585E-15, -1.000000000000000000, 1.665334536937738262E-16 ) ) ;
#155118=FACE_OUTER_BOUND ( 'NONE', #103767, .T. ) ;
#155147=CARTESIAN_POINT ( 'NONE',  ( 1.360316468749997565, 2.067708333674723509, -0.7853790794159001276 ) ) ;
#155167=VECTOR ( 'NONE', #4972, 1000.000000000000000 ) ;
#155224=CARTESIAN_POINT ( 'NONE',  ( 1.224999999999991207, 0.9166666673494643369, 0.7072540797572697269 ) ) ;
#155251=CYLINDRICAL_SURFACE ( 'NONE', #70357, 0.04999999999999991257 ) ;
#155260=AXIS2_PLACEMENT_3D ( 'NONE', #201367, #148397, #168892 ) ;
#155280=DIRECTION ( 'NONE',  ( -1.000000000000000000, 7.771561172376094797E-16, -3.330669073875481454E-16 ) ) ;
#155327=FACE_OUTER_BOUND ( 'NONE', #37636, .T. ) ;
#155335=ADVANCED_FACE ( 'NONE', ( #114918 ), #192083, .T. ) ;
#155428=CARTESIAN_POINT ( 'NONE',  ( 0.6801582343749744686, 0.3385416670080923507, -1.178068619123886718 ) ) ;
#155451=CARTESIAN_POINT ( 'NONE',  ( 1.224999999999943023, -0.3958333333332818005, 0.7072540797572536286 ) ) ;
#155554=CARTESIAN_POINT ( 'NONE',  ( 0.3282377607281101173, 2.738835450998162280, -1.225000000000008527 ) ) ;
#155577=EDGE_LOOP ( 'NONE', ( #39939, #32672, #156641, #200341 ) ) ;
#155611=ORIENTED_EDGE ( 'NONE', *, *, #118886, .F. ) ;
#155697=EDGE_CURVE ( 'NONE', #99612, #98321, #46878, .T. ) ;
#155754=CARTESIAN_POINT ( 'NONE',  ( -1.360316468750002894, 0.4114583336747319464, 0.7853790794158961308 ) ) ;
#155804=CARTESIAN_POINT ( 'NONE',  ( 0.6311622855796270581, 3.199999999999994404, 0.3999999999999819811 ) ) ;
#155818=CARTESIAN_POINT ( 'NONE',  ( 0.3000000000000016542, 3.322650755865477645, 0.5865692111442620815 ) ) ;
#155826=CARTESIAN_POINT ( 'NONE',  ( -1.225000000000012523, 2.000000000000001776, -1.214306433183764966E-14 ) ) ;
#155839=CARTESIAN_POINT ( 'NONE',  ( 0.4626273691814064004, 3.108307088186316403, 0.4053073865230037987 ) ) ;
#155851=ORIENTED_EDGE ( 'NONE', *, *, #212155, .T. ) ;
#155917=CARTESIAN_POINT ( 'NONE',  ( -3.355169270512988773E-14, -0.8749999993172000723, 1.414508159514567431 ) ) ;
#155945=ORIENTED_EDGE ( 'NONE', *, *, #20664, .T. ) ;
#155982=CARTESIAN_POINT ( 'NONE',  ( 0.6801582343749796866, 1.473958333674751930, 1.178068619123789462 ) ) ;
#155989=EDGE_CURVE ( 'NONE', #68973, #61933, #7159, .T. ) ;
#156018=EDGE_LOOP ( 'NONE', ( #167844, #76479, #196118, #176337, #39064, #139250, #10636, #207567, #3963, #143002, #35387 ) ) ;
#156107=ADVANCED_BREP_SHAPE_REPRESENTATION ( '', ( #85152, #200407 ), #141734 ) ;
#156129=ORIENTED_EDGE ( 'NONE', *, *, #6013, .F. ) ;
#156222=CARTESIAN_POINT ( 'NONE',  ( 0.6124999999999707345, 0.7291666673494984208, -1.060881119635972647 ) ) ;
#156224=CARTESIAN_POINT ( 'NONE',  ( -1.360316468750006669, 2.442708333674733723, 0.7853790794158861388 ) ) ;
#156235=CARTESIAN_POINT ( 'NONE',  ( 0.3282377607281116716, 2.488835450998179599, -1.225000000000015410 ) ) ;
#156257=ORIENTED_EDGE ( 'NONE', *, *, #160015, .T. ) ;
#156275=FACE_OUTER_BOUND ( 'NONE', #12368, .T. ) ;
#156298=CARTESIAN_POINT ( 'NONE',  ( -1.552391752028397856E-14, 0.5000000006828063670, -1.414508159514587415 ) ) ;
#156327=ORIENTED_EDGE ( 'NONE', *, *, #190484, .T. ) ;
#156355=CARTESIAN_POINT ( 'NONE',  ( -1.162044386198238837E-16, 1.437500000000019540, -1.225000000000020739 ) ) ;
#156379=ORIENTED_EDGE ( 'NONE', *, *, #77841, .F. ) ;
#156382=CARTESIAN_POINT ( 'NONE',  ( -0.3423093779010479842, 3.099999999999998757, 0.3999999999999559464 ) ) ;
#156407=ORIENTED_EDGE ( 'NONE', *, *, #124535, .T. ) ;
#156421=LINE ( 'NONE', #205133, #206951 ) ;
#156425=CARTESIAN_POINT ( 'NONE',  ( 0.3282377607281158904, 1.823664549684622882, 1.224999999999982991 ) ) ;
#156507=CARTESIAN_POINT ( 'NONE',  ( -0.3769810270648435990, 3.049942316455334090, 0.4288785890452350702 ) ) ;
#156512=CARTESIAN_POINT ( 'NONE',  ( -0.6801582343750559589, -0.03645833299194961574, 1.178068619123796568 ) ) ;
#156534=CARTESIAN_POINT ( 'NONE',  ( -1.225000000000040057, -0.02083333333332007889, -0.7072540797572998139 ) ) ;
#156604=CARTESIAN_POINT ( 'NONE',  ( -0.6311622855796928944, 3.199999999999994404, 0.3999999999999611644 ) ) ;
#156641=ORIENTED_EDGE ( 'NONE', *, *, #191456, .T. ) ;
#156646=LINE ( 'NONE', #88443, #209301 ) ;
#156689=DIRECTION ( 'NONE',  ( -3.330669073875478989E-16, 3.330669073875478989E-16, 1.000000000000000000 ) ) ;
#156743=CARTESIAN_POINT ( 'NONE',  ( 1.224999999999989875, 2.624999999999995559, -2.255140518769849223E-14 ) ) ;
#156830=CARTESIAN_POINT ( 'NONE',  ( 0.6801582343749970061, 0.8072916670080754198, -1.178068619123858962 ) ) ;
#156850=LINE ( 'NONE', #7357, #11224 ) ;
#156901=CARTESIAN_POINT ( 'NONE',  ( -0.6125000000000037081, 2.458333333333319271, -1.060881119635955327 ) ) ;
#157038=ORIENTED_EDGE ( 'NONE', *, *, #202085, .T. ) ;
#157060=CARTESIAN_POINT ( 'NONE',  ( 1.360316468749983576, 1.515625000341386253, -4.163336342344337027E-14 ) ) ;
#157068=CARTESIAN_POINT ( 'NONE',  ( -1.975475456537005874E-15, 2.812500000000000888, 1.224999999999953904 ) ) ;
#157075=CARTESIAN_POINT ( 'NONE',  ( 1.907519672996875082, 3.236073672982398008, -0.4612874649729831744 ) ) ;
#157103=ORIENTED_EDGE ( 'NONE', *, *, #191456, .F. ) ;
#157223=EDGE_CURVE ( 'NONE', #168515, #125736, #120986, .T. ) ;
#157243=EDGE_CURVE ( 'NONE', #23953, #35460, #149176, .T. ) ;
#157289=CARTESIAN_POINT ( 'NONE',  ( -1.360316468750028651, 1.692708333674761922, 0.7853790794158620470 ) ) ;
#157368=CARTESIAN_POINT ( 'NONE',  ( 1.224999999999947020, 0.1666666673495328654, 0.7072540797572737237 ) ) ;
#157417=CYLINDRICAL_SURFACE ( 'NONE', #48087, 1.224999999999996980 ) ;
#157437=B_SPLINE_CURVE_WITH_KNOTS ( 'NONE', 3,
 ( #205531, #190348, #55037, #154669 ),
 .UNSPECIFIED., .F., .F.,
 ( 4, 4 ),
 ( 0.000000000000000000, 0.0007699926951938503451 ),
 .UNSPECIFIED. ) ;
#157465=CARTESIAN_POINT ( 'NONE',  ( 0.3282377607281144472, 0.6763354503153764519, -1.225000000000007194 ) ) ;
#157490=ORIENTED_EDGE ( 'NONE', *, *, #183389, .F. ) ;
#157583=CARTESIAN_POINT ( 'NONE',  ( 0.6801582343749847936, 0.5052083336747614783, 1.178068619123803451 ) ) ;
#157604=CARTESIAN_POINT ( 'NONE',  ( -0.6125000000000037081, -0.2083333333333242665, 1.060881119635920689 ) ) ;
#157704=ORIENTED_EDGE ( 'NONE', *, *, #91562, .F. ) ;
#157809=CARTESIAN_POINT ( 'NONE',  ( 1.224999999999951017, 0.1458333333333527160, -0.7072540797573078075 ) ) ;
#157900=CARTESIAN_POINT ( 'NONE',  ( -1.360316468750006669, 0.1614583336747227316, 0.7853790794158981292 ) ) ;
#157971=CARTESIAN_POINT ( 'NONE',  ( 0.6124999999999862776, 2.333333333333325932, 1.060881119635898040 ) ) ;
#158028=DIRECTION ( 'NONE',  ( -3.497202527569253358E-15, 0.000000000000000000, -1.000000000000000000 ) ) ;
#158033=ORIENTED_EDGE ( 'NONE', *, *, #115854, .T. ) ;
#158048=CARTESIAN_POINT ( 'NONE',  ( 1.772826578343093873, 3.949999999999995293, 0.3999999999999819811 ) ) ;
#158077=DIRECTION ( 'NONE',  ( 3.330669073875478989E-16, -3.540251991789410786E-16, -1.000000000000000000 ) ) ;
#158125=CARTESIAN_POINT ( 'NONE',  ( -5.758872628492444169E-14, 0.4531250003414521998, 1.570758158831760287 ) ) ;
#158133=CARTESIAN_POINT ( 'NONE',  ( -1.360316468750002450, 0.4114583336747319464, 0.7853790794158961308 ) ) ;
#158181=AXIS2_PLACEMENT_3D ( 'NONE', #71448, #88808, #158077 ) ;
#158201=CARTESIAN_POINT ( 'NONE',  ( 0.3282377607281126153, 0.2388354509981848728, -1.225000000000013411 ) ) ;
#158235=EDGE_CURVE ( 'NONE', #198538, #195414, #141808, .T. ) ;
#158264=EDGE_LOOP ( 'NONE', ( #185735, #34450, #181822 ) ) ;
#158353=CARTESIAN_POINT ( 'NONE',  ( -1.360316468750036645, 1.901041667008058988, -0.7853790794159222211 ) ) ;
#158391=EDGE_LOOP ( 'NONE', ( #13569, #121262, #16466, #156129 ) ) ;
#158424=CARTESIAN_POINT ( 'NONE',  ( -0.6125000000000158096, 0.1041666673494701101, 1.060881119635906700 ) ) ;
#158482=EDGE_CURVE ( 'NONE', #213643, #6267, #103615, .T. ) ;
#158508=FACE_OUTER_BOUND ( 'NONE', #168197, .T. ) ;
#158640=CARTESIAN_POINT ( 'NONE',  ( -1.360316468750030428, 1.171875000341417117, -4.336808689942017736E-14 ) ) ;
#158661=CARTESIAN_POINT ( 'NONE',  ( -0.6125000000000262457, -0.5416666666666763996, -1.060881119635976200 ) ) ;
#158784=ORIENTED_EDGE ( 'NONE', *, *, #170968, .T. ) ;
#158810=ORIENTED_EDGE ( 'NONE', *, *, #64709, .F. ) ;
#158951=CARTESIAN_POINT ( 'NONE',  ( 0.6124999999999846123, 2.645833334016141514, 1.060881119635910252 ) ) ;
#158958=LINE ( 'NONE', #207695, #66035 ) ;
#158984=EDGE_CURVE ( 'NONE', #17367, #12050, #133740, .T. ) ;
#159093=CARTESIAN_POINT ( 'NONE',  ( 1.889141968554370221, 3.755428628636679811, 0.3999999999999819811 ) ) ;
#159155=CARTESIAN_POINT ( 'NONE',  ( 4.067155351693835485E-15, 0.2500000006828133059, -1.225000000000014300 ) ) ;
#159171=CARTESIAN_POINT ( 'NONE',  ( 0.6801582343749970061, 0.5572916670080683144, -1.178068619123862515 ) ) ;
#159203=CARTESIAN_POINT ( 'NONE',  ( 1.889772045536109779, 3.296949564223924156, -0.4024211290685810183 ) ) ;
#159205=CARTESIAN_POINT ( 'NONE',  ( 0.2999999999999842792, 3.975028841772351829, 0.9637995837462106641 ) ) ;
#159215=CARTESIAN_POINT ( 'NONE',  ( 0.6124999999999637401, 2.416666666666629659, -1.060881119635962211 ) ) ;
#159246=CARTESIAN_POINT ( 'NONE',  ( -4.415768667553308270E-15, 0.1250000006828069499, 1.224999999999963229 ) ) ;
#159325=DIRECTION ( 'NONE',  ( 3.330669073875478989E-16, -3.540251991789410786E-16, -1.000000000000000000 ) ) ;
#159344=ORIENTED_EDGE ( 'NONE', *, *, #144969, .F. ) ;
#159370=COLOUR_RGB ( '', 0.72549020, 0.75294118, 0.79215686) ;
#159402=CARTESIAN_POINT ( 'NONE',  ( -0.6801582343750177673, 1.713541667008065872, 1.178068619123799898 ) ) ;
#159439=CARTESIAN_POINT ( 'NONE',  ( -1.360316468750056851, 2.119791667008092073, -0.7853790794159083433 ) ) ;
#159485=CARTESIAN_POINT ( 'NONE',  ( 1.224999999999969225, 0.6666666673495352802, 0.7072540797572596238 ) ) ;
#159498=( BOUNDED_CURVE ( )  B_SPLINE_CURVE ( 2, ( #66106, #49897, #2170, #118158, #82384, #86654, #18444, #119219, #133312 ),
 .UNSPECIFIED., .F., .T. ) 
 B_SPLINE_CURVE_WITH_KNOTS ( ( 3, 2, 2, 2, 3 ),
 ( 0.3281250000000001665, 0.3333333333333333148, 0.3437500000000000000, 0.3541666666666666852, 0.3593749999999999445 ),
 .UNSPECIFIED. ) 
 CURVE ( )  GEOMETRIC_REPRESENTATION_ITEM ( )  RATIONAL_B_SPLINE_CURVE ( ( 0.9330127018922194093, 0.9330127018922215187, 1.000000000000000000, 0.8660254037844387076, 1.000000000000000000, 0.8660254037844387076, 1.000000000000000000, 0.9330127018922200755, 0.9330127018922194093 ) ) 
 REPRESENTATION_ITEM ( '' )  );
#159528=CARTESIAN_POINT ( 'NONE',  ( -1.225000000000005640, 1.387778780781445676E-14, -1.387778780781445676E-14 ) ) ;
#159604=ORIENTED_EDGE ( 'NONE', *, *, #94595, .F. ) ;
#159617=CARTESIAN_POINT ( 'NONE',  ( 0.6125000000000019318, 1.833333333333346582, 1.060881119635934455 ) ) ;
#159620=AXIS2_PLACEMENT_3D ( 'NONE', #167053, #183287, #1314 ) ;
#159677=CARTESIAN_POINT ( 'NONE',  ( -0.4288785890453234995, 3.049942316455299451, -0.4196807566834767078 ) ) ;
#159688=EDGE_CURVE ( 'NONE', #196234, #99096, #112745, .T. ) ;
#159700=CARTESIAN_POINT ( 'NONE',  ( -3.755786496842897795E-14, 1.109375000341423112, -1.570758158831814466 ) ) ;
#159717=CARTESIAN_POINT ( 'NONE',  ( -1.734723475976807094E-15, 2.999999999999988898, -6.938893903907228378E-15 ) ) ;
#159722=CARTESIAN_POINT ( 'NONE',  ( 1.224999999999949241, -0.6041666666666428709, -0.7072540797572917093 ) ) ;
#159743=CARTESIAN_POINT ( 'NONE',  ( -0.4500000000000232703, 4.000000000000003553, 0.8338124244295432863 ) ) ;
#159750=ORIENTED_EDGE ( 'NONE', *, *, #42362, .T. ) ;
#159755=ORIENTED_EDGE ( 'NONE', *, *, #117424, .F. ) ;
#159917=EDGE_CURVE ( 'NONE', #164105, #39288, #10180, .T. ) ;
#159924=CIRCLE ( 'NONE', #135660, 0.04999999999999989869 ) ;
#160014=CARTESIAN_POINT ( 'NONE',  ( 1.224999999999963007, 2.458333334016087335, -0.7072540797572877125 ) ) ;
#160015=EDGE_CURVE ( 'NONE', #212450, #30458, #134333, .T. ) ;
#160083=DIRECTION ( 'NONE',  ( -3.330669073875478989E-16, 3.540251991789410786E-16, 1.000000000000000000 ) ) ;
#160092=CARTESIAN_POINT ( 'NONE',  ( -0.3000000000000190292, 3.949999999999967315, 1.007084189318380618 ) ) ;
#160116=CARTESIAN_POINT ( 'NONE',  ( 0.6801582343749952297, 2.255208333674735499, 1.178068619123839866 ) ) ;
#160120=VERTEX_POINT ( 'NONE', #10669 ) ;
#160124=CARTESIAN_POINT ( 'NONE',  ( -0.4465194593918104249, 3.080450244942120719, -0.4155024747329819634 ) ) ;
#160144=VECTOR ( 'NONE', #185807, 1000.000000000000000 ) ;
#160240=CARTESIAN_POINT ( 'NONE',  ( 0.6801582343749970061, 0.8072916670080754198, -1.178068619123858962 ) ) ;
#160273=CARTESIAN_POINT ( 'NONE',  ( 1.878188943807069800, 3.299815425349211129, -0.3999999999999993006 ) ) ;
#160277=ORIENTED_EDGE ( 'NONE', *, *, #20664, .F. ) ;
#160345=DIRECTION ( 'NONE',  ( 0.000000000000000000, 0.000000000000000000, -1.000000000000000000 ) ) ;
#160355=CARTESIAN_POINT ( 'NONE',  ( -0.5000000000000056621, 3.172938907704293765, -0.4000000000000305533 ) ) ;
#160386=ORIENTED_EDGE ( 'NONE', *, *, #138098, .T. ) ;
#160389=LINE ( 'NONE', #79128, #25383 ) ;
#160437=B_SPLINE_CURVE_WITH_KNOTS ( 'NONE', 3,
 ( #161967, #160890, #46089, #146799, #111135, #209606, #48229 ),
 .UNSPECIFIED., .F., .F.,
 ( 4, 3, 4 ),
 ( -2.180065393147345858E-06, 0.000000000000000000, 4.270488675890887276E-05 ),
 .UNSPECIFIED. ) ;
#160450=CARTESIAN_POINT ( 'NONE',  ( -0.3000000000000155320, 3.999999999999955147, 1.007084189318345757 ) ) ;
#160472=CARTESIAN_POINT ( 'NONE',  ( 0.6801582343749952297, 1.088541667008086078, -1.178068619123883165 ) ) ;
#160507=CARTESIAN_POINT ( 'NONE',  ( -0.3978093821461001767, 3.011896635411785983, 0.3978093821460482182 ) ) ;
#160548=ORIENTED_EDGE ( 'NONE', *, *, #207277, .T. ) ;
#160570=CYLINDRICAL_SURFACE ( 'NONE', #168852, 1.224999999999996980 ) ;
#160611=ADVANCED_FACE ( 'NONE', ( #79942 ), #179592, .F. ) ;
#160758=CARTESIAN_POINT ( 'NONE',  ( -0.4123176713736765309, 3.999999999999973799, 0.8977835139437544409 ) ) ;
#160771=CARTESIAN_POINT ( 'NONE',  ( -3.956095110007852622E-14, -1.015624999658570893, 1.570758158831770279 ) ) ;
#160775=VERTEX_POINT ( 'NONE', #11221 ) ;
#160890=CARTESIAN_POINT ( 'NONE',  ( -0.3776192402222604549, 3.049641483663570352, -0.4287046358292799231 ) ) ;
#160893=EDGE_LOOP ( 'NONE', ( #141051, #182875, #45729, #189295, #9748, #66108 ) ) ;
#160909=EDGE_CURVE ( 'NONE', #181560, #102463, #9127, .T. ) ;
#161016=SURFACE_SIDE_STYLE ('',( #128604 ) ) ;
#161083=CARTESIAN_POINT ( 'NONE',  ( 0.6801582343749744686, -0.2760416663252704406, 1.178068619123780802 ) ) ;
#161085=CARTESIAN_POINT ( 'NONE',  ( 0.3094237646162965594, 2.106443173867519437E-14, 1.330970632288056787 ) ) ;
#161187=CARTESIAN_POINT ( 'NONE',  ( 0.6801582343749952297, 1.088541667008086078, -1.178068619123883165 ) ) ;
#161266=DIRECTION ( 'NONE',  ( 1.000000000000000000, 0.000000000000000000, 0.000000000000000000 ) ) ;
#161315=CARTESIAN_POINT ( 'NONE',  ( 1.360316468749973584, 0.7864583336747016373, -0.7853790794159161148 ) ) ;
#161369=CIRCLE ( 'NONE', #81735, 0.09999999999999982514 ) ;
#161387=( BOUNDED_CURVE ( )  B_SPLINE_CURVE ( 2, ( #62804, #158201, #76917, #143043, #92147, #44452, #176571, #93211, #178710 ),
 .UNSPECIFIED., .F., .T. ) 
 B_SPLINE_CURVE_WITH_KNOTS ( ( 3, 2, 2, 2, 3 ),
 ( 0.6406250000000002220, 0.6458333333333333703, 0.6562500000000000000, 0.6666666666666666297, 0.6718749999999998890 ),
 .UNSPECIFIED. ) 
 CURVE ( )  GEOMETRIC_REPRESENTATION_ITEM ( )  RATIONAL_B_SPLINE_CURVE ( ( 0.9330127018922194093, 0.9330127018922221849, 1.000000000000000000, 0.8660254037844387076, 1.000000000000000000, 0.8660254037844387076, 1.000000000000000000, 0.9330127018922207416, 0.9330127018922192983 ) ) 
 REPRESENTATION_ITEM ( '' )  );
#161442=FACE_OUTER_BOUND ( 'NONE', #150346, .T. ) ;
#161457=CARTESIAN_POINT ( 'NONE',  ( 1.224999999999958789, 0.8541666666667161456, 0.7072540797572558491 ) ) ;
#161481=CARTESIAN_POINT ( 'NONE',  ( 0.6124999999999776179, 1.479166667349464337, -1.060881119635962211 ) ) ;
#161553=CARTESIAN_POINT ( 'NONE',  ( 1.360316468749971364, 0.04687500034143698979, -3.469446951953614189E-14 ) ) ;
#161554=CARTESIAN_POINT ( 'NONE',  ( -0.4254946254914159787, 3.044090126848159716, 0.4192457809233481880 ) ) ;
#161592=EDGE_CURVE ( 'NONE', #95302, #126635, #654, .T. ) ;
#161593=CARTESIAN_POINT ( 'NONE',  ( -0.6801582343750004478, 2.598958333674746157, -1.178068619123848526 ) ) ;
#161688=ORIENTED_EDGE ( 'NONE', *, *, #146265, .T. ) ;
#161696=ORIENTED_EDGE ( 'NONE', *, *, #110826, .T. ) ;
#161765=CARTESIAN_POINT ( 'NONE',  ( -0.4500000000000339839, 3.999999999999980904, -0.8338124244296073462 ) ) ;
#161766=EDGE_CURVE ( 'NONE', #205644, #88486, #196640, .T. ) ;
#161776=( BOUNDED_CURVE ( )  B_SPLINE_CURVE ( 3, ( #127561, #193529, #28904, #80851 ),
 .UNSPECIFIED., .F., .T. ) 
 B_SPLINE_CURVE_WITH_KNOTS ( ( 4, 4 ),
 ( 4.712388980384627502, 6.283185307179586232 ),
 .UNSPECIFIED. ) 
 CURVE ( )  GEOMETRIC_REPRESENTATION_ITEM ( )  RATIONAL_B_SPLINE_CURVE ( ( 1.000000000000000000, 0.8047378541243503935, 0.8047378541243503935, 1.000000000000000000 ) ) 
 REPRESENTATION_ITEM ( '' )  );
#161780=CARTESIAN_POINT ( 'NONE',  ( 0.3776192402222143807, 3.049641483663593888, 0.4287046358292035952 ) ) ;
#161798=CARTESIAN_POINT ( 'NONE',  ( -1.225000000000038058, 0.08333333401614038960, 0.7072540797572558491 ) ) ;
#161799=CARTESIAN_POINT ( 'NONE',  ( 0.3000000000000016542, 4.000000000000003553, -1.007084189318387502 ) ) ;
#161851=CARTESIAN_POINT ( 'NONE',  ( 1.360316468749969809, -0.6822916663252893699, -0.7853790794159082322 ) ) ;
#161894=CYLINDRICAL_SURFACE ( 'NONE', #170331, 1.224999999999996980 ) ;
#161967=CARTESIAN_POINT ( 'NONE',  ( -0.3769810270651957618, 3.049942316455299451, -0.4288785890453079008 ) ) ;
#162041=( BOUNDED_CURVE ( )  B_SPLINE_CURVE ( 2, ( #102510, #168572, #205326, #126044, #159528 ),
 .UNSPECIFIED., .F., .T. ) 
 B_SPLINE_CURVE_WITH_KNOTS ( ( 3, 2, 3 ),
 ( 0.7343749999999997780, 0.7395833333333319271, 0.7499999999999956701 ),
 .UNSPECIFIED. ) 
 CURVE ( )  GEOMETRIC_REPRESENTATION_ITEM ( )  RATIONAL_B_SPLINE_CURVE ( ( 0.9330127018922194093, 0.9330127018922165227, 1.000000000000000000, 0.8660254037844944408, 0.9999999999999442668 ) ) 
 REPRESENTATION_ITEM ( '' )  );
#162102=CARTESIAN_POINT ( 'NONE',  ( 1.360316468749964480, 2.796875000341370043, -3.989863994746656317E-14 ) ) ;
#162110=DIRECTION ( 'NONE',  ( 1.276756478318932585E-15, -1.000000000000000000, 1.665334536937738262E-16 ) ) ;
#162147=ORIENTED_EDGE ( 'NONE', *, *, #161592, .T. ) ;
#162158=CARTESIAN_POINT ( 'NONE',  ( -1.360316468750021768, -1.109374999658574446, -3.122502256758252770E-14 ) ) ;
#162204=CARTESIAN_POINT ( 'NONE',  ( 0.4465194593917913846, 3.080450244942120719, -0.4155024747329958412 ) ) ;
#162255=CARTESIAN_POINT ( 'NONE',  ( 1.360316468750005781, 1.567708333674729504, -0.7853790794158981292 ) ) ;
#162381=DIRECTION ( 'NONE',  ( -1.276756478318932585E-15, 1.000000000000000000, -1.665334536937738262E-16 ) ) ;
#162387=CARTESIAN_POINT ( 'NONE',  ( -0.6801582343750074422, 0.5989583336747372755, -1.178068619123841643 ) ) ;
#162406=CARTESIAN_POINT ( 'NONE',  ( 0.3282377607281116716, 2.073664549684627545, 1.224999999999953015 ) ) ;
#162554=CARTESIAN_POINT ( 'NONE',  ( -1.225000000000036282, 2.291666667349470554, -0.7072540797573277915 ) ) ;
#162571=CARTESIAN_POINT ( 'NONE',  ( 0.3817069231124535778, 3.999999999999974243, -1.007084182327222965 ) ) ;
#162614=CARTESIAN_POINT ( 'NONE',  ( -2.353626204688216217E-14, 0.7343750003414536431, 1.570758158831780271 ) ) ;
#162655=CARTESIAN_POINT ( 'NONE',  ( -1.360316468750034646, 2.619791667008062319, -0.7853790794159261068 ) ) ;
#162678=ORIENTED_EDGE ( 'NONE', *, *, #117402, .F. ) ;
#162864=CARTESIAN_POINT ( 'NONE',  ( -1.225000000000046052, 0.04166666734950023182, -0.7072540797573217963 ) ) ;
#162901=CARTESIAN_POINT ( 'NONE',  ( -0.3645075752536136582, 3.999999999999973799, 0.9782388703846811584 ) ) ;
#162912=CARTESIAN_POINT ( 'NONE',  ( 1.360316468749997565, 2.744791667008062763, 0.7853790794158921340 ) ) ;
#162929=FACE_OUTER_BOUND ( 'NONE', #175842, .T. ) ;
#162974=CARTESIAN_POINT ( 'NONE',  ( -0.3282377607281317111, 0.4486645496846296544, -1.225000000000047828 ) ) ;
#163032=VECTOR ( 'NONE', #135260, 1000.000000000000000 ) ;
#163067=VERTEX_POINT ( 'NONE', #161799 ) ;
#163223=CARTESIAN_POINT ( 'NONE',  ( 1.360316468749977581, -0.2135416663252950598, -0.7853790794159261068 ) ) ;
#163291=EDGE_CURVE ( 'NONE', #12920, #116778, #201203, .T. ) ;
#163319=CARTESIAN_POINT ( 'NONE',  ( -1.360316468750038865, 1.651041667008089853, -0.7853790794159041244 ) ) ;
#163344=DIRECTION ( 'NONE',  ( -3.330669073875478989E-16, 3.330669073875478989E-16, 1.000000000000000000 ) ) ;
#163373=CARTESIAN_POINT ( 'NONE',  ( 0.3999999999999906408, 3.949999999999988187, -0.8338124244295798126 ) ) ;
#163450=CARTESIAN_POINT ( 'NONE',  ( -1.360316468750030428, -0.6093749996585878792, -1.908195823574487804E-14 ) ) ;
#163516=CARTESIAN_POINT ( 'NONE',  ( 0.3878679656440017220, 3.999999999999996891, 1.007084189318337542 ) ) ;
#163547=CARTESIAN_POINT ( 'NONE',  ( -0.5000000000000073275, 3.299999999999997158, 0.4999999999999917843 ) ) ;
#163637=CARTESIAN_POINT ( 'NONE',  ( 0.4499999960734660243, 3.999999999999974243, -0.9281957781481884329 ) ) ;
#163641=VECTOR ( 'NONE', #35769, 1000.000000000000000 ) ;
#163681=CARTESIAN_POINT ( 'NONE',  ( 0.6801582343749847936, 0.5052083336747614783, 1.178068619123803451 ) ) ;
#163718=CARTESIAN_POINT ( 'NONE',  ( -1.214306433183764966E-14, 3.299999999999969624, -3.122502256758252770E-14 ) ) ;
#163719=CARTESIAN_POINT ( 'NONE',  ( 1.360316468749965590, 2.494791667008093849, 0.7853790794158861388 ) ) ;
#163745=SPHERICAL_SURFACE ( 'NONE', #193218, 0.05000000000000000278 ) ;
#163826=ADVANCED_FACE ( 'NONE', ( #80843 ), #31089, .F. ) ;
#163860=VECTOR ( 'NONE', #51090, 1000.000000000000000 ) ;
#163900=DIRECTION ( 'NONE',  ( -3.330669073875479482E-16, 3.330669073875479482E-16, 1.000000000000000000 ) ) ;
#163913=CARTESIAN_POINT ( 'NONE',  ( 5.884182030513498086E-16, 2.999999999999988898, -1.225000000000007638 ) ) ;
#163922=ORIENTED_EDGE ( 'NONE', *, *, #163291, .F. ) ;
#163933=CARTESIAN_POINT ( 'NONE',  ( -1.225000000000004086, 1.979166666666657193, -0.7072540797572898219 ) ) ;
#163940=AXIS2_PLACEMENT_3D ( 'NONE', #9028, #205076, #137977 ) ;
#163980=CARTESIAN_POINT ( 'NONE',  ( -1.360316468750010666, 2.869791667008063651, -0.7853790794158961308 ) ) ;
#163984=ORIENTED_EDGE ( 'NONE', *, *, #5066, .F. ) ;
#164105=VERTEX_POINT ( 'NONE', #189932 ) ;
#164121=CARTESIAN_POINT ( 'NONE',  ( -1.225000000000019407, 2.500000000000009326, -1.387778780781445676E-14 ) ) ;
#164213=( NAMED_UNIT ( * ) PLANE_ANGLE_UNIT ( ) SI_UNIT ( $, .RADIAN. ) );
#164381=CARTESIAN_POINT ( 'NONE',  ( 0.6801582343749900117, 1.588541667008100511, -1.178068619123890270 ) ) ;
#164391=CARTESIAN_POINT ( 'NONE',  ( -1.734723475976807094E-15, 2.999999999999988898, -6.938893903907228378E-15 ) ) ;
#164428=CARTESIAN_POINT ( 'NONE',  ( 0.4000000000000019096, 3.964661556059719594, -0.9099571394229579724 ) ) ;
#164441=FACE_OUTER_BOUND ( 'NONE', #11427, .T. ) ;
#164508=CARTESIAN_POINT ( 'NONE',  ( -1.360316468750044860, -0.8385416663252739378, 0.7853790794158720390 ) ) ;
#164529=CARTESIAN_POINT ( 'NONE',  ( -5.758872628492444169E-14, 2.203125000341452200, 1.570758158831754070 ) ) ;
#164560=CARTESIAN_POINT ( 'NONE',  ( 1.826099658463333775, 3.981846818257634979, -0.4000000000000274447 ) ) ;
#164598=AXIS2_PLACEMENT_3D ( 'NONE', #159717, #93675, #14510 ) ;
#164640=CARTESIAN_POINT ( 'NONE',  ( -1.893304937267642707, 3.295344712542805254, 0.4038802767148285677 ) ) ;
#164657=CARTESIAN_POINT ( 'NONE',  ( -0.4500000000000389244, 3.999999999999948042, 0.4999999999999779066 ) ) ;
#164710=SPHERICAL_SURFACE ( 'NONE', #196208, 0.05000000000000000278 ) ;
#164729=CARTESIAN_POINT ( 'NONE',  ( -0.6801582343750334214, 1.213541667008023683, 1.178068619123810334 ) ) ;
#164772=CARTESIAN_POINT ( 'NONE',  ( 1.360316468749966257, 1.765625000341414230, -3.642919299551294898E-14 ) ) ;
#164796=DIRECTION ( 'NONE',  ( -1.276756478318932191E-15, 1.000000000000000000, -3.330669073875483426E-16 ) ) ;
#164874=CARTESIAN_POINT ( 'NONE',  ( 0.4288785890452679883, 3.049942316455285685, 0.3999999999999715450 ) ) ;
#164926=EDGE_LOOP ( 'NONE', ( #133341, #89003, #165865, #202208 ) ) ;
#164969=ORIENTED_EDGE ( 'NONE', *, *, #80620, .T. ) ;
#164978=CARTESIAN_POINT ( 'NONE',  ( 0.4499999999999851341, 4.000000000000003553, 0.8338124244295520571 ) ) ;
#165026=CARTESIAN_POINT ( 'NONE',  ( -1.360316468750002894, -0.3072916663252554526, 0.7853790794158901356 ) ) ;
#165090=CARTESIAN_POINT ( 'NONE',  ( -1.225000000000038058, 0.4791666666666983265, -0.7072540797573158011 ) ) ;
#165121=AXIS2_PLACEMENT_3D ( 'NONE', #31528, #29392, #78125 ) ;
#165198=CARTESIAN_POINT ( 'NONE',  ( -6.158835246850665884E-15, 0.8125000000000031086, 1.224999999999960565 ) ) ;
#165324=EDGE_CURVE ( 'NONE', #189127, #133087, #48874, .T. ) ;
#165344=LINE ( 'NONE', #149093, #151994 ) ;
#165366=CARTESIAN_POINT ( 'NONE',  ( 0.5101186646354113341, -1.387778780781445676E-14, 1.261047121698059215 ) ) ;
#165371=EDGE_LOOP ( 'NONE', ( #208996, #117376, #187001, #6783, #24065, #212545 ) ) ;
#165434=ORIENTED_EDGE ( 'NONE', *, *, #74132, .F. ) ;
#165438=CARTESIAN_POINT ( 'NONE',  ( 1.360316468749957597, 1.776041667008106506, 0.7853790794158801436 ) ) ;
#165444=ADVANCED_FACE ( 'NONE', ( #74876 ), #42398, .F. ) ;
#165503=CYLINDRICAL_SURFACE ( 'NONE', #108410, 0.04999999999999991257 ) ;
#165510=ORIENTED_EDGE ( 'NONE', *, *, #21017, .T. ) ;
#165569=CARTESIAN_POINT ( 'NONE',  ( -7.561650146977034455E-14, -0.5468749996585524631, 1.570758158831754070 ) ) ;
#165593=CARTESIAN_POINT ( 'NONE',  ( -1.953008978358306879E-14, 1.828125000341410678, -1.570758158831798257 ) ) ;
#165609=AXIS2_PLACEMENT_3D ( 'NONE', #11925, #106292, #207987 ) ;
#165684=CARTESIAN_POINT ( 'NONE',  ( -1.893304937267614285, 3.295344712542847887, -0.4038802767149019535 ) ) ;
#165702=FACE_OUTER_BOUND ( 'NONE', #213065, .T. ) ;
#165735=CARTESIAN_POINT ( 'NONE',  ( -1.225000000000010747, 2.312500000682803147, -2.081668171172168513E-14 ) ) ;
#165754=ORIENTED_EDGE ( 'NONE', *, *, #62818, .T. ) ;
#165756=DIRECTION ( 'NONE',  ( 1.276756478318932585E-15, -1.000000000000000000, 1.665334536937738262E-16 ) ) ;
#165800=CARTESIAN_POINT ( 'NONE',  ( -0.6801582343750403048, -0.5364583329919083710, 1.178068619123807004 ) ) ;
#165838=CARTESIAN_POINT ( 'NONE',  ( -0.6801582343750125492, 1.098958333674737720, -1.178068619123855409 ) ) ;
#165844=DIRECTION ( 'NONE',  ( 1.276756478318932585E-15, -1.000000000000000000, 1.665334536937738262E-16 ) ) ;
#165865=ORIENTED_EDGE ( 'NONE', *, *, #129225, .T. ) ;
#165919=LINE ( 'NONE', #17504, #79169 ) ;
#166013=CARTESIAN_POINT ( 'NONE',  ( -0.3544712801349413911, 3.975028838742715287, -0.9637995819944503717 ) ) ;
#166087=DIRECTION ( 'NONE',  ( -3.330669073875479482E-16, 3.330669073875479482E-16, 1.000000000000000000 ) ) ;
#166093=CARTESIAN_POINT ( 'NONE',  ( -1.360316468750004448, 1.640625000341400241, -2.602085213965210642E-14 ) ) ;
#166314=CARTESIAN_POINT ( 'NONE',  ( -0.3000000000000103140, 3.322650755865456773, 0.5865692111442551981 ) ) ;
#166364=CARTESIAN_POINT ( 'NONE',  ( 1.224999999999984990, 1.104166666666725138, 0.7072540797572737237 ) ) ;
#166395=ORIENTED_EDGE ( 'NONE', *, *, #141897, .T. ) ;
#166410=CARTESIAN_POINT ( 'NONE',  ( 0.5101186646354113341, -1.387778780781445676E-14, 1.261047121698059215 ) ) ;
#166426=EDGE_CURVE ( 'NONE', #154544, #63320, #208177, .T. ) ;
#166512=CARTESIAN_POINT ( 'NONE',  ( 0.6801582343750056658, 0.5885416670080856338, -1.178068619123862515 ) ) ;
#166514=CARTESIAN_POINT ( 'NONE',  ( 1.814759087649938429, 3.975067388631681187, 0.4606438099578180068 ) ) ;
#166560=CARTESIAN_POINT ( 'NONE',  ( 1.224999999999995204, 1.145833333333333259, -0.7072540797572898219 ) ) ;
#166567=CARTESIAN_POINT ( 'NONE',  ( 3.486133158594716510E-16, 0.8750000006828204668, 1.224999999999968336 ) ) ;
#166662=CYLINDRICAL_SURFACE ( 'NONE', #192911, 1.224999999999996980 ) ;
#166663=CARTESIAN_POINT ( 'NONE',  ( 0.6124999999999914957, 2.083333333333339699, 1.060881119635884051 ) ) ;
#166666=CARTESIAN_POINT ( 'NONE',  ( 1.360316468749963592, 1.244791667008120051, 0.7853790794158760358 ) ) ;
#166783=B_SPLINE_CURVE_WITH_KNOTS ( 'NONE', 3,
 ( #6388, #56232, #188350, #39990 ),
 .UNSPECIFIED., .F., .F.,
 ( 4, 4 ),
 ( 0.000000000000000000, 1.930757672285080358E-06 ),
 .UNSPECIFIED. ) ;
#166830=CARTESIAN_POINT ( 'NONE',  ( -0.6125000000000262457, 2.791666666666692276, 1.060881119635882497 ) ) ;
#166831=CARTESIAN_POINT ( 'NONE',  ( -0.3282377607281317666, 0.3013354503153871100, 1.224999999999968114 ) ) ;
#166868=CARTESIAN_POINT ( 'NONE',  ( 1.360316468749955598, -0.7239583329918893861, 0.7853790794158480582 ) ) ;
#166870=( BOUNDED_CURVE ( )  B_SPLINE_CURVE ( 2, ( #121170, #5160, #200173, #38768, #70169, #135224, #34486, #170895, #154655 ),
 .UNSPECIFIED., .F., .T. ) 
 B_SPLINE_CURVE_WITH_KNOTS ( ( 3, 2, 2, 2, 3 ),
 ( 0.2968749999999998335, 0.3020833333333333148, 0.3125000000000000000, 0.3229166666666666852, 0.3281250000000001665 ),
 .UNSPECIFIED. ) 
 CURVE ( )  GEOMETRIC_REPRESENTATION_ITEM ( )  RATIONAL_B_SPLINE_CURVE ( ( 0.9330127018922194093, 0.9330127018922171889, 1.000000000000000000, 0.8660254037844387076, 1.000000000000000000, 0.8660254037844387076, 1.000000000000000000, 0.9330127018922171889, 0.9330127018922194093 ) ) 
 REPRESENTATION_ITEM ( '' )  );
#166911=CARTESIAN_POINT ( 'NONE',  ( -1.360316468750062624, 1.619791667008073865, -0.7853790794159302147 ) ) ;
#166929=VECTOR ( 'NONE', #16767, 1000.000000000000000 ) ;
#167037=EDGE_LOOP ( 'NONE', ( #148358, #16664, #39060, #7962, #91651 ) ) ;
#167053=CARTESIAN_POINT ( 'NONE',  ( -0.3000000000000103140, 3.372708439410163184, -0.5000000000000056621 ) ) ;
#167204=CARTESIAN_POINT ( 'NONE',  ( 1.224999999999928812, 2.208333334016110427, -0.7072540797573098059 ) ) ;
#167264=TOROIDAL_SURFACE ( 'NONE', #73876, 1.829047314007947955, 0.05000000000000000278 ) ;
#167378=CARTESIAN_POINT ( 'NONE',  ( 1.874158809982156670, 3.299964346911599122, 0.3999999999999681033 ) ) ;
#167398=CIRCLE ( 'NONE', #1318, 0.1000000000000000472 ) ;
#167414=CARTESIAN_POINT ( 'NONE',  ( -1.947569660854454598, 3.752493983412270140, -0.4616071351974295189 ) ) ;
#167417=CARTESIAN_POINT ( 'NONE',  ( -0.6801582343750420812, 1.880208333674727950, -1.178068619123883165 ) ) ;
#167437=CARTESIAN_POINT ( 'NONE',  ( 0.6124999999999967137, 0.5833333333333314830, 1.060881119635929348 ) ) ;
#167451=CIRCLE ( 'NONE', #132988, 0.09999999999999971412 ) ;
#167476=CARTESIAN_POINT ( 'NONE',  ( 0.3999999999999442890, 3.322650755865476757, 0.5865692111442147860 ) ) ;
#167581=CARTESIAN_POINT ( 'NONE',  ( 1.360316468749971364, 0.04687500034143698979, -3.469446951953614189E-14 ) ) ;
#167615=LINE ( 'NONE', #5076, #88142 ) ;
#167728=CARTESIAN_POINT ( 'NONE',  ( 0.6801582343749865700, 2.307291667008083635, -1.178068619123879834 ) ) ;
#167735=LINE ( 'NONE', #66999, #163032 ) ;
#167761=EDGE_CURVE ( 'NONE', #102576, #182627, #3986, .T. ) ;
#167802=CARTESIAN_POINT ( 'NONE',  ( -1.225000000000060263, 2.729166666666693164, -0.7072540797573217963 ) ) ;
#167815=CARTESIAN_POINT ( 'NONE',  ( -1.911175648939902105, 3.243131119507697502, -0.4542559028653506692 ) ) ;
#167844=ORIENTED_EDGE ( 'NONE', *, *, #205468, .T. ) ;
#167852=VECTOR ( 'NONE', #57095, 1000.000000000000000 ) ;
#167892=CARTESIAN_POINT ( 'NONE',  ( -3.154860657348034577E-14, -1.124999999317153332, 1.414508159514557439 ) ) ;
#167899=CIRCLE ( 'NONE', #78073, 0.05000000000000008604 ) ;
#167919=CARTESIAN_POINT ( 'NONE',  ( 1.224999999999958789, 1.166666667349521624, 0.7072540797572417492 ) ) ;
#167929=CARTESIAN_POINT ( 'NONE',  ( 1.360316468749979801, -0.9322916663252904801, -0.7853790794159041244 ) ) ;
#167968=CARTESIAN_POINT ( 'NONE',  ( 0.6801582343749952297, 1.807291667008069425, -1.178068619123869398 ) ) ;
#167990=ORIENTED_EDGE ( 'NONE', *, *, #15653, .T. ) ;
#167991=ORIENTED_EDGE ( 'NONE', *, *, #187759, .T. ) ;
#168065=TOROIDAL_SURFACE ( 'NONE', #50091, 1.829047314007947955, 0.05000000000000000278 ) ;
#168172=ORIENTED_EDGE ( 'NONE', *, *, #11493, .T. ) ;
#168176=CARTESIAN_POINT ( 'NONE',  ( -1.225000000000005640, 2.812500000682796486, -1.734723475976807094E-15 ) ) ;
#168197=EDGE_LOOP ( 'NONE', ( #174054, #84983, #201734, #90992 ) ) ;
#168265=CARTESIAN_POINT ( 'NONE',  ( 1.224999999999991651, 2.437500000682837786, -4.336808689942017736E-14 ) ) ;
#168283=B_SPLINE_CURVE_WITH_KNOTS ( 'NONE', 3,
 ( #208601, #151621, #26664, #3187, #120245, #109061, #201393 ),
 .UNSPECIFIED., .F., .F.,
 ( 4, 3, 4 ),
 ( 2.109323616200222937E-18, 2.617081137855649704E-05, 3.552777339501059120E-05 ),
 .UNSPECIFIED. ) ;
#168351=ORIENTED_EDGE ( 'NONE', *, *, #150248, .T. ) ;
#168453=CARTESIAN_POINT ( 'NONE',  ( -1.772826578343109416, 3.949999999999995293, -0.4000000000000270561 ) ) ;
#168473=CARTESIAN_POINT ( 'NONE',  ( -1.360316468750021768, 1.421875000341424222, -4.510281037539698445E-14 ) ) ;
#168496=CARTESIAN_POINT ( 'NONE',  ( 1.224999999999979661, 0.6249999999999866773, -2.775557561562891351E-14 ) ) ;
#168515=VERTEX_POINT ( 'NONE', #199267 ) ;
#168529=ORIENTED_EDGE ( 'NONE', *, *, #2174, .F. ) ;
#168572=CARTESIAN_POINT ( 'NONE',  ( -0.3282377607281391496, 0.05133545031538289116, 1.224999999999979217 ) ) ;
#168642=CARTESIAN_POINT ( 'NONE',  ( 1.360316468749939833, 0.02604166700813021276, 0.7853790794158660438 ) ) ;
#168708=( BOUNDED_CURVE ( )  B_SPLINE_CURVE ( 2, ( #4283, #71424, #69289, #35744, #34678, #21594, #120277, #88784, #171076 ),
 .UNSPECIFIED., .F., .T. ) 
 B_SPLINE_CURVE_WITH_KNOTS ( ( 3, 2, 2, 2, 3 ),
 ( 0.2031250000000002220, 0.2083333333333333426, 0.2187500000000000000, 0.2291666666666666574, 0.2343749999999998057 ),
 .UNSPECIFIED. ) 
 CURVE ( )  GEOMETRIC_REPRESENTATION_ITEM ( )  RATIONAL_B_SPLINE_CURVE ( ( 0.9330127018922194093, 0.9330127018922221849, 1.000000000000000000, 0.8660254037844387076, 1.000000000000000000, 0.8660254037844387076, 1.000000000000000000, 0.9330127018922218518, 0.9330127018922194093 ) ) 
 REPRESENTATION_ITEM ( '' )  );
#168790=CARTESIAN_POINT ( 'NONE',  ( -3.956095110007852622E-14, 2.328125000341396689, -1.570758158831800255 ) ) ;
#168793=EDGE_CURVE ( 'NONE', #184329, #179126, #168283, .T. ) ;
#168852=AXIS2_PLACEMENT_3D ( 'NONE', #210373, #80389, #146485 ) ;
#168892=DIRECTION ( 'NONE',  ( -1.276756478318931402E-15, 1.000000000000000000, 0.000000000000000000 ) ) ;
#168895=CARTESIAN_POINT ( 'NONE',  ( -1.907862554904952379, 3.236716050607317818, 0.4606469147255249363 ) ) ;
#168952=CARTESIAN_POINT ( 'NONE',  ( -1.225000000000034284, -0.4166666659838699771, 0.7072540797572656190 ) ) ;
#168990=CARTESIAN_POINT ( 'NONE',  ( 1.360316468750003782, -0.1822916663252708847, -0.7853790794158961308 ) ) ;
#169029=CARTESIAN_POINT ( 'NONE',  ( -1.360316468750072838, 1.661458333674769694, 0.7853790794158600486 ) ) ;
#169074=VERTEX_POINT ( 'NONE', #209666 ) ;
#169245=CARTESIAN_POINT ( 'NONE',  ( -1.734723475976807094E-15, 2.999999999999988898, -6.938893903907228378E-15 ) ) ;
#169309=EDGE_LOOP ( 'NONE', ( #23311, #10938, #150687, #26930, #203145, #95490, #1804, #186469, #142613, #134076, #65242, #56993, #198336, #60845, #159755, #205108, #21021, #114919, #15006, #132790, #137445, #32134, #136043, #14804, #44784, #8974 ) ) ;
#169332=CARTESIAN_POINT ( 'NONE',  ( 1.224999999999992983, 1.458333334016138849, -0.7072540797572817173 ) ) ;
#169333=CARTESIAN_POINT ( 'NONE',  ( -0.4500000000000545231, 4.000000000000003553, -0.8338124244296075682 ) ) ;
#169388=CARTESIAN_POINT ( 'NONE',  ( -1.225000000000010747, 1.500000000000008216, -8.673617379884035472E-15 ) ) ;
#169449=CARTESIAN_POINT ( 'NONE',  ( 0.4032277238576422174, 3.019957635004400842, -0.4115402804778697243 ) ) ;
#169516=ORIENTED_EDGE ( 'NONE', *, *, #79132, .T. ) ;
#169540=CARTESIAN_POINT ( 'NONE',  ( 1.360316468749997565, 2.067708333674723509, -0.7853790794159001276 ) ) ;
#169563=CARTESIAN_POINT ( 'NONE',  ( -1.225000000000040057, 0.7708333333333476922, 0.7072540797572656190 ) ) ;
#169710=CARTESIAN_POINT ( 'NONE',  ( -1.360316468750014884, 0.1927083336747308917, 0.7853790794158901356 ) ) ;
#169756=FACE_OUTER_BOUND ( 'NONE', #196878, .T. ) ;
#169856=CARTESIAN_POINT ( 'NONE',  ( -1.360316468750007779, 0.1406250003413919702, -1.734723475976807094E-15 ) ) ;
#169957=CARTESIAN_POINT ( 'NONE',  ( -1.913201741516695087, 3.249623237789911023, 0.4478572873795984566 ) ) ;
#169962=TOROIDAL_SURFACE ( 'NONE', #197639, 0.05000000000000000278, 0.05000000000000000278 ) ;
#169971=( BOUNDED_CURVE ( )  B_SPLINE_CURVE ( 3, ( #169333, #35047, #104344, #133673 ),
 .UNSPECIFIED., .F., .T. ) 
 B_SPLINE_CURVE_WITH_KNOTS ( ( 4, 4 ),
 ( 1.570796326795096620, 3.141592653589643014 ),
 .UNSPECIFIED. ) 
 CURVE ( )  GEOMETRIC_REPRESENTATION_ITEM ( )  RATIONAL_B_SPLINE_CURVE ( ( 1.000000000000000000, 0.8047378541244475381, 0.8047378541244475381, 1.000000000000000000 ) ) 
 REPRESENTATION_ITEM ( '' )  );
#169985=ORIENTED_EDGE ( 'NONE', *, *, #84896, .T. ) ;
#170013=CARTESIAN_POINT ( 'NONE',  ( -0.6125000000000401235, -0.3958333326505372729, 1.060881119635892933 ) ) ;
#170021=CYLINDRICAL_SURFACE ( 'NONE', #120457, 0.09999999999999961697 ) ;
#170029=FACE_OUTER_BOUND ( 'NONE', #89774, .T. ) ;
#170049=CARTESIAN_POINT ( 'NONE',  ( 1.360316468749973140, -0.2031249996586187434, -5.030698080332740574E-14 ) ) ;
#170082=CARTESIAN_POINT ( 'NONE',  ( 1.360316468749963592, 1.244791667008120051, 0.7853790794158760358 ) ) ;
#170090=CARTESIAN_POINT ( 'NONE',  ( -4.757329562667670667E-14, 0.5781250003414448724, -1.570758158831812246 ) ) ;
#170186=EDGE_LOOP ( 'NONE', ( #172375, #79155, #192232, #198637 ) ) ;
#170222=CARTESIAN_POINT ( 'NONE',  ( 0.3769810270647828698, 3.049942316455306113, 0.4288785890452298522 ) ) ;
#170308=CARTESIAN_POINT ( 'NONE',  ( 1.224999999999968781, 0.6666666673495352802, 0.7072540797572596238 ) ) ;
#170331=AXIS2_PLACEMENT_3D ( 'NONE', #209533, #12407, #64377 ) ;
#170387=CARTESIAN_POINT ( 'NONE',  ( -5.157946788997579689E-14, 2.000000000682813805, -1.414508159514627383 ) ) ;
#170498=ORIENTED_EDGE ( 'NONE', *, *, #2927, .T. ) ;
#170512=CARTESIAN_POINT ( 'NONE',  ( 0.4307572970102537813, 3.041534709929992975, -0.4240169840791682132 ) ) ;
#170552=EDGE_CURVE ( 'NONE', #126346, #23033, #211334, .T. ) ;
#170601=CARTESIAN_POINT ( 'NONE',  ( -0.6801582343750368631, 2.130208333674714183, -1.178068619123862515 ) ) ;
#170625=CARTESIAN_POINT ( 'NONE',  ( 0.6125000000000001554, 1.166666666666656083, -1.060881119635941339 ) ) ;
#170658=ORIENTED_EDGE ( 'NONE', *, *, #195789, .F. ) ;
#170664=ORIENTED_EDGE ( 'NONE', *, *, #144905, .T. ) ;
#170722=CARTESIAN_POINT ( 'NONE',  ( 0.6311622855796304998, 3.199999999999987743, -0.4000000000000236144 ) ) ;
#170740=EDGE_CURVE ( 'NONE', #22081, #118779, #130611, .T. ) ;
#170783=VERTEX_POINT ( 'NONE', #81780 ) ;
#170895=CARTESIAN_POINT ( 'NONE',  ( -0.3282377607281367626, 1.698664549684633096, -1.225000000000013411 ) ) ;
#170922=CARTESIAN_POINT ( 'NONE',  ( -0.6801582343750143256, 0.3489583336747370534, -1.178068619123865846 ) ) ;
#170968=EDGE_CURVE ( 'NONE', #150426, #134733, #16754, .T. ) ;
#170974=CARTESIAN_POINT ( 'NONE',  ( -1.873515663034567291, 3.299988112486733627, 0.3999999999999993006 ) ) ;
#170994=CARTESIAN_POINT ( 'NONE',  ( -1.225000000000028066, 2.020833333333377446, 0.7072540797572697269 ) ) ;
#170995=ADVANCED_FACE ( 'NONE', ( #70825 ), #82837, .F. ) ;
#171076=CARTESIAN_POINT ( 'NONE',  ( -1.743066579297358008E-15, 1.875000000682791379, 1.224999999999958566 ) ) ;
#171083=CARTESIAN_POINT ( 'NONE',  ( -1.225000000000045386, -0.9374999993171719836, -5.551115123125782702E-14 ) ) ;
#171129=VECTOR ( 'NONE', #37541, 1000.000000000000114 ) ;
#171136=CARTESIAN_POINT ( 'NONE',  ( -1.814759087649988833, 3.975067388631688292, -0.4606438099578630818 ) ) ;
#171137=CARTESIAN_POINT ( 'NONE',  ( -1.772826578343109416, 3.949999999999995293, -0.4000000000000270561 ) ) ;
#171154=CARTESIAN_POINT ( 'NONE',  ( 1.360316468750000896, 2.515625000341401130, -3.469446951953614189E-15 ) ) ;
#171163=CARTESIAN_POINT ( 'NONE',  ( 1.360316468749971586, 0.008342803999308550170, 0.2745256636459995070 ) ) ;
#171194=DIRECTION ( 'NONE',  ( 1.276756478318932585E-15, -1.000000000000000000, 1.665334536937738262E-16 ) ) ;
#171254=( BOUNDED_CURVE ( )  B_SPLINE_CURVE ( 2, ( #141244, #157465, #176902, #56748, #108767, #90322, #61014, #24220, #205106 ),
 .UNSPECIFIED., .F., .T. ) 
 B_SPLINE_CURVE_WITH_KNOTS ( ( 3, 2, 2, 2, 3 ),
 ( 0.5781250000000001110, 0.5833333333333333703, 0.5937500000000000000, 0.6041666666666666297, 0.6093749999999997780 ),
 .UNSPECIFIED. ) 
 CURVE ( )  GEOMETRIC_REPRESENTATION_ITEM ( )  RATIONAL_B_SPLINE_CURVE ( ( 0.9330127018922192983, 0.9330127018922207416, 1.000000000000000000, 0.8660254037844387076, 1.000000000000000000, 0.8660254037844387076, 1.000000000000000000, 0.9330127018922221849, 0.9330127018922194093 ) ) 
 REPRESENTATION_ITEM ( '' )  );
#171264=ORIENTED_EDGE ( 'NONE', *, *, #138892, .T. ) ;
#171350=VECTOR ( 'NONE', #165844, 1000.000000000000000 ) ;
#171384=CARTESIAN_POINT ( 'NONE',  ( -0.6801582343750229853, 1.380208333674720622, -1.178068619123855409 ) ) ;
#171411=EDGE_CURVE ( 'NONE', #43349, #56038, #152116, .T. ) ;
#171466=CARTESIAN_POINT ( 'NONE',  ( -1.352083138863443345E-14, 1.500000000682843115, -1.414508159514601626 ) ) ;
#171547=EDGE_CURVE ( 'NONE', #108528, #132409, #41584, .T. ) ;
#171576=VERTEX_POINT ( 'NONE', #174791 ) ;
#171597=AXIS2_PLACEMENT_3D ( 'NONE', #50931, #186241, #37876 ) ;
#171670=CARTESIAN_POINT ( 'NONE',  ( -0.6801582343750316451, 0.2135416670080853008, 1.178068619123807004 ) ) ;
#171693=CARTESIAN_POINT ( 'NONE',  ( -1.360316468750058627, 2.692708333674814991, 0.7853790794158641564 ) ) ;
#171725=ORIENTED_EDGE ( 'NONE', *, *, #114638, .T. ) ;
#171986=ORIENTED_EDGE ( 'NONE', *, *, #137088, .T. ) ;
#172005=CARTESIAN_POINT ( 'NONE',  ( 5.007715329123863766E-16, 0.8281250003414059035, -1.570758158831786266 ) ) ;
#172024=CARTESIAN_POINT ( 'NONE',  ( 1.813763795902409548, 4.000000000000003553, -0.4500000000000250466 ) ) ;
#172056=DIRECTION ( 'NONE',  ( -3.330669073875725015E-16, 0.000000000000000000, 1.000000000000000000 ) ) ;
#172077=CARTESIAN_POINT ( 'NONE',  ( -1.225000000000014078, 1.479166666666654972, -0.7072540797573018123 ) ) ;
#172157=CARTESIAN_POINT ( 'NONE',  ( 0.4626273691814121181, 3.108307088186288869, -0.4053073865230417128 ) ) ;
#172210=CIRCLE ( 'NONE', #78803, 0.04999999999999991257 ) ;
#172227=CARTESIAN_POINT ( 'NONE',  ( 0.4465194593917913846, 3.080450244942120719, -0.4155024747329958412 ) ) ;
#172238=CARTESIAN_POINT ( 'NONE',  ( -0.6801582343750316451, 2.098958333674738608, -1.178068619123862515 ) ) ;
#172269=CARTESIAN_POINT ( 'NONE',  ( 1.907862554904935060, 3.236716050607304052, -0.4606469147255498608 ) ) ;
#172283=CARTESIAN_POINT ( 'NONE',  ( 1.224999999999965006, 2.395833333333299286, -0.7072540797573078075 ) ) ;
#172308=CARTESIAN_POINT ( 'NONE',  ( 0.3999999999999576672, 3.949999999999981526, 0.8338124244295311849 ) ) ;
#172375=ORIENTED_EDGE ( 'NONE', *, *, #61547, .F. ) ;
#172423=CARTESIAN_POINT ( 'NONE',  ( -1.734723475976807094E-15, 2.999999999999988898, -6.938893903907228378E-15 ) ) ;
#172467=CARTESIAN_POINT ( 'NONE',  ( -0.6801582343750403048, 2.463541667008038782, 1.178068619123829430 ) ) ;
#172546=CARTESIAN_POINT ( 'NONE',  ( -0.6125000000000314637, 0.8541666673494846540, 1.060881119635901593 ) ) ;
#172583=CIRCLE ( 'NONE', #10058, 0.04999999999999991257 ) ;
#172680=CARTESIAN_POINT ( 'NONE',  ( 1.889151116980546385, 3.755413325229098653, -0.4000000000000479283 ) ) ;
#172761=CARTESIAN_POINT ( 'NONE',  ( 0.6801582343749917881, 1.005208333674747934, 1.178068619123807004 ) ) ;
#172784=CARTESIAN_POINT ( 'NONE',  ( -1.225000000000022293, -0.5208333333333224902, -0.7072540797573136917 ) ) ;
#172825=CARTESIAN_POINT ( 'NONE',  ( -0.6125000000000262457, 2.604166667349451458, 1.060881119635917136 ) ) ;
#172880=CARTESIAN_POINT ( 'NONE',  ( 1.224999999999974332, 2.687500000682768508, -4.163336342344337027E-14 ) ) ;
#172994=CARTESIAN_POINT ( 'NONE',  ( 1.224999999999979217, 2.604166666666692720, 0.7072540797572558491 ) ) ;
#173081=CARTESIAN_POINT ( 'NONE',  ( 1.360316468749949825, 0.2447916670081152490, 0.7853790794158741484 ) ) ;
#173155=CARTESIAN_POINT ( 'NONE',  ( -1.225000000000044276, 1.770833333333392545, 0.7072540797572737237 ) ) ;
#173192=CARTESIAN_POINT ( 'NONE',  ( 0.6801582343750022241, 2.838541667008094738, -1.178068619123834759 ) ) ;
#173195=EDGE_LOOP ( 'NONE', ( #210939, #144432, #194008, #165434 ) ) ;
#173215=LINE ( 'NONE', #107190, #47814 ) ;
#173251=CARTESIAN_POINT ( 'NONE',  ( -0.3275200278799458298, 3.116672424413460263, 0.4674645318177237940 ) ) ;
#173300=CARTESIAN_POINT ( 'NONE',  ( -0.4170821662629279336, 3.033599471985628959, -0.4170821662629279336 ) ) ;
#173312=CARTESIAN_POINT ( 'NONE',  ( 1.360316468749994012, 2.265625000341386919, -1.387778780781445676E-14 ) ) ;
#173322=CARTESIAN_POINT ( 'NONE',  ( -1.360316468750046859, 0.3697916670080757529, -0.7853790794159101196 ) ) ;
#173345=CARTESIAN_POINT ( 'NONE',  ( 1.908029163539552098, 3.237038651130924372, -0.4603255239806359200 ) ) ;
#173419=ORIENTED_EDGE ( 'NONE', *, *, #181736, .F. ) ;
#173550=CARTESIAN_POINT ( 'NONE',  ( 1.743066579297358008E-15, 0.7500000006828128063, -1.225000000000021849 ) ) ;
#173552=CARTESIAN_POINT ( 'NONE',  ( 0.6801582343749900117, 2.005208333674748822, 1.178068619123818994 ) ) ;
#173581=ORIENTED_EDGE ( 'NONE', *, *, #61620, .F. ) ;
#173635=CARTESIAN_POINT ( 'NONE',  ( 0.6124999999999862776, 0.3958333340161462877, 1.060881119635934455 ) ) ;
#173760=CARTESIAN_POINT ( 'NONE',  ( -1.225000000000006084, 2.041666667349461672, -0.7072540797572977045 ) ) ;
#173773=CIRCLE ( 'NONE', #21557, 1.829047314007942848 ) ;
#173842=CARTESIAN_POINT ( 'NONE',  ( 0.6801582343749952297, 1.088541667008086078, -1.178068619123883165 ) ) ;
#173865=CARTESIAN_POINT ( 'NONE',  ( 1.224999999999969225, -0.3541666666666576369, -0.7072540797573098059 ) ) ;
#173885=ADVANCED_FACE ( 'NONE', ( #69180 ), #151541, .T. ) ;
#173915=DIRECTION ( 'NONE',  ( -3.330669073875478496E-16, 1.665334536937734318E-16, 1.000000000000000000 ) ) ;
#173979=EDGE_CURVE ( 'NONE', #133087, #194227, #204293, .T. ) ;
#174034=CARTESIAN_POINT ( 'NONE',  ( 0.2999999999999686806, 3.975028841772344723, -0.9637995837462834947 ) ) ;
#174054=ORIENTED_EDGE ( 'NONE', *, *, #210348, .F. ) ;
#174088=CARTESIAN_POINT ( 'NONE',  ( -1.326716514427061987E-15, 2.999999999999988454, -1.225000000000003864 ) ) ;
#174160=CARTESIAN_POINT ( 'NONE',  ( 1.360316468749985575, 0.2864583336747233422, -0.7853790794158961308 ) ) ;
#174203=CARTESIAN_POINT ( 'NONE',  ( -1.992711204631002198E-15, 2.999999999999989342, 1.224999999999989875 ) ) ;
#174230=CARTESIAN_POINT ( 'NONE',  ( -1.225000000000046052, 2.520833333333404092, 0.7072540797572777205 ) ) ;
#174264=CARTESIAN_POINT ( 'NONE',  ( 1.360316468749978469, 2.296875000341369599, -4.857225732735059864E-14 ) ) ;
#174382=VECTOR ( 'NONE', #139305, 1000.000000000000000 ) ;
#174383=ADVANCED_FACE ( 'NONE', ( #34292 ), #214074, .T. ) ;
#174384=CARTESIAN_POINT ( 'NONE',  ( -1.360316468750040642, 1.161458333674751486, 0.7853790794158861388 ) ) ;
#174390=EDGE_CURVE ( 'NONE', #169074, #181560, #66289, .T. ) ;
#174401=ORIENTED_EDGE ( 'NONE', *, *, #123768, .T. ) ;
#174442=CARTESIAN_POINT ( 'NONE',  ( 0.3769810270647828698, 3.049942316455306113, 0.4288785890452298522 ) ) ;
#174454=DIRECTION ( 'NONE',  ( 3.330669073875478989E-16, -3.540251991789410786E-16, -1.000000000000000000 ) ) ;
#174505=CARTESIAN_POINT ( 'NONE',  ( 1.907519672996849103, 3.236073672982398008, 0.4612874649729346022 ) ) ;
#174533=EDGE_CURVE ( 'NONE', #59826, #53788, #28443, .T. ) ;
#174538=VECTOR ( 'NONE', #163900, 1000.000000000000000 ) ;
#174618=CARTESIAN_POINT ( 'NONE',  ( -6.760415694317216410E-14, 2.234375000341476625, 1.570758158831744078 ) ) ;
#174628=DIRECTION ( 'NONE',  ( -4.440892098500630106E-16, -3.330669073875473073E-16, -1.000000000000000000 ) ) ;
#174655=CARTESIAN_POINT ( 'NONE',  ( -1.734723475976807094E-14, 4.000000000000003553, -1.734723475976807094E-14 ) ) ;
#174697=CARTESIAN_POINT ( 'NONE',  ( -4.557020949502716471E-14, 0.2500000006828292376, -1.414508159514595409 ) ) ;
#174779=FACE_OUTER_BOUND ( 'NONE', #54386, .T. ) ;
#174791=CARTESIAN_POINT ( 'NONE',  ( -1.814759087649955749, 3.975067388631681187, 0.4606438099578266665 ) ) ;
#174806=CARTESIAN_POINT ( 'NONE',  ( 0.3999999999999802047, 3.950000000000008171, 0.8338124244295502807 ) ) ;
#174827=CARTESIAN_POINT ( 'NONE',  ( 2.672702088255949078E-15, 1.937500000000013323, -1.225000000000018074 ) ) ;
#174868=CARTESIAN_POINT ( 'NONE',  ( -1.162044386198238738E-15, 2.937500000000009326, -1.225000000000010303 ) ) ;
#174880=DIRECTION ( 'NONE',  ( -1.276756478318932585E-15, 1.000000000000000000, -1.665334536937738262E-16 ) ) ;
#174884=AXIS2_PLACEMENT_3D ( 'NONE', #7459, #121313, #185140 ) ;
#174910=CARTESIAN_POINT ( 'NONE',  ( 1.360316468749971808, 1.026041667008142921, 0.7853790794158540534 ) ) ;
#174930=CARTESIAN_POINT ( 'NONE',  ( 1.225000000000001199, -0.1041666666666644925, -0.7072540797572898219 ) ) ;
#174950=CARTESIAN_POINT ( 'NONE',  ( 0.3999999999999889200, 3.949999999999988187, -0.4999999999999987232 ) ) ;
#174961=EDGE_LOOP ( 'NONE', ( #177324, #194620, #194887 ) ) ;
#175014=DIRECTION ( 'NONE',  ( 1.000000000000000000, 0.000000000000000000, 0.000000000000000000 ) ) ;
#175052=ORIENTED_EDGE ( 'NONE', *, *, #159688, .T. ) ;
#175066=DIRECTION ( 'NONE',  ( 0.000000000000000000, 0.000000000000000000, 1.000000000000000000 ) ) ;
#175116=DIRECTION ( 'NONE',  ( -1.276756478318932585E-15, 1.000000000000000000, -1.665334536937738262E-16 ) ) ;
#175127=ORIENTED_EDGE ( 'NONE', *, *, #4291, .T. ) ;
#175130=CARTESIAN_POINT ( 'NONE',  ( 1.224999999999967004, 0.1041666666667366015, 0.7072540797572677285 ) ) ;
#175206=ORIENTED_EDGE ( 'NONE', *, *, #89413, .T. ) ;
#175218=CARTESIAN_POINT ( 'NONE',  ( -0.6801582343750213200, -0.3177083329919394572, 1.178068619123815663 ) ) ;
#175318=CARTESIAN_POINT ( 'NONE',  ( -1.360316468750058849, 2.692708333674814991, 0.7853790794158641564 ) ) ;
#175328=CARTESIAN_POINT ( 'NONE',  ( 1.872228381520318896, 3.299999999999997158, 0.3999999999999958589 ) ) ;
#175424=CARTESIAN_POINT ( 'NONE',  ( -1.772826578343124959, 3.950000000000009059, -0.4500000000000423661 ) ) ;
#175439=CARTESIAN_POINT ( 'NONE',  ( 1.360316468749969809, 1.036458333674743049, -0.7853790794158820310 ) ) ;
#175466=VERTEX_POINT ( 'NONE', #171136 ) ;
#175593=CARTESIAN_POINT ( 'NONE',  ( -0.5000000000000108802, 3.950000000000001954, -0.5000000000000091038 ) ) ;
#175633=DIRECTION ( 'NONE',  ( -3.330669073875479975E-16, 2.334947598634344260E-16, 1.000000000000000000 ) ) ;
#175649=SPHERICAL_SURFACE ( 'NONE', #177617, 0.05000000000000000278 ) ;
#175670=CARTESIAN_POINT ( 'NONE',  ( 1.360316468749987573, 1.817708333674738608, -0.7853790794158981292 ) ) ;
#175680=CARTESIAN_POINT ( 'NONE',  ( 1.224999999999963007, 2.458333334016087335, -0.7072540797572877125 ) ) ;
#175705=CARTESIAN_POINT ( 'NONE',  ( -0.6801582343750125492, 2.182291667008062763, 1.178068619123824323 ) ) ;
#175712=EDGE_LOOP ( 'NONE', ( #136152, #177147, #173419, #56764 ) ) ;
#175728=CIRCLE ( 'NONE', #110071, 0.05000000000000012768 ) ;
#175731=VERTEX_POINT ( 'NONE', #159155 ) ;
#175753=CARTESIAN_POINT ( 'NONE',  ( 1.224999999999998757, 0.9375000006827949317, -8.673617379884035472E-15 ) ) ;
#175842=EDGE_LOOP ( 'NONE', ( #112319, #53980, #97681, #54768 ) ) ;
#175850=ORIENTED_EDGE ( 'NONE', *, *, #100401, .T. ) ;
#175852=B_SPLINE_CURVE_WITH_KNOTS ( 'NONE', 3,
 ( #80284, #161554, #45677, #79218 ),
 .UNSPECIFIED., .F., .F.,
 ( 4, 4 ),
 ( 0.000000000000000000, 2.032232339056924315E-05 ),
 .UNSPECIFIED. ) ;
#175884=CARTESIAN_POINT ( 'NONE',  ( -5.810221930991193690E-16, 2.125000000682803147, 1.224999999999976774 ) ) ;
#175918=CARTESIAN_POINT ( 'NONE',  ( 2.007420792093927986E-08, -6.938893903907228378E-15, -1.225000000000033396 ) ) ;
#175967=CARTESIAN_POINT ( 'NONE',  ( -3.355169270512988773E-14, 1.234375000341463968, 1.570758158831764062 ) ) ;
#175970=EDGE_LOOP ( 'NONE', ( #48232, #75401, #82850, #201444, #175206 ) ) ;
#175988=CARTESIAN_POINT ( 'NONE',  ( 0.6124999999999793943, -0.4166666666666346552, 1.060881119635891157 ) ) ;
#176069=DIRECTION ( 'NONE',  ( -1.276756478318932585E-15, 1.000000000000000000, -1.665334536937738262E-16 ) ) ;
#176177=DIRECTION ( 'NONE',  ( 3.330669073875479482E-16, -3.330669073875479482E-16, -1.000000000000000000 ) ) ;
#176188=EDGE_LOOP ( 'NONE', ( #58649, #12983, #39778, #118078, #124552, #115402 ) ) ;
#176198=VERTEX_POINT ( 'NONE', #94633 ) ;
#176275=CARTESIAN_POINT ( 'NONE',  ( -0.6124999999999984901, 2.770833334016134408, -1.060881119635941339 ) ) ;
#176337=ORIENTED_EDGE ( 'NONE', *, *, #94595, .T. ) ;
#176367=CARTESIAN_POINT ( 'NONE',  ( -0.3000000000000172529, 3.975028841772365595, -0.9637995837462973725 ) ) ;
#176494=CARTESIAN_POINT ( 'NONE',  ( 0.6801582343749744686, 0.4739583336747441034, 1.178068619123803451 ) ) ;
#176571=CARTESIAN_POINT ( 'NONE',  ( 0.6124999999999741762, 0.1458333340161460656, 1.060881119635889380 ) ) ;
#176639=ORIENTED_EDGE ( 'NONE', *, *, #89445, .T. ) ;
#176720=VECTOR ( 'NONE', #50347, 1000.000000000000114 ) ;
#176724=CARTESIAN_POINT ( 'NONE',  ( 1.360316468749957597, 1.276041667008120051, 0.7853790794158580502 ) ) ;
#176756=CARTESIAN_POINT ( 'NONE',  ( -0.3713344243775837383, 2.999999999999995115, 0.3713344243775316689 ) ) ;
#176758=CARTESIAN_POINT ( 'NONE',  ( 1.360316468749947605, 2.536458333674726173, -0.7853790794159141164 ) ) ;
#176765=ORIENTED_EDGE ( 'NONE', *, *, #75861, .F. ) ;
#176883=VECTOR ( 'NONE', #108765, 1000.000000000000114 ) ;
#176902=CARTESIAN_POINT ( 'NONE',  ( 0.6124999999999776179, 0.6666666666666626329, -1.060881119635955327 ) ) ;
#177022=CARTESIAN_POINT ( 'NONE',  ( -1.360316468750028651, -0.8281249996586054207, -3.469446951953614189E-14 ) ) ;
#177081=CARTESIAN_POINT ( 'NONE',  ( -0.3282377607281428689, 2.511164550367429804, -1.225000000000032285 ) ) ;
#177147=ORIENTED_EDGE ( 'NONE', *, *, #43686, .F. ) ;
#177247=VERTEX_POINT ( 'NONE', #24004 ) ;
#177270=( LENGTH_UNIT ( ) NAMED_UNIT ( * ) SI_UNIT ( .MILLI., .METRE. ) );
#177324=ORIENTED_EDGE ( 'NONE', *, *, #91508, .F. ) ;
#177335=CARTESIAN_POINT ( 'NONE',  ( -5.157946788997579689E-14, -0.2968749996585513529, 1.570758158831766060 ) ) ;
#177442=ADVANCED_FACE ( 'NONE', ( #155118 ), #104234, .F. ) ;
#177464=EDGE_CURVE ( 'NONE', #125996, #189127, #67176, .T. ) ;
#177469=ORIENTED_EDGE ( 'NONE', *, *, #204783, .F. ) ;
#177489=CARTESIAN_POINT ( 'NONE',  ( -1.734723475976807094E-15, 2.999999999999988898, -6.938893903907228378E-15 ) ) ;
#177565=CARTESIAN_POINT ( 'NONE',  ( -0.6801582343750334214, 0.1822916670080609869, 1.178068619123799898 ) ) ;
#177587=CARTESIAN_POINT ( 'NONE',  ( -1.360316468749997565, 2.890625000341401574, 1.734723475976807094E-15 ) ) ;
#177588=EDGE_CURVE ( 'NONE', #205644, #146356, #89679, .T. ) ;
#177615=CIRCLE ( 'NONE', #205252, 1.872309607372811158 ) ;
#177617=AXIS2_PLACEMENT_3D ( 'NONE', #108566, #105323, #55482 ) ;
#177624=CIRCLE ( 'NONE', #35816, 0.04999999999999991257 ) ;
#177700=CARTESIAN_POINT ( 'NONE',  ( 0.3282377607281237730, 0.9263354503153991004, -1.225000000000000311 ) ) ;
#177704=LINE ( 'NONE', #29315, #89209 ) ;
#177736=ORIENTED_EDGE ( 'NONE', *, *, #4291, .F. ) ;
#177779=ORIENTED_EDGE ( 'NONE', *, *, #191715, .F. ) ;
#177798=CARTESIAN_POINT ( 'NONE',  ( -0.6801582343750438575, 0.1302083336747333897, -1.178068619123883165 ) ) ;
#177838=CARTESIAN_POINT ( 'NONE',  ( 1.360316468749992236, 2.015625000341400685, -1.040834085586084257E-14 ) ) ;
#178074=CIRCLE ( 'NONE', #22494, 0.04999999999999991257 ) ;
#178084=CARTESIAN_POINT ( 'NONE',  ( -0.4500000000000409228, 3.999999999999974243, 0.8338124244295310739 ) ) ;
#178096=CARTESIAN_POINT ( 'NONE',  ( -0.6801582343750022241, -0.6197916663252672764, -1.178068619123841643 ) ) ;
#178138=CARTESIAN_POINT ( 'NONE',  ( 0.4999999999999709677, 3.949999999999967315, 0.4499999999999590994 ) ) ;
#178161=CARTESIAN_POINT ( 'NONE',  ( 0.3423093779009924731, 3.000000000000002665, -0.3423093779010306092 ) ) ;
#178324=ORIENTED_EDGE ( 'NONE', *, *, #108284, .F. ) ;
#178380=LINE ( 'NONE', #29989, #25378 ) ;
#178407=CARTESIAN_POINT ( 'NONE',  ( -5.508486862036250636E-15, -0.6718749996586012019, -1.570758158831788265 ) ) ;
#178446=CARTESIAN_POINT ( 'NONE',  ( -1.814759087649955749, 3.975067388631681187, 0.4606438099578266665 ) ) ;
#178493=DIRECTION ( 'NONE',  ( 3.497202527569253358E-15, 0.000000000000000000, 1.000000000000000000 ) ) ;
#178505=CARTESIAN_POINT ( 'NONE',  ( -0.6801582343750177673, 1.713541667008065872, 1.178068619123799898 ) ) ;
#178529=EDGE_CURVE ( 'NONE', #191858, #89507, #82545, .T. ) ;
#178554=CARTESIAN_POINT ( 'NONE',  ( 1.896367326442688350, 3.293421909012307580, 0.4056650308922344350 ) ) ;
#178587=DIRECTION ( 'NONE',  ( -3.330669073875479482E-16, 3.330669073875479482E-16, 1.000000000000000000 ) ) ;
#178635=CARTESIAN_POINT ( 'NONE',  ( 0.6801582343749935644, -0.02604166632526327962, 1.178068619123817218 ) ) ;
#178641=PRODUCT_DEFINITION_SHAPE ( 'NONE', 'NONE',  #35864 ) ;
#178657=CARTESIAN_POINT ( 'NONE',  ( -2.954552044183079750E-14, 2.578125000341414452, -1.570758158831808249 ) ) ;
#178710=CARTESIAN_POINT ( 'NONE',  ( -4.415768667553307481E-15, 0.1250000006828069499, 1.224999999999963229 ) ) ;
#178826=CARTESIAN_POINT ( 'NONE',  ( 0.4123176713737303767, 3.999999999999973799, -0.8977835139438099521 ) ) ;
#178872=CARTESIAN_POINT ( 'NONE',  ( 1.360316468749989793, 0.5677083336747246189, -0.7853790794158941324 ) ) ;
#178908=CARTESIAN_POINT ( 'NONE',  ( -5.758872628492442907E-14, 2.203125000341452200, 1.570758158831754070 ) ) ;
#178916=ORIENTED_EDGE ( 'NONE', *, *, #212859, .T. ) ;
#178992=ORIENTED_EDGE ( 'NONE', *, *, #173979, .T. ) ;
#179091=CARTESIAN_POINT ( 'NONE',  ( 0.3914079065635613919, 3.043201908700355229, 0.4248930002254733829 ) ) ;
#179126=VERTEX_POINT ( 'NONE', #71767 ) ;
#179161=CARTESIAN_POINT ( 'NONE',  ( -0.6801582343750091075, -1.036458332991943454, 1.178068619123817218 ) ) ;
#179164=EDGE_LOOP ( 'NONE', ( #80342, #140673, #110079, #87123, #136485, #12529, #59153, #27283, #4374, #17286 ) ) ;
#179209=CYLINDRICAL_SURFACE ( 'NONE', #154246, 0.05000000000000002359 ) ;
#179313=ORIENTED_EDGE ( 'NONE', *, *, #185632, .F. ) ;
#179471=VERTEX_POINT ( 'NONE', #127036 ) ;
#179472=CARTESIAN_POINT ( 'NONE',  ( -1.360316468750024876, -0.5885416663252728275, 0.7853790794158701516 ) ) ;
#179474=CARTESIAN_POINT ( 'NONE',  ( -0.3221776901982874031, -8.373013763170321601E-15, 1.292830470765887307 ) ) ;
#179506=DIRECTION ( 'NONE',  ( -1.000000000000000000, 7.771561172376097755E-16, 4.440892098500627148E-16 ) ) ;
#179518=( BOUNDED_CURVE ( )  B_SPLINE_CURVE ( 2, ( #31109, #80910, #100348, #35335, #84097, #150184, #97181, #214057, #13758 ),
 .UNSPECIFIED., .F., .T. ) 
 B_SPLINE_CURVE_WITH_KNOTS ( ( 3, 2, 2, 2, 3 ),
 ( 0.1406250000000001943, 0.1458333333333333426, 0.1562500000000000000, 0.1666666666666666574, 0.1718749999999998335 ),
 .UNSPECIFIED. ) 
 CURVE ( )  GEOMETRIC_REPRESENTATION_ITEM ( )  RATIONAL_B_SPLINE_CURVE ( ( 0.9330127018922194093, 0.9330127018922218518, 1.000000000000000000, 0.8660254037844387076, 1.000000000000000000, 0.8660254037844387076, 1.000000000000000000, 0.9330127018922215187, 0.9330127018922194093 ) ) 
 REPRESENTATION_ITEM ( '' )  );
#179572=CARTESIAN_POINT ( 'NONE',  ( -1.360316468750036645, 2.151041667008108060, -0.7853790794159302147 ) ) ;
#179592=PLANE ( 'NONE',  #58774 ) ;
#179620=CARTESIAN_POINT ( 'NONE',  ( 0.3585786437626907741, 3.975028841772316301, -0.9637995837462947080 ) ) ;
#179701=CARTESIAN_POINT ( 'NONE',  ( -5.157946788997579689E-14, -0.2968749996585513529, 1.570758158831766060 ) ) ;
#179715=CARTESIAN_POINT ( 'NONE',  ( 0.3914079065635684973, 3.043201908700336578, -0.4248930002255459359 ) ) ;
#179807=ORIENTED_EDGE ( 'NONE', *, *, #191370, .F. ) ;
#179815=CARTESIAN_POINT ( 'NONE',  ( -1.898923903056559004, 3.739065552179622554, 0.3999999999999835909 ) ) ;
#179833=CARTESIAN_POINT ( 'NONE',  ( -1.882262909678046769, 3.299172163371774325, 0.4004916885352270417 ) ) ;
#179925=CARTESIAN_POINT ( 'NONE',  ( 1.360316468750004448, 0.2968750003413955785, -6.938893903907228378E-15 ) ) ;
#179965=CARTESIAN_POINT ( 'NONE',  ( -2.954552044183079750E-14, 2.578125000341414008, -1.570758158831808249 ) ) ;
#179979=ORIENTED_EDGE ( 'NONE', *, *, #28302, .T. ) ;
#180058=ADVANCED_FACE ( 'NONE', ( #200357 ), #8023, .T. ) ;
#180223=CARTESIAN_POINT ( 'NONE',  ( -1.360316468750013108, -0.3281249996585910989, -3.469446951953614189E-14 ) ) ;
#180283=CARTESIAN_POINT ( 'NONE',  ( 7.785697387528199762E-15, 0.5624999999999894529, 1.224999999999973443 ) ) ;
#180361=CARTESIAN_POINT ( 'NONE',  ( -0.3282377607281457554, 2.551335450315352915, 1.224999999999984324 ) ) ;
#180388=CARTESIAN_POINT ( 'NONE',  ( -1.225000000000040057, 0.7708333333333476922, 0.7072540797572656190 ) ) ;
#180391=EDGE_CURVE ( 'NONE', #107567, #116778, #115995, .T. ) ;
#180461=SURFACE_STYLE_USAGE ( .BOTH. , #161016 ) ;
#180622=CARTESIAN_POINT ( 'NONE',  ( -1.360316468750030428, 1.171875000341417117, -4.336808689942017736E-14 ) ) ;
#180643=CARTESIAN_POINT ( 'NONE',  ( -0.3769810270651957618, 3.049942316455299451, -0.4288785890453079008 ) ) ;
#180646=LINE ( 'NONE', #113590, #205718 ) ;
#180673=CARTESIAN_POINT ( 'NONE',  ( 1.911175648939857030, 3.243131119507701943, 0.4542559028653122555 ) ) ;
#180740=CARTESIAN_POINT ( 'NONE',  ( -0.3999999999999979683, 3.322650755865472760, -0.5865692111442778467 ) ) ;
#180751=CARTESIAN_POINT ( 'NONE',  ( -1.360316468750021768, -1.109374999658574446, -3.122502256758252770E-14 ) ) ;
#180771=CARTESIAN_POINT ( 'NONE',  ( 0.6801582343750004478, 2.057291667008069425, -1.178068619123876282 ) ) ;
#180828=( BOUNDED_CURVE ( )  B_SPLINE_CURVE ( 3, ( #110758, #160507, #176756, #211373 ),
 .UNSPECIFIED., .F., .T. ) 
 B_SPLINE_CURVE_WITH_KNOTS ( ( 4, 4 ),
 ( 0.7261627075363390471, 1.570796326794784870 ),
 .UNSPECIFIED. ) 
 CURVE ( )  GEOMETRIC_REPRESENTATION_ITEM ( )  RATIONAL_B_SPLINE_CURVE ( ( 1.000000000000000000, 0.9414278581754953468, 0.9414278581754953468, 1.000000000000000000 ) ) 
 REPRESENTATION_ITEM ( '' )  );
#180862=CARTESIAN_POINT ( 'NONE',  ( -1.907692715643339199, 3.236394383240548400, -0.4609675857477846805 ) ) ;
#180898=LINE ( 'NONE', #164657, #192153 ) ;
#180976=CARTESIAN_POINT ( 'NONE',  ( -1.360316468750056851, 0.6510416670080609869, -0.7853790794158981292 ) ) ;
#181015=CARTESIAN_POINT ( 'NONE',  ( -1.360316468750046859, 0.6197916670081009549, -0.7853790794159322131 ) ) ;
#181044=PLANE ( 'NONE',  #86067 ) ;
#181080=CARTESIAN_POINT ( 'NONE',  ( 0.6124999999999793943, 0.4791666673494773820, -1.060881119635969094 ) ) ;
#181210=EDGE_CURVE ( 'NONE', #55379, #191858, #111002, .T. ) ;
#181270=CARTESIAN_POINT ( 'NONE',  ( -0.6801582343750282034, 2.682291667008049441, 1.178068619123805227 ) ) ;
#181414=ADVANCED_FACE ( 'NONE', ( #80572 ), #81019, .T. ) ;
#181462=ORIENTED_EDGE ( 'NONE', *, *, #108010, .F. ) ;
#181560=VERTEX_POINT ( 'NONE', #196461 ) ;
#181575=CARTESIAN_POINT ( 'NONE',  ( 0.4307572970102366283, 3.041534709929996527, 0.4240169840790947164 ) ) ;
#181606=DIRECTION ( 'NONE',  ( 0.000000000000000000, 0.000000000000000000, 1.000000000000000000 ) ) ;
#181674=CARTESIAN_POINT ( 'NONE',  ( -1.360316468749998675, 1.442708333674736831, 0.7853790794158961308 ) ) ;
#181719=CARTESIAN_POINT ( 'NONE',  ( 0.3282377607281140031, 1.073664549684631986, 1.224999999999960565 ) ) ;
#181736=EDGE_CURVE ( 'NONE', #52005, #76056, #46678, .T. ) ;
#181740=VECTOR ( 'NONE', #7248, 1000.000000000000000 ) ;
#181784=CARTESIAN_POINT ( 'NONE',  ( 1.224999999999961231, 0.9583333340161364067, -0.7072540797573237947 ) ) ;
#181790=CARTESIAN_POINT ( 'NONE',  ( -0.4000000000000118461, 3.372708439410149417, -0.5000000000000247580 ) ) ;
#181802=CARTESIAN_POINT ( 'NONE',  ( 1.360316468749967589, -0.2552083329918390930, 0.7853790794158500566 ) ) ;
#181822=ORIENTED_EDGE ( 'NONE', *, *, #87194, .F. ) ;
#181824=CARTESIAN_POINT ( 'NONE',  ( -1.360316468750056851, 1.369791667008064540, -0.7853790794159101196 ) ) ;
#181840=DIRECTION ( 'NONE',  ( -3.330669073875478496E-16, 1.665334536937734318E-16, 1.000000000000000000 ) ) ;
#181852=CARTESIAN_POINT ( 'NONE',  ( 1.906195883197611129, 3.231669652568789353, -0.4612786727878129822 ) ) ;
#181866=CARTESIAN_POINT ( 'NONE',  ( 0.4499999999999851341, 4.000000000000003553, 0.8338124244295520571 ) ) ;
#181906=ORIENTED_EDGE ( 'NONE', *, *, #178529, .T. ) ;
#181913=CARTESIAN_POINT ( 'NONE',  ( -1.910130646976128110, 3.278792710263301657, -0.4195261609911116740 ) ) ;
#181961=VECTOR ( 'NONE', #188695, 1000.000000000000000 ) ;
#182034=ORIENTED_EDGE ( 'NONE', *, *, #48267, .T. ) ;
#182064=CARTESIAN_POINT ( 'NONE',  ( -5.358255402162534516E-14, 1.328125000341439987, -1.570758158831820239 ) ) ;
#182075=DIRECTION ( 'NONE',  ( 3.330669073875479482E-16, -3.330669073875479482E-16, -1.000000000000000000 ) ) ;
#182087=CARTESIAN_POINT ( 'NONE',  ( -0.6125000000000296874, 0.3541666673494772710, 1.060881119635899816 ) ) ;
#182125=ORIENTED_EDGE ( 'NONE', *, *, #115854, .F. ) ;
#182160=DIRECTION ( 'NONE',  ( 5.828670879282089587E-16, -0.8656921114426507913, 0.5005768354468322912 ) ) ;
#182246=CARTESIAN_POINT ( 'NONE',  ( -0.3000000000000260791, 3.975028841772316301, -0.9637995837462940418 ) ) ;
#182264=CARTESIAN_POINT ( 'NONE',  ( -1.734723475976807094E-15, 2.999999999999988898, -6.938893903907228378E-15 ) ) ;
#182326=CARTESIAN_POINT ( 'NONE',  ( -1.953008978358306879E-14, 1.828125000341410678, -1.570758158831798257 ) ) ;
#182333=PLANE ( 'NONE',  #46967 ) ;
#182420=CIRCLE ( 'NONE', #89071, 0.09999999999999971412 ) ;
#182487=CARTESIAN_POINT ( 'NONE',  ( 0.3999999999999701572, 3.322650755865473648, -0.5865692111442885048 ) ) ;
#182576=CARTESIAN_POINT ( 'NONE',  ( -1.963753466588807894, 3.754052640047090161, -0.4000000000001296963 ) ) ;
#182601=CARTESIAN_POINT ( 'NONE',  ( -2.954552044183079750E-14, 1.062499999999981126, 1.414508159514567431 ) ) ;
#182627=VERTEX_POINT ( 'NONE', #12109 ) ;
#182643=CARTESIAN_POINT ( 'NONE',  ( 0.4516138619287866085, 3.070015318549083272, 0.4124855346667386513 ) ) ;
#182652=CARTESIAN_POINT ( 'NONE',  ( 1.253848497529134409, -2.775557561562891351E-14, 0.5275650105875644424 ) ) ;
#182709=EDGE_CURVE ( 'NONE', #98321, #190021, #147475, .T. ) ;
#182745=ORIENTED_EDGE ( 'NONE', *, *, #22206, .T. ) ;
#182749=CARTESIAN_POINT ( 'NONE',  ( -1.360316468750038865, 1.192708333674735721, 0.7853790794158880262 ) ) ;
#182875=ORIENTED_EDGE ( 'NONE', *, *, #178529, .F. ) ;
#182879=CARTESIAN_POINT ( 'NONE',  ( -5.508486862036250636E-15, -0.6718749996586012019, -1.570758158831788265 ) ) ;
#182902=CARTESIAN_POINT ( 'NONE',  ( -2.353626204688216217E-14, 2.453125000341405570, 1.570758158831792262 ) ) ;
#183007=AXIS2_PLACEMENT_3D ( 'NONE', #36393, #102471, #136051 ) ;
#183059=CARTESIAN_POINT ( 'NONE',  ( 0.2999999999999927169, 3.999999999999974243, -1.007084189318427025 ) ) ;
#183088=CARTESIAN_POINT ( 'NONE',  ( -0.3999999999999854228, -6.938893903907228378E-15, -0.5000000000000368594 ) ) ;
#183097=ORIENTED_EDGE ( 'NONE', *, *, #139883, .T. ) ;
#183104=FILL_AREA_STYLE_COLOUR ( '', #159370 ) ;
#183106=CARTESIAN_POINT ( 'NONE',  ( 1.360316468749971364, -0.7031249996586053097, -3.469446951953614189E-14 ) ) ;
#183117=CARTESIAN_POINT ( 'NONE',  ( -8.673617379884035472E-15, 3.975067388631681187, -1.561251128379126385E-14 ) ) ;
#183143=EDGE_CURVE ( 'NONE', #175731, #34023, #161387, .T. ) ;
#183149=CARTESIAN_POINT ( 'NONE',  ( -1.360316468750023544, 0.8906250003414064587, -2.602085213965210642E-14 ) ) ;
#183158=CARTESIAN_POINT ( 'NONE',  ( -1.743066579297358008E-15, 1.875000000682791379, 1.224999999999958566 ) ) ;
#183213=FACE_OUTER_BOUND ( 'NONE', #192864, .T. ) ;
#183287=DIRECTION ( 'NONE',  ( -1.568190022283037360E-15, 0.8656921114426511243, -0.5005768354468317360 ) ) ;
#183317=( BOUNDED_CURVE ( )  B_SPLINE_CURVE ( 2, ( #173550, #190818, #156222, #25124, #123801, #170308, #189761, #40336, #141066 ),
 .UNSPECIFIED., .F., .T. ) 
 B_SPLINE_CURVE_WITH_KNOTS ( ( 3, 2, 2, 2, 3 ),
 ( 0.5156250000000002220, 0.5208333333333333703, 0.5312500000000000000, 0.5416666666666666297, 0.5468749999999997780 ),
 .UNSPECIFIED. ) 
 CURVE ( )  GEOMETRIC_REPRESENTATION_ITEM ( )  RATIONAL_B_SPLINE_CURVE ( ( 0.9330127018922194093, 0.9330127018922221849, 1.000000000000000000, 0.8660254037844387076, 1.000000000000000000, 0.8660254037844387076, 1.000000000000000000, 0.9330127018922221849, 0.9330127018922194093 ) ) 
 REPRESENTATION_ITEM ( '' )  );
#183322=FACE_OUTER_BOUND ( 'NONE', #96707, .T. ) ;
#183389=EDGE_CURVE ( 'NONE', #203057, #60914, #177624, .T. ) ;
#183442=CARTESIAN_POINT ( 'NONE',  ( 1.224999999999971001, 2.187500000682782275, -4.683753385137379155E-14 ) ) ;
#183452=CARTESIAN_POINT ( 'NONE',  ( -0.5000000000000299760, 3.299999999999955858, -0.5000000000000403011 ) ) ;
#183615=CARTESIAN_POINT ( 'NONE',  ( 1.873515663034551304, 3.299988112486747394, 0.3999999999999681033 ) ) ;
#183654=CARTESIAN_POINT ( 'NONE',  ( 0.6801582343749900117, 2.005208333674748822, 1.178068619123818994 ) ) ;
#183678=CARTESIAN_POINT ( 'NONE',  ( -3.555477883677943599E-14, 0.5624999999999785727, 1.414508159514563435 ) ) ;
#183715=CARTESIAN_POINT ( 'NONE',  ( 0.3999999999999511169, 3.372708439410156522, 0.4999999999999558686 ) ) ;
#183720=CARTESIAN_POINT ( 'NONE',  ( 0.3999999999999681033, 3.372708439410100567, 0.4999999999999501510 ) ) ;
#183782=EDGE_CURVE ( 'NONE', #118779, #130707, #167398, .T. ) ;
#183822=CARTESIAN_POINT ( 'NONE',  ( 0.6801582343749813520, 0.005208333674754095366, 1.178068619123793015 ) ) ;
#183966=CARTESIAN_POINT ( 'NONE',  ( -1.360316468749997565, 2.890625000341401574, 1.734723475976807094E-15 ) ) ;
#183969=CARTESIAN_POINT ( 'NONE',  ( -4.757329562667670667E-14, 1.953125000341451312, 1.570758158831762286 ) ) ;
#183986=FACE_OUTER_BOUND ( 'NONE', #1330, .T. ) ;
#183996=CARTESIAN_POINT ( 'NONE',  ( 1.772826578343118742, 3.950000000000034373, -0.4000000000000274447 ) ) ;
#184037=CARTESIAN_POINT ( 'NONE',  ( -3.755786496842897795E-14, 2.812499999999973355, 1.414508159514537455 ) ) ;
#184071=CARTESIAN_POINT ( 'NONE',  ( -1.896367326442750745, 3.293421909012280047, 0.4056650308922222781 ) ) ;
#184078=B_SPLINE_CURVE_WITH_KNOTS ( 'NONE', 3,
 ( #88598, #19296, #138414, #69100, #20364, #21415, #117945 ),
 .UNSPECIFIED., .F., .F.,
 ( 4, 3, 4 ),
 ( 0.000000000000000000, 2.617081137853276995E-05, 3.552777339496689108E-05 ),
 .UNSPECIFIED. ) ;
#184123=DIRECTION ( 'NONE',  ( -2.126226658603517140E-31, 1.665334536937738015E-16, 1.000000000000000000 ) ) ;
#184127=CARTESIAN_POINT ( 'NONE',  ( 1.224999999999988320, -0.06249999931720595647, -6.938893903907228378E-15 ) ) ;
#184164=CARTESIAN_POINT ( 'NONE',  ( -0.6801582343750265380, -0.2864583329919220822, 1.178068619123820771 ) ) ;
#184202=CARTESIAN_POINT ( 'NONE',  ( 0.6801582343749796866, 1.473958333674751930, 1.178068619123789462 ) ) ;
#184258=VERTEX_POINT ( 'NONE', #115624 ) ;
#184285=ORIENTED_EDGE ( 'NONE', *, *, #6013, .T. ) ;
#184329=VERTEX_POINT ( 'NONE', #162204 ) ;
#184416=CARTESIAN_POINT ( 'NONE',  ( -0.3282377607281419252, 2.051335450315354691, 1.224999999999995870 ) ) ;
#184497=CARTESIAN_POINT ( 'NONE',  ( 1.224999999999996980, 1.687500000682823353, -2.602085213965210642E-14 ) ) ;
#184526=DIRECTION ( 'NONE',  ( 0.000000000000000000, 0.000000000000000000, 1.000000000000000000 ) ) ;
#184565=FACE_OUTER_BOUND ( 'NONE', #112241, .T. ) ;
#184575=( BOUNDED_CURVE ( )  B_SPLINE_CURVE ( 3, ( #201858, #187760, #104399, #154211 ),
 .UNSPECIFIED., .F., .T. ) 
 B_SPLINE_CURVE_WITH_KNOTS ( ( 4, 4 ),
 ( 0.000000000000000000, 1.570796326794816844 ),
 .UNSPECIFIED. ) 
 CURVE ( )  GEOMETRIC_REPRESENTATION_ITEM ( )  RATIONAL_B_SPLINE_CURVE ( ( 1.000000000000000000, 0.8047378541243839223, 0.8047378541243839223, 1.000000000000000000 ) ) 
 REPRESENTATION_ITEM ( '' )  );
#184618=CARTESIAN_POINT ( 'NONE',  ( 0.4516138619287948797, 3.070015318549077943, -0.4124855346668246381 ) ) ;
#184621=CIRCLE ( 'NONE', #163940, 0.04999999999999991257 ) ;
#184631=CARTESIAN_POINT ( 'NONE',  ( -1.225000000000038058, 1.041666667349488984, -0.7072540797573257931 ) ) ;
#184683=ORIENTED_EDGE ( 'NONE', *, *, #91921, .F. ) ;
#184705=CARTESIAN_POINT ( 'NONE',  ( 0.6801582343749900117, 1.588541667008100511, -1.178068619123890270 ) ) ;
#184725=CARTESIAN_POINT ( 'NONE',  ( -1.225000000000060263, 1.270833333333358128, 0.7072540797572717253 ) ) ;
#184840=ADVANCED_FACE ( 'NONE', ( #120991 ), #186958, .F. ) ;
#184872=ORIENTED_EDGE ( 'NONE', *, *, #124535, .F. ) ;
#184878=CARTESIAN_POINT ( 'NONE',  ( 1.360316468750004448, 0.2968750003413955785, -6.938893903907228378E-15 ) ) ;
#184941=ORIENTED_EDGE ( 'NONE', *, *, #199216, .T. ) ;
#185002=TOROIDAL_SURFACE ( 'NONE', #39850, 1.829047314007947955, 0.05000000000000000278 ) ;
#185019=DIRECTION ( 'NONE',  ( 1.276756478318932585E-15, -1.000000000000000000, 1.665334536937738262E-16 ) ) ;
#185023=CARTESIAN_POINT ( 'NONE',  ( -0.6801582343750316451, 2.098958333674738608, -1.178068619123862515 ) ) ;
#185069=DIRECTION ( 'NONE',  ( 1.000000000000000000, 0.000000000000000000, -5.421010862427519212E-16 ) ) ;
#185099=EDGE_CURVE ( 'NONE', #212450, #41218, #61236, .T. ) ;
#185128=CARTESIAN_POINT ( 'NONE',  ( -1.911175648939861693, 3.243131119507702387, 0.4542559028653238573 ) ) ;
#185140=DIRECTION ( 'NONE',  ( 3.330669073875478989E-16, -3.540251991789410786E-16, -1.000000000000000000 ) ) ;
#185169=CYLINDRICAL_SURFACE ( 'NONE', #188475, 1.224999999999996980 ) ;
#185187=CARTESIAN_POINT ( 'NONE',  ( 0.6124999999999967137, -0.5208333326505234506, -1.060881119635972647 ) ) ;
#185222=CARTESIAN_POINT ( 'NONE',  ( -1.360316468750066843, -0.09895833299191045263, -0.7853790794159082322 ) ) ;
#185266=CARTESIAN_POINT ( 'NONE',  ( -3.355169270512988773E-14, 0.9531250003414385441, 1.570758158831740081 ) ) ;
#185333=CARTESIAN_POINT ( 'NONE',  ( 0.3282377607281135035, 0.4888354509981784335, -1.225000000000015410 ) ) ;
#185460=CARTESIAN_POINT ( 'NONE',  ( -0.3282377607281410370, 0.6138354509981421847, 1.224999999999986766 ) ) ;
#185543=ORIENTED_EDGE ( 'NONE', *, *, #83130, .F. ) ;
#185565=CARTESIAN_POINT ( 'NONE',  ( 0.6124999999999932720, 2.229166667349451014, -1.060881119635948444 ) ) ;
#185632=EDGE_CURVE ( 'NONE', #126635, #88486, #171254, .T. ) ;
#185640=CARTESIAN_POINT ( 'NONE',  ( 1.946531837068834925, 3.754233237397152312, 0.4615996190889071760 ) ) ;
#185735=ORIENTED_EDGE ( 'NONE', *, *, #103939, .T. ) ;
#185771=CARTESIAN_POINT ( 'NONE',  ( -4.957638175832625493E-14, 1.734375000341442208, 1.570758158831756068 ) ) ;
#185793=CARTESIAN_POINT ( 'NONE',  ( 0.6124999999999707345, 0.4166666666666901664, -1.060881119635969094 ) ) ;
#185807=DIRECTION ( 'NONE',  ( -1.000000000000000000, 7.771561172376097755E-16, 4.440892098500627148E-16 ) ) ;
#185879=AXIS2_PLACEMENT_3D ( 'NONE', #175424, #27009, #93116 ) ;
#186098=CARTESIAN_POINT ( 'NONE',  ( 1.360316468749963592, 0.03645833367470611985, -0.7853790794159122290 ) ) ;
#186100=FACE_OUTER_BOUND ( 'NONE', #69040, .T. ) ;
#186200=CARTESIAN_POINT ( 'NONE',  ( -1.907713928855389263, 3.283019769909803820, 0.4154771360143557635 ) ) ;
#186241=DIRECTION ( 'NONE',  ( -0.2460297208025352678, 6.661338147750954034E-16, 0.9692622846690294169 ) ) ;
#186259=CARTESIAN_POINT ( 'NONE',  ( -0.6125000000000331291, -0.6458333326505374394, 1.060881119635882497 ) ) ;
#186275=LINE ( 'NONE', #98655, #124015 ) ;
#186324=ORIENTED_EDGE ( 'NONE', *, *, #211148, .F. ) ;
#186329=CARTESIAN_POINT ( 'NONE',  ( 0.6801582343749865700, 1.307291667008089853, -1.178068619123883165 ) ) ;
#186360=CARTESIAN_POINT ( 'NONE',  ( 1.907713928855353069, 3.283019769909847785, -0.4154771360144025039 ) ) ;
#186399=CARTESIAN_POINT ( 'NONE',  ( 0.6124999999999862776, 0.3958333340161462877, 1.060881119635934455 ) ) ;
#186469=ORIENTED_EDGE ( 'NONE', *, *, #84254, .F. ) ;
#186640=CARTESIAN_POINT ( 'NONE',  ( -4.356712336337761644E-14, 2.250000000682782719, -1.414508159514601626 ) ) ;
#186729=CIRCLE ( 'NONE', #58724, 0.05000000000000007910 ) ;
#186848=CARTESIAN_POINT ( 'NONE',  ( 0.6801582343749900117, 1.338541667008072533, -1.178068619123872729 ) ) ;
#186870=CARTESIAN_POINT ( 'NONE',  ( 0.6124999999999776179, 0.6666666666666626329, -1.060881119635955327 ) ) ;
#186958=PLANE ( 'NONE',  #84367 ) ;
#187001=ORIENTED_EDGE ( 'NONE', *, *, #171547, .T. ) ;
#187095=DIRECTION ( 'NONE',  ( 1.276756478318932585E-15, -1.000000000000000000, 1.665334536937738262E-16 ) ) ;
#187169=CARTESIAN_POINT ( 'NONE',  ( -0.6801582343750299797, 0.9322916670080338974, 1.178068619123803451 ) ) ;
#187243=CARTESIAN_POINT ( 'NONE',  ( -0.6125000000000089262, 1.791666666666677621, 1.060881119635936232 ) ) ;
#187251=EDGE_CURVE ( 'NONE', #55298, #23033, #195244, .T. ) ;
#187262=B_SPLINE_CURVE_WITH_KNOTS ( 'NONE', 3,
 ( #166410, #52662, #118790, #1750, #72086, #182652 ),
 .UNSPECIFIED., .F., .F.,
 ( 4, 2, 4 ),
 ( 0.000000000000000000, 0.0005369603738926351233, 0.001073920747785270247 ),
 .UNSPECIFIED. ) ;
#187270=ORIENTED_EDGE ( 'NONE', *, *, #88956, .F. ) ;
#187334=CARTESIAN_POINT ( 'NONE',  ( -1.225000000000038058, -0.6666666659838712539, 0.7072540797572637317 ) ) ;
#187394=ORIENTED_EDGE ( 'NONE', *, *, #198353, .T. ) ;
#187398=CARTESIAN_POINT ( 'NONE',  ( 0.6801582343750004478, 2.057291667008069425, -1.178068619123876282 ) ) ;
#187407=CARTESIAN_POINT ( 'NONE',  ( -1.360316468750006669, 0.1614583336747227316, 0.7853790794158981292 ) ) ;
#187475=CARTESIAN_POINT ( 'NONE',  ( 0.3585786437626807821, 3.975028841772350052, 0.9637995837462361992 ) ) ;
#187627=CARTESIAN_POINT ( 'NONE',  ( 1.360316468749955598, 1.526041667008097180, 0.7853790794158861388 ) ) ;
#187705=CARTESIAN_POINT ( 'NONE',  ( -0.6125000000000123679, 1.770833334016133520, -1.060881119635941339 ) ) ;
#187759=EDGE_CURVE ( 'NONE', #44750, #12260, #204744, .T. ) ;
#187760=CARTESIAN_POINT ( 'NONE',  ( 0.3878679656440350287, 3.999999999999961808, -1.007084189318423473 ) ) ;
#187785=ORIENTED_EDGE ( 'NONE', *, *, #72377, .T. ) ;
#187849=DIRECTION ( 'NONE',  ( 3.330669073875478989E-16, -3.540251991789410786E-16, -1.000000000000000000 ) ) ;
#187870=CIRCLE ( 'NONE', #94539, 1.829047314007942848 ) ;
#187912=CARTESIAN_POINT ( 'NONE',  ( 1.360316468749975582, 2.317708333674725285, -0.7853790794158961308 ) ) ;
#187934=CARTESIAN_POINT ( 'NONE',  ( -1.225000000000005640, -1.000000000000000888, -1.908195823574487804E-14 ) ) ;
#188015=EDGE_CURVE ( 'NONE', #179471, #64456, #178074, .T. ) ;
#188019=LINE ( 'NONE', #38586, #155167 ) ;
#188068=ADVANCED_FACE ( 'NONE', ( #210998 ), #185002, .T. ) ;
#188070=EDGE_LOOP ( 'NONE', ( #31850, #2144, #204296, #142841, #154599, #178916, #200538 ) ) ;
#188087=CARTESIAN_POINT ( 'NONE',  ( -1.360316468750056851, 0.6510416670080610979, -0.7853790794158981292 ) ) ;
#188091=ORIENTED_EDGE ( 'NONE', *, *, #89116, .T. ) ;
#188233=CARTESIAN_POINT ( 'NONE',  ( -1.360316468750006669, 1.119791667008071201, -0.7853790794158921340 ) ) ;
#188304=CARTESIAN_POINT ( 'NONE',  ( 1.224999999999986988, 1.645833333333327930, -0.7072540797572998139 ) ) ;
#188350=CARTESIAN_POINT ( 'NONE',  ( 1.873515663034563961, 3.299988112486734071, -0.3999999999999993006 ) ) ;
#188374=CARTESIAN_POINT ( 'NONE',  ( 0.4170821662628897974, 3.033599471985628959, -0.4170821662629418114 ) ) ;
#188415=CARTESIAN_POINT ( 'NONE',  ( 0.4999999999999900080, 3.949999999999995293, -0.4000000000000339950 ) ) ;
#188468=CARTESIAN_POINT ( 'NONE',  ( 0.6801582343749970061, 2.223958333674731946, 1.178068619123799898 ) ) ;
#188475=AXIS2_PLACEMENT_3D ( 'NONE', #84486, #34667, #120266 ) ;
#188479=CARTESIAN_POINT ( 'NONE',  ( -1.360316468750007779, 0.1406250003413919702, -1.734723475976807094E-15 ) ) ;
#188508=EDGE_CURVE ( 'NONE', #130707, #23166, #180646, .T. ) ;
#188524=CARTESIAN_POINT ( 'NONE',  ( -1.874158809982179319, 3.299964346911585356, 0.3999999999999993006 ) ) ;
#188544=CARTESIAN_POINT ( 'NONE',  ( 0.3999999999999901412, 3.964661556059753789, 0.9099571394228996857 ) ) ;
#188624=AXIS2_PLACEMENT_3D ( 'NONE', #23683, #61523, #89794 ) ;
#188643=LINE ( 'NONE', #20785, #19312 ) ;
#188695=DIRECTION ( 'NONE',  ( 1.276756478318932585E-15, -1.000000000000000000, 1.665334536937738262E-16 ) ) ;
#188702=CARTESIAN_POINT ( 'NONE',  ( -3.555477883677943599E-14, 2.484375000341469963, 1.570758158831768281 ) ) ;
#188713=CARTESIAN_POINT ( 'NONE',  ( 0.3282377607281151133, 2.386164550367423587, 1.224999999999977440 ) ) ;
#188754=DIRECTION ( 'NONE',  ( 0.000000000000000000, -0.5005768354468324022, 0.8656921114426507913 ) ) ;
#188779=CARTESIAN_POINT ( 'NONE',  ( 0.6124999999999914957, 0.2291666673494702211, -1.060881119635965764 ) ) ;
#188856=CARTESIAN_POINT ( 'NONE',  ( -0.3000000000000344058, 3.322650755865458994, 0.5865692111442272205 ) ) ;
#188942=CARTESIAN_POINT ( 'NONE',  ( -1.224999999999995204, 3.000000000000002665, -1.387778780781445676E-14 ) ) ;
#188987=CARTESIAN_POINT ( 'NONE',  ( -1.360316468749995789, 0.9218750003414100114, -6.938893903907228378E-15 ) ) ;
#189012=CARTESIAN_POINT ( 'NONE',  ( -0.6125000000000226930, -0.04166666666667595553, -1.060881119635941339 ) ) ;
#189050=EDGE_LOOP ( 'NONE', ( #194379, #59375, #84186, #92222 ) ) ;
#189127=VERTEX_POINT ( 'NONE', #85534 ) ;
#189159=CARTESIAN_POINT ( 'NONE',  ( -1.992711204631002198E-15, 2.999999999999989342, 1.224999999999989875 ) ) ;
#189216=CIRCLE ( 'NONE', #75118, 0.04999999999999991257 ) ;
#189295=ORIENTED_EDGE ( 'NONE', *, *, #25609, .F. ) ;
#189310=CARTESIAN_POINT ( 'NONE',  ( -3.755786496842897795E-14, 1.078125000341431106, -1.570758158831814466 ) ) ;
#189380=CARTESIAN_POINT ( 'NONE',  ( 0.6125000000000019318, 1.833333333333346582, 1.060881119635934455 ) ) ;
#189416=CARTESIAN_POINT ( 'NONE',  ( -0.6801582343750351978, 2.630208333674721732, -1.178068619123886718 ) ) ;
#189519=CARTESIAN_POINT ( 'NONE',  ( -1.926045559592023171, 3.520657594588521455, -0.4000000000000374922 ) ) ;
#189522=AXIS2_PLACEMENT_3D ( 'NONE', #8788, #26100, #10905 ) ;
#189535=CARTESIAN_POINT ( 'NONE',  ( -1.360316468750056851, 2.119791667008092517, -0.7853790794159082322 ) ) ;
#189543=CARTESIAN_POINT ( 'NONE',  ( -1.162044386198238738E-15, 2.937500000000009326, -1.225000000000010303 ) ) ;
#189671=( BOUNDED_CURVE ( )  B_SPLINE_CURVE ( 3, ( #89870, #173251, #138610, #60534 ),
 .UNSPECIFIED., .F., .T. ) 
 B_SPLINE_CURVE_WITH_KNOTS ( ( 4, 4 ),
 ( 0.6625062783163327973, 1.570796326794872799 ),
 .UNSPECIFIED. ) 
 CURVE ( )  GEOMETRIC_REPRESENTATION_ITEM ( )  RATIONAL_B_SPLINE_CURVE ( ( 1.000000000000000000, 0.9324242863012305316, 0.9324242863012305316, 1.000000000000000000 ) ) 
 REPRESENTATION_ITEM ( '' )  );
#189740=CARTESIAN_POINT ( 'NONE',  ( 1.224999999999965006, 0.3541666666667217522, 0.7072540797572456350 ) ) ;
#189761=CARTESIAN_POINT ( 'NONE',  ( 0.6124999999999828360, 0.6458333340161465097, 1.060881119635891157 ) ) ;
#189763=CARTESIAN_POINT ( 'NONE',  ( -0.6801582343750351978, 2.630208333674721732, -1.178068619123886718 ) ) ;
#189845=CARTESIAN_POINT ( 'NONE',  ( -1.225000000000044276, 0.7916666673494796580, -0.7072540797572998139 ) ) ;
#189932=CARTESIAN_POINT ( 'NONE',  ( -1.394453263437886604E-15, 2.375000000682794266, 1.224999999999975220 ) ) ;
#190004=CARTESIAN_POINT ( 'NONE',  ( -0.3282377607281330989, 2.301335450315363129, 1.224999999999980771 ) ) ;
#190021=VERTEX_POINT ( 'NONE', #180643 ) ;
#190055=CARTESIAN_POINT ( 'NONE',  ( 1.360316468749957597, 0.7760416670081098367, 0.7853790794158520550 ) ) ;
#190077=CARTESIAN_POINT ( 'NONE',  ( 1.224999999999957012, -0.8958333333332680892, 0.7072540797572596238 ) ) ;
#190260=ORIENTED_EDGE ( 'NONE', *, *, #191685, .T. ) ;
#190278=CARTESIAN_POINT ( 'NONE',  ( -1.326716514427061987E-15, 2.999999999999988454, -1.225000000000003864 ) ) ;
#190322=EDGE_LOOP ( 'NONE', ( #182034, #54098, #108342, #210878, #16389, #192070 ) ) ;
#190348=CARTESIAN_POINT ( 'NONE',  ( -1.980939963429228401, 3.482546949474376596, -0.4617747962884479751 ) ) ;
#190362=CARTESIAN_POINT ( 'NONE',  ( 1.360316468749953600, 0.4947916670081083934, 0.7853790794158861388 ) ) ;
#190433=CARTESIAN_POINT ( 'NONE',  ( 1.224999999999955014, 2.145833333333346360, -0.7072540797573136917 ) ) ;
#190446=CARTESIAN_POINT ( 'NONE',  ( 0.4809368265653416463, 3.139971263792683764, 0.3999999999999678257 ) ) ;
#190468=CARTESIAN_POINT ( 'NONE',  ( 0.6801582343749987825, 2.338541667008108060, -1.178068619123883165 ) ) ;
#190476=CARTESIAN_POINT ( 'NONE',  ( -0.4000000000000109024, 3.251480759208445814, -0.4649507210925222789 ) ) ;
#190484=EDGE_CURVE ( 'NONE', #4353, #168515, #103570, .T. ) ;
#190494=CARTESIAN_POINT ( 'NONE',  ( -1.225000000000060263, 1.270833333333357906, 0.7072540797572717253 ) ) ;
#190570=ORIENTED_EDGE ( 'NONE', *, *, #77841, .T. ) ;
#190590=CARTESIAN_POINT ( 'NONE',  ( -1.953008978358306879E-14, 0.7031250003414774019, 1.570758158831782270 ) ) ;
#190598=CARTESIAN_POINT ( 'NONE',  ( -1.752700365193352683E-14, 0.07812500034142640104, -1.570758158831804474 ) ) ;
#190723=DIRECTION ( 'NONE',  ( 1.000000000000000000, 0.000000000000000000, 0.000000000000000000 ) ) ;
#190730=ORIENTED_EDGE ( 'NONE', *, *, #187759, .F. ) ;
#190818=CARTESIAN_POINT ( 'NONE',  ( 0.3282377607281143916, 0.7388354509981899243, -1.225000000000014300 ) ) ;
#190820=CARTESIAN_POINT ( 'NONE',  ( 0.6801582343749883464, 1.505208333674713739, 1.178068619123805227 ) ) ;
#190859=FACE_OUTER_BOUND ( 'NONE', #156018, .T. ) ;
#190901=CARTESIAN_POINT ( 'NONE',  ( 1.224999999999935030, 0.7083333340161593883, -0.7072540797573136917 ) ) ;
#190972=CARTESIAN_POINT ( 'NONE',  ( -0.4516138619288456169, 3.070015318549070393, 0.4124855346667622435 ) ) ;
#191005=CARTESIAN_POINT ( 'NONE',  ( 0.4499999999999800826, 4.000000000000008882, 0.8338124244295482823 ) ) ;
#191033=CARTESIAN_POINT ( 'NONE',  ( -1.772826578343097204, 3.950000000000001954, 0.3999999999999941380 ) ) ;
#191112=CARTESIAN_POINT ( 'NONE',  ( -1.360316468750038643, 0.4427083336747321130, 0.7853790794158701516 ) ) ;
#191133=CARTESIAN_POINT ( 'NONE',  ( -1.225000000000048050, -0.2291666666666410390, 0.7072540797572577365 ) ) ;
#191370=EDGE_CURVE ( 'NONE', #74569, #196234, #199043, .T. ) ;
#191426=CARTESIAN_POINT ( 'NONE',  ( -0.6801582343750074422, -0.8177083329919260235, 1.178068619123834759 ) ) ;
#191456=EDGE_CURVE ( 'NONE', #146356, #4353, #105887, .T. ) ;
#191597=ORIENTED_EDGE ( 'NONE', *, *, #153901, .T. ) ;
#191634=CARTESIAN_POINT ( 'NONE',  ( -1.889141968554442386, 3.755428628636585220, -0.4000000000000271116 ) ) ;
#191639=CARTESIAN_POINT ( 'NONE',  ( 0.3999999999999883649, 3.251480759208426274, -0.4649507210925284961 ) ) ;
#191650=CARTESIAN_POINT ( 'NONE',  ( -1.360316468750007779, 0.1406250003413919702, -1.734723475976807094E-15 ) ) ;
#191685=EDGE_CURVE ( 'NONE', #209652, #99096, #109116, .T. ) ;
#191702=VECTOR ( 'NONE', #108355, 1000.000000000000000 ) ;
#191715=EDGE_CURVE ( 'NONE', #125736, #149597, #206033, .T. ) ;
#191805=FACE_OUTER_BOUND ( 'NONE', #197390, .T. ) ;
#191858=VERTEX_POINT ( 'NONE', #28862 ) ;
#191885=CARTESIAN_POINT ( 'NONE',  ( -1.360316468749998675, 1.442708333674736831, 0.7853790794158961308 ) ) ;
#191960=CARTESIAN_POINT ( 'NONE',  ( -1.225000000000028066, 0.3125000006828221322, -4.336808689942017736E-14 ) ) ;
#192043=VERTEX_POINT ( 'NONE', #37161 ) ;
#192046=DIRECTION ( 'NONE',  ( 1.000000000000000000, 0.000000000000000000, -4.336808689942017736E-15 ) ) ;
#192070=ORIENTED_EDGE ( 'NONE', *, *, #182709, .F. ) ;
#192083=CYLINDRICAL_SURFACE ( 'NONE', #196641, 1.224999999999996980 ) ;
#192091=CARTESIAN_POINT ( 'NONE',  ( 1.224999999999955014, 1.895833333333313053, -0.7072540797573217963 ) ) ;
#192096=EDGE_CURVE ( 'NONE', #122076, #204354, #102287, .T. ) ;
#192153=VECTOR ( 'NONE', #68186, 1000.000000000000000 ) ;
#192179=CARTESIAN_POINT ( 'NONE',  ( -0.6801582343750316451, 0.8802083336747270614, -1.178068619123876282 ) ) ;
#192200=CARTESIAN_POINT ( 'NONE',  ( 1.360316468749961816, 2.817708333674743493, -0.7853790794159141164 ) ) ;
#192232=ORIENTED_EDGE ( 'NONE', *, *, #108284, .T. ) ;
#192296=VECTOR ( 'NONE', #92930, 1000.000000000000000 ) ;
#192406=CARTESIAN_POINT ( 'NONE',  ( 0.6124999999999914957, 2.583333333333347248, 1.060881119635894487 ) ) ;
#192493=CARTESIAN_POINT ( 'NONE',  ( -1.360316468750034868, -0.3385416663252556191, 0.7853790794158601596 ) ) ;
#192495=CARTESIAN_POINT ( 'NONE',  ( -1.192422653747474470, -9.167912422188539046E-15, 0.4243420385968842967 ) ) ;
#192557=ADVANCED_FACE ( 'NONE', ( #202839 ), #182333, .F. ) ;
#192602=DIRECTION ( 'NONE',  ( 1.000000000000000000, -7.771561172376097755E-16, -4.440892098500627148E-16 ) ) ;
#192718=CARTESIAN_POINT ( 'NONE',  ( -1.360316468750030650, 0.8697916670080861890, -0.7853790794159041244 ) ) ;
#192763=ORIENTED_EDGE ( 'NONE', *, *, #87277, .T. ) ;
#192765=ORIENTED_EDGE ( 'NONE', *, *, #81270, .T. ) ;
#192774=VECTOR ( 'NONE', #139703, 1000.000000000000000 ) ;
#192822=CYLINDRICAL_SURFACE ( 'NONE', #72311, 0.05000000000000002359 ) ;
#192849=EDGE_LOOP ( 'NONE', ( #138102, #20133, #83994 ) ) ;
#192857=DIRECTION ( 'NONE',  ( 1.276756478318932585E-15, -1.000000000000000000, 1.665334536937738262E-16 ) ) ;
#192864=EDGE_LOOP ( 'NONE', ( #37981, #51956, #193891, #131350 ) ) ;
#192868=CARTESIAN_POINT ( 'NONE',  ( -0.3000000000000068723, 0.6284510210557009424, 1.086836331270357281 ) ) ;
#192874=CARTESIAN_POINT ( 'NONE',  ( -1.734723475976807094E-15, 2.999999999999988898, -6.938893903907228378E-15 ) ) ;
#192911=AXIS2_PLACEMENT_3D ( 'NONE', #151488, #185019, #203393 ) ;
#192933=EDGE_CURVE ( 'NONE', #62112, #192043, #169971, .T. ) ;
#192934=CARTESIAN_POINT ( 'NONE',  ( -0.4500000000000059508, 3.950000000000009059, -0.8338124244295693765 ) ) ;
#192936=ORIENTED_EDGE ( 'NONE', *, *, #87194, .T. ) ;
#192956=CARTESIAN_POINT ( 'NONE',  ( -3.755786496842897795E-14, 1.109375000341423112, -1.570758158831814466 ) ) ;
#193167=DIRECTION ( 'NONE',  ( -1.000000000000000000, 7.771561172376097755E-16, 4.440892098500627148E-16 ) ) ;
#193187=VECTOR ( 'NONE', #35368, 1000.000000000000000 ) ;
#193218=AXIS2_PLACEMENT_3D ( 'NONE', #123, #103809, #99799 ) ;
#193262=CARTESIAN_POINT ( 'NONE',  ( 1.360316468749971364, 0.04687500034143698979, -3.469446951953614189E-14 ) ) ;
#193364=CARTESIAN_POINT ( 'NONE',  ( -0.5000000000000213163, 3.299999999999983391, -0.4000000000000444311 ) ) ;
#193372=CARTESIAN_POINT ( 'NONE',  ( 1.772826578343088544, 3.950000000000001954, -0.4500000000000284883 ) ) ;
#193411=( BOUNDED_CURVE ( )  B_SPLINE_CURVE ( 3, ( #37400, #149024, #119787, #87223 ),
 .UNSPECIFIED., .F., .T. ) 
 B_SPLINE_CURVE_WITH_KNOTS ( ( 4, 4 ),
 ( 4.712388980384718984, 5.718907872238413681 ),
 .UNSPECIFIED. ) 
 CURVE ( )  GEOMETRIC_REPRESENTATION_ITEM ( )  RATIONAL_B_SPLINE_CURVE ( ( 1.000000000000000000, 0.9173434942194829134, 0.9173434942194829134, 1.000000000000000000 ) ) 
 REPRESENTATION_ITEM ( '' )  );
#193501=ORIENTED_EDGE ( 'NONE', *, *, #130401, .T. ) ;
#193529=CARTESIAN_POINT ( 'NONE',  ( -0.4000000000000447087, 3.964661556059721814, 0.9099571394228918031 ) ) ;
#193574=CARTESIAN_POINT ( 'NONE',  ( 4.506943796211477291E-15, 2.625000000682800483, 1.414508159514579644 ) ) ;
#193647=DIRECTION ( 'NONE',  ( -1.000000000000000000, 7.771561172376097755E-16, 4.440892098500627148E-16 ) ) ;
#193649=CARTESIAN_POINT ( 'NONE',  ( 0.4465194593917843902, 3.080450244942134486, 0.4155024747329351120 ) ) ;
#193671=CARTESIAN_POINT ( 'NONE',  ( -3.555477883677943599E-14, 2.484375000341469963, 1.570758158831768281 ) ) ;
#193729=CARTESIAN_POINT ( 'NONE',  ( -6.158835246850665095E-15, 0.8125000000000031086, 1.224999999999960565 ) ) ;
#193739=ORIENTED_EDGE ( 'NONE', *, *, #144993, .F. ) ;
#193793=CARTESIAN_POINT ( 'NONE',  ( -0.6801582343750299797, 1.182291667008061875, 1.178068619123820771 ) ) ;
#193800=DIRECTION ( 'NONE',  ( -3.330669073875478989E-16, 3.330669073875478989E-16, 1.000000000000000000 ) ) ;
#193814=CARTESIAN_POINT ( 'NONE',  ( 0.6801582343749987825, 2.723958333674732391, 1.178068619123836314 ) ) ;
#193829=ORIENTED_EDGE ( 'NONE', *, *, #61547, .T. ) ;
#193891=ORIENTED_EDGE ( 'NONE', *, *, #51475, .F. ) ;
#193899=FACE_OUTER_BOUND ( 'NONE', #109610, .T. ) ;
#193911=CARTESIAN_POINT ( 'NONE',  ( -0.4465194593918104249, 3.080450244942120719, -0.4155024747329819634 ) ) ;
#193916=CARTESIAN_POINT ( 'NONE',  ( -1.997523430356386465, 3.481192892629605407, 0.4000000000002922329 ) ) ;
#194004=DIRECTION ( 'NONE',  ( 4.107825191113088666E-15, 4.274358644806862147E-15, 1.000000000000000000 ) ) ;
#194008=ORIENTED_EDGE ( 'NONE', *, *, #35341, .F. ) ;
#194026=CARTESIAN_POINT ( 'NONE',  ( 0.6801582343750056658, 0.5885416670080856338, -1.178068619123862515 ) ) ;
#194063=CARTESIAN_POINT ( 'NONE',  ( 1.360316468749985797, 2.036458333674739940, -0.7853790794159022370 ) ) ;
#194227=VERTEX_POINT ( 'NONE', #188524 ) ;
#194301=CARTESIAN_POINT ( 'NONE',  ( -1.734723475976807094E-14, 4.000000000000003553, -1.734723475976807094E-14 ) ) ;
#194331=CARTESIAN_POINT ( 'NONE',  ( -0.6801582343750091075, 2.848958333674732391, -1.178068619123848526 ) ) ;
#194379=ORIENTED_EDGE ( 'NONE', *, *, #198353, .F. ) ;
#194389=CARTESIAN_POINT ( 'NONE',  ( -1.225000000000024736, 2.562500000682817358, -1.908195823574487804E-14 ) ) ;
#194570=( LENGTH_UNIT ( ) NAMED_UNIT ( * ) SI_UNIT ( .MILLI., .METRE. ) );
#194580=CARTESIAN_POINT ( 'NONE',  ( -0.6801582343750420812, 2.713541667008087632, 1.178068619123787908 ) ) ;
#194589=AXIS2_PLACEMENT_3D ( 'NONE', #63696, #50642, #47471 ) ;
#194620=ORIENTED_EDGE ( 'NONE', *, *, #68527, .T. ) ;
#194637=CARTESIAN_POINT ( 'NONE',  ( 0.6801582343749952297, -0.1927083329918907739, -1.178068619123876282 ) ) ;
#194738=CARTESIAN_POINT ( 'NONE',  ( -1.752700365193352683E-14, 1.609375000341425554, -1.570758158831794260 ) ) ;
#194762=DIRECTION ( 'NONE',  ( -1.276756478318932585E-15, 1.000000000000000000, -1.665334536937738262E-16 ) ) ;
#194818=DIRECTION ( 'NONE',  ( 1.000000000000000000, 0.000000000000000000, 0.000000000000000000 ) ) ;
#194858=CARTESIAN_POINT ( 'NONE',  ( -0.3000000002818342670, 3.198312376128883194, -0.5146719259196198548 ) ) ;
#194868=CARTESIAN_POINT ( 'NONE',  ( -1.360316468750006669, 1.119791667008071201, -0.7853790794158921340 ) ) ;
#194887=ORIENTED_EDGE ( 'NONE', *, *, #206691, .F. ) ;
#194889=CARTESIAN_POINT ( 'NONE',  ( 1.360316468749973584, 2.786458333674735499, -0.7853790794159101196 ) ) ;
#194900=CARTESIAN_POINT ( 'NONE',  ( 1.893304937267609622, 3.295344712542843446, -0.4038802767148514383 ) ) ;
#194947=ORIENTED_EDGE ( 'NONE', *, *, #22206, .F. ) ;
#195016=VERTEX_POINT ( 'NONE', #103424 ) ;
#195107=CARTESIAN_POINT ( 'NONE',  ( -4.957638175832625493E-14, 0.8593750003414141192, -1.570758158831808249 ) ) ;
#195132=ORIENTED_EDGE ( 'NONE', *, *, #31157, .T. ) ;
#195142=EDGE_CURVE ( 'NONE', #213643, #154544, #76259, .T. ) ;
#195149=CARTESIAN_POINT ( 'NONE',  ( -3.505400730386704341E-15, 2.703125000341406903, 1.570758158831794260 ) ) ;
#195155=CARTESIAN_POINT ( 'NONE',  ( -1.326716514427061987E-15, 2.999999999999988454, -1.225000000000003864 ) ) ;
#195244=CIRCLE ( 'NONE', #25760, 0.04999999999999991257 ) ;
#195411=CARTESIAN_POINT ( 'NONE',  ( -1.360316468750028651, -1.078124999658591765, -4.510281037539698445E-14 ) ) ;
#195414=VERTEX_POINT ( 'NONE', #211576 ) ;
#195432=CIRCLE ( 'NONE', #57038, 1.224999999999996980 ) ;
#195541=CARTESIAN_POINT ( 'NONE',  ( 0.6311622855796235054, 3.299999999999983391, 0.3999999999999663824 ) ) ;
#195620=CARTESIAN_POINT ( 'NONE',  ( 1.224999999999996980, 1.687500000682823353, -2.602085213965210642E-14 ) ) ;
#195663=CARTESIAN_POINT ( 'NONE',  ( -2.954552044183079750E-14, 2.734375000341430884, 1.570758158831788265 ) ) ;
#195717=CARTESIAN_POINT ( 'NONE',  ( -0.6125000000000262457, 2.604166667349451458, 1.060881119635917136 ) ) ;
#195719=DIRECTION ( 'NONE',  ( -0.5005768354468334014, 0.8656921114426502362, 1.887379141862767696E-15 ) ) ;
#195754=CARTESIAN_POINT ( 'NONE',  ( -0.3000000000000172529, 3.975028841772365595, -0.9637995837462973725 ) ) ;
#195789=EDGE_CURVE ( 'NONE', #108115, #12260, #161369, .T. ) ;
#195815=CARTESIAN_POINT ( 'NONE',  ( -0.6801582343750022241, 1.130208333674734167, -1.178068619123841643 ) ) ;
#195879=DIRECTION ( 'NONE',  ( 1.000000000000000000, -7.771561172376097755E-16, -4.440892098500627148E-16 ) ) ;
#195942=CARTESIAN_POINT ( 'NONE',  ( 0.000000000000000000, 0.000000000000000000, 0.000000000000000000 ) ) ;
#195947=CARTESIAN_POINT ( 'NONE',  ( -1.360316468750006225, -0.3593749996585737794, -1.734723475976807094E-15 ) ) ;
#195962=CYLINDRICAL_SURFACE ( 'NONE', #82628, 1.224999999999996980 ) ;
#196070=CARTESIAN_POINT ( 'NONE',  ( -1.947641667917469510, 3.752373307046521944, 0.4616076617487344658 ) ) ;
#196118=ORIENTED_EDGE ( 'NONE', *, *, #134087, .T. ) ;
#196132=ORIENTED_EDGE ( 'NONE', *, *, #96704, .F. ) ;
#196176=CARTESIAN_POINT ( 'NONE',  ( -1.360316468750044860, 1.151041667008095404, -0.7853790794159261068 ) ) ;
#196208=AXIS2_PLACEMENT_3D ( 'NONE', #77054, #126975, #14169 ) ;
#196213=CARTESIAN_POINT ( 'NONE',  ( -1.162044386198238837E-16, 2.062499999999991562, 1.224999999999974332 ) ) ;
#196234=VERTEX_POINT ( 'NONE', #64570 ) ;
#196372=ORIENTED_EDGE ( 'NONE', *, *, #35863, .F. ) ;
#196461=CARTESIAN_POINT ( 'NONE',  ( 1.814759087649916003, 3.975067388631702059, -0.4606438099578838985 ) ) ;
#196471=CARTESIAN_POINT ( 'NONE',  ( -1.953008978358306879E-14, -0.5156249996585442474, 1.570758158831760287 ) ) ;
#196616=ORIENTED_EDGE ( 'NONE', *, *, #157243, .T. ) ;
#196621=CARTESIAN_POINT ( 'NONE',  ( -0.5000000000000091038, 3.949999999999960654, 0.3999999999999455103 ) ) ;
#196640=LINE ( 'NONE', #2664, #6935 ) ;
#196641=AXIS2_PLACEMENT_3D ( 'NONE', #81295, #82343, #77287 ) ;
#196775=CARTESIAN_POINT ( 'NONE',  ( 0.5101186646354113341, -1.387778780781445676E-14, 1.261047121698059215 ) ) ;
#196813=CARTESIAN_POINT ( 'NONE',  ( -3.469446951953614189E-15, 3.236073672982384242, -5.377642775528101993E-14 ) ) ;
#196873=CARTESIAN_POINT ( 'NONE',  ( 1.360316468749965590, 1.067708333674703081, -0.7853790794159083433 ) ) ;
#196878=EDGE_LOOP ( 'NONE', ( #13404, #74501, #1916, #127058, #143457, #206184 ) ) ;
#196922=CARTESIAN_POINT ( 'NONE',  ( 1.914442667406905496, 3.262253226108020154, 0.4355078757043838178 ) ) ;
#196981=CARTESIAN_POINT ( 'NONE',  ( -0.4000000000000513700, 3.949999999999967315, 0.8338124244295243015 ) ) ;
#196992=EDGE_CURVE ( 'NONE', #177247, #80420, #117540, .T. ) ;
#197001=CARTESIAN_POINT ( 'NONE',  ( 1.360316468749955598, -0.7135416663252973635, -0.7853790794159122290 ) ) ;
#197103=ORIENTED_EDGE ( 'NONE', *, *, #31466, .F. ) ;
#197220=CARTESIAN_POINT ( 'NONE',  ( 1.360316468750007779, 1.296875000341410455, -2.602085213965210642E-14 ) ) ;
#197259=CARTESIAN_POINT ( 'NONE',  ( 0.6801582343749796866, 1.723958333674766141, 1.178068619123784355 ) ) ;
#197283=CARTESIAN_POINT ( 'NONE',  ( -0.6125000000000019318, 0.2708333340161322988, -1.060881119635941339 ) ) ;
#197284=( BOUNDED_CURVE ( )  B_SPLINE_CURVE ( 2, ( #209390, #41609, #75155, #40531, #106635, #91425, #28537, #127195, #56767 ),
 .UNSPECIFIED., .F., .T. ) 
 B_SPLINE_CURVE_WITH_KNOTS ( ( 3, 2, 2, 2, 3 ),
 ( 0.3593749999999997224, 0.3645833333333333148, 0.3750000000000000000, 0.3854166666666666852, 0.3906250000000002220 ),
 .UNSPECIFIED. ) 
 CURVE ( )  GEOMETRIC_REPRESENTATION_ITEM ( )  RATIONAL_B_SPLINE_CURVE ( ( 0.9330127018922194093, 0.9330127018922158566, 1.000000000000000000, 0.8660254037844387076, 1.000000000000000000, 0.8660254037844387076, 1.000000000000000000, 0.9330127018922165227, 0.9330127018922194093 ) ) 
 REPRESENTATION_ITEM ( '' )  );
#197298=EDGE_LOOP ( 'NONE', ( #125199, #23329, #18213, #132754 ) ) ;
#197355=CARTESIAN_POINT ( 'NONE',  ( -0.3000000000000068723, 3.172938907704321743, -0.5000000000000195399 ) ) ;
#197390=EDGE_LOOP ( 'NONE', ( #62104, #209172, #51700, #117278 ) ) ;
#197402=ADVANCED_FACE ( 'NONE', ( #118137 ), #126963, .T. ) ;
#197436=CARTESIAN_POINT ( 'NONE',  ( -0.6125000000000105915, 1.604166667349450570, 1.060881119635899816 ) ) ;
#197470=CARTESIAN_POINT ( 'NONE',  ( -1.225000000000012523, 2.000000000000001776, -1.214306433183764966E-14 ) ) ;
#197493=EDGE_CURVE ( 'NONE', #107567, #195016, #168708, .T. ) ;
#197497=CARTESIAN_POINT ( 'NONE',  ( -0.4465194593918104249, 3.080450244942120719, -0.4155024747329819634 ) ) ;
#197517=CARTESIAN_POINT ( 'NONE',  ( -0.6801582343750316451, -0.7864583329919294652, 1.178068619123805227 ) ) ;
#197577=CARTESIAN_POINT ( 'NONE',  ( -0.6125000000000262457, 0.4583333333333244886, -1.060881119635996850 ) ) ;
#197639=AXIS2_PLACEMENT_3D ( 'NONE', #97802, #15441, #81530 ) ;
#197756=EDGE_CURVE ( 'NONE', #109478, #196234, #204622, .T. ) ;
#197767=CARTESIAN_POINT ( 'NONE',  ( -0.6801582343750351978, 2.630208333674721732, -1.178068619123886718 ) ) ;
#197851=CIRCLE ( 'NONE', #21556, 0.04999999999999985706 ) ;
#197928=CARTESIAN_POINT ( 'NONE',  ( -1.360316468750062624, 1.401041667008104730, -0.7853790794158941324 ) ) ;
#197951=CARTESIAN_POINT ( 'NONE',  ( 0.000000000000000000, 0.000000000000000000, 0.000000000000000000 ) ) ;
#197975=CARTESIAN_POINT ( 'NONE',  ( -2.440293211016301606E-15, 1.187499999999993117, -1.225000000000025624 ) ) ;
#197980=CARTESIAN_POINT ( 'NONE',  ( 1.889772045536127765, 3.296949564223940143, 0.4024211290685025255 ) ) ;
#198000=ORIENTED_EDGE ( 'NONE', *, *, #187251, .F. ) ;
#198058=CARTESIAN_POINT ( 'NONE',  ( -0.6801582343750125492, -0.6510416663252707181, -1.178068619123848526 ) ) ;
#198082=CARTESIAN_POINT ( 'NONE',  ( -0.6801582343750299797, 1.182291667008061875, 1.178068619123820771 ) ) ;
#198264=CARTESIAN_POINT ( 'NONE',  ( 1.224999999999979217, 1.208333334016137739, -0.7072540797573078075 ) ) ;
#198275=CARTESIAN_POINT ( 'NONE',  ( -0.6801582343750316451, -0.7864583329919294652, 1.178068619123805227 ) ) ;
#198314=CARTESIAN_POINT ( 'NONE',  ( -1.360316468750004448, 1.640625000341400241, -2.602085213965210642E-14 ) ) ;
#198321=LINE ( 'NONE', #195155, #171350 ) ;
#198336=ORIENTED_EDGE ( 'NONE', *, *, #9020, .F. ) ;
#198353=EDGE_CURVE ( 'NONE', #124142, #67541, #62460, .T. ) ;
#198391=AXIS2_PLACEMENT_3D ( 'NONE', #207439, #210640, #173915 ) ;
#198421=DIRECTION ( 'NONE',  ( 3.497202527569253358E-15, -0.000000000000000000, 1.000000000000000000 ) ) ;
#198429=CARTESIAN_POINT ( 'NONE',  ( 0.4169036860909946518, 3.145283463680713432, 0.4342470185718878550 ) ) ;
#198510=PLANE ( 'NONE',  #150611 ) ;
#198523=CARTESIAN_POINT ( 'NONE',  ( -0.3282377607281401488, 1.948664549684637315, -1.225000000000025846 ) ) ;
#198538=VERTEX_POINT ( 'NONE', #79772 ) ;
#198568=CARTESIAN_POINT ( 'NONE',  ( 1.360316468749981800, -0.4739583329918962695, 0.7853790794158760358 ) ) ;
#198600=CARTESIAN_POINT ( 'NONE',  ( -0.3282377607281340426, 1.051335450315359576, 1.224999999999977440 ) ) ;
#198637=ORIENTED_EDGE ( 'NONE', *, *, #124980, .F. ) ;
#198691=ORIENTED_EDGE ( 'NONE', *, *, #161766, .T. ) ;
#198698=EDGE_CURVE ( 'NONE', #61933, #13808, #161776, .T. ) ;
#198712=CARTESIAN_POINT ( 'NONE',  ( -2.091679895156829610E-15, 2.562499999999987121, 1.224999999999973888 ) ) ;
#198731=DIRECTION ( 'NONE',  ( 1.000000000000000000, -7.771561172376097755E-16, -4.440892098500627148E-16 ) ) ;
#198779=CARTESIAN_POINT ( 'NONE',  ( 1.872871967411071648, 3.299999999999997158, 0.3999999999999958589 ) ) ;
#198781=ORIENTED_EDGE ( 'NONE', *, *, #155989, .F. ) ;
#198878=CARTESIAN_POINT ( 'NONE',  ( 1.772826578343093873, 3.949999999999995293, 0.3999999999999819811 ) ) ;
#198979=CARTESIAN_POINT ( 'NONE',  ( -0.6801582343750229853, 1.380208333674720622, -1.178068619123855409 ) ) ;
#198996=CARTESIAN_POINT ( 'NONE',  ( -0.4626273691814692390, 3.108307088186299527, 0.4053073865229923078 ) ) ;
#199043=( BOUNDED_CURVE ( )  B_SPLINE_CURVE ( 2, ( #126443, #108048, #206529, #139427, #156743, #172994, #192406, #72249, #124319 ),
 .UNSPECIFIED., .F., .T. ) 
 B_SPLINE_CURVE_WITH_KNOTS ( ( 3, 2, 2, 2, 3 ),
 ( 0.07812500000000006939, 0.08333333333333332871, 0.09375000000000000000, 0.1041666666666666713, 0.1093749999999997641 ),
 .UNSPECIFIED. ) 
 CURVE ( )  GEOMETRIC_REPRESENTATION_ITEM ( )  RATIONAL_B_SPLINE_CURVE ( ( 0.9330127018922194093, 0.9330127018922202975, 1.000000000000000000, 0.8660254037844387076, 1.000000000000000000, 0.8660254037844387076, 1.000000000000000000, 0.9330127018922224069, 0.9330127018922194093 ) ) 
 REPRESENTATION_ITEM ( '' )  );
#199106=CARTESIAN_POINT ( 'NONE',  ( -5.758872628492444169E-14, -0.1718749996585747786, -1.570758158831818241 ) ) ;
#199130=CARTESIAN_POINT ( 'NONE',  ( 1.360316468749949825, 1.994791667008131597, 0.7853790794158701516 ) ) ;
#199193=EDGE_CURVE ( 'NONE', #106774, #22081, #102756, .T. ) ;
#199201=VECTOR ( 'NONE', #9530, 1000.000000000000000 ) ;
#199216=EDGE_CURVE ( 'NONE', #81519, #109478, #42864, .T. ) ;
#199237=CARTESIAN_POINT ( 'NONE',  ( -0.3000000000000033751, 3.950000000000001954, -1.007084189318394385 ) ) ;
#199267=CARTESIAN_POINT ( 'NONE',  ( -1.162044386198238935E-15, 0.3125000000000180411, 1.224999999999967004 ) ) ;
#199298=CARTESIAN_POINT ( 'NONE',  ( -1.225000000000014300, 2.750000000000002665, -3.469446951953614189E-14 ) ) ;
#199337=CARTESIAN_POINT ( 'NONE',  ( 0.6801582343749813520, 0.005208333674754095366, 1.178068619123793015 ) ) ;
#199377=CARTESIAN_POINT ( 'NONE',  ( -1.360316468749990459, 1.890625000341386475, -2.428612866367529932E-14 ) ) ;
#199403=CARTESIAN_POINT ( 'NONE',  ( -1.734723475976807094E-15, 2.999999999999988898, -6.938893903907228378E-15 ) ) ;
#199415=EDGE_CURVE ( 'NONE', #179126, #23953, #76415, .T. ) ;
#199593=CARTESIAN_POINT ( 'NONE',  ( -0.6125000000000140332, 2.041666666666650087, 1.060881119635936232 ) ) ;
#199644=CARTESIAN_POINT ( 'NONE',  ( -2.449742653233043743, 3.299999999999976730, -0.4000000000000339950 ) ) ;
#199677=CARTESIAN_POINT ( 'NONE',  ( -0.6125000000000244693, 1.520833334016126415, -1.060881119635955327 ) ) ;
#199787=LINE ( 'NONE', #86055, #166929 ) ;
#199813=CARTESIAN_POINT ( 'NONE',  ( -0.3282377607281289911, 0.6986645496846380921, -1.225000000000010747 ) ) ;
#199815=CARTESIAN_POINT ( 'NONE',  ( -0.3282377607281401488, 1.011164550367433579, -1.225000000000022959 ) ) ;
#199891=CARTESIAN_POINT ( 'NONE',  ( -6.760415694317216410E-14, 2.234375000341476625, 1.570758158831744078 ) ) ;
#199914=CARTESIAN_POINT ( 'NONE',  ( -1.225000000000028066, 0.5000000000000143219, -5.030698080332740574E-14 ) ) ;
#199982=DIRECTION ( 'NONE',  ( -1.276756478318932585E-15, 1.000000000000000000, -1.665334536937738262E-16 ) ) ;
#200060=CARTESIAN_POINT ( 'NONE',  ( -1.360316468750032204, 0.6718750003414097893, -2.081668171172168513E-14 ) ) ;
#200127=ORIENTED_EDGE ( 'NONE', *, *, #107456, .T. ) ;
#200173=CARTESIAN_POINT ( 'NONE',  ( -0.6125000000000089262, 1.791666666666677621, 1.060881119635936232 ) ) ;
#200203=CARTESIAN_POINT ( 'NONE',  ( -1.360316468749998675, 2.411458333674741716, 0.7853790794158941324 ) ) ;
#200290=CARTESIAN_POINT ( 'NONE',  ( -1.907713928855368168, 3.283019769909846897, -0.4154771360143861836 ) ) ;
#200341=ORIENTED_EDGE ( 'NONE', *, *, #81383, .F. ) ;
#200357=FACE_OUTER_BOUND ( 'NONE', #173195, .T. ) ;
#200364=CARTESIAN_POINT ( 'NONE',  ( -1.225000000000040279, 0.2500000000000002220, -4.857225732735059864E-14 ) ) ;
#200368=CARTESIAN_POINT ( 'NONE',  ( 1.224999999999992983, -0.04166666598383617082, -0.7072540797572937077 ) ) ;
#200402=CARTESIAN_POINT ( 'NONE',  ( 0.6801582343749900117, -0.6614583329919085930, -1.178068619123883165 ) ) ;
#200407=AXIS2_PLACEMENT_3D ( 'NONE', #95216, #132002, #161266 ) ;
#200423=EDGE_CURVE ( 'NONE', #118779, #89507, #65776, .T. ) ;
#200443=CARTESIAN_POINT ( 'NONE',  ( 0.6801582343749917881, 0.7239583336747443809, 1.178068619123793015 ) ) ;
#200538=ORIENTED_EDGE ( 'NONE', *, *, #160015, .F. ) ;
#200617=DIRECTION ( 'NONE',  ( -5.828670879282089587E-16, 0.8656921114426507913, -0.5005768354468322912 ) ) ;
#200735=CARTESIAN_POINT ( 'NONE',  ( -0.6125000000000383471, 1.854166667349464781, 1.060881119635894487 ) ) ;
#200746=DIRECTION ( 'NONE',  ( -1.276756478318932585E-15, 1.000000000000000000, -1.665334536937738262E-16 ) ) ;
#200801=CARTESIAN_POINT ( 'NONE',  ( -2.449742653233059286, 3.300000000000011369, 0.3999999999999750422 ) ) ;
#200808=CARTESIAN_POINT ( 'NONE',  ( 1.980939963429169115, 3.482546949474367715, 0.4617747962883785862 ) ) ;
#200857=CARTESIAN_POINT ( 'NONE',  ( 7.785697387528199762E-15, 0.4375000000000076605, -1.225000000000032951 ) ) ;
#200942=CARTESIAN_POINT ( 'NONE',  ( -1.360316468750002672, 1.921875000341424666, -3.642919299551294898E-14 ) ) ;
#200965=CARTESIAN_POINT ( 'NONE',  ( -1.225000000000016076, 0.2708333333333532988, 0.7072540797572717253 ) ) ;
#200986=ORIENTED_EDGE ( 'NONE', *, *, #4745, .F. ) ;
#201009=CARTESIAN_POINT ( 'NONE',  ( 0.4999999999999674705, 3.999999999999989786, 0.4499999999999625966 ) ) ;
#201019=AXIS2_PLACEMENT_3D ( 'NONE', #93166, #45475, #128919 ) ;
#201053=ADVANCED_FACE ( 'NONE', ( #104738 ), #22376, .T. ) ;
#201117=CARTESIAN_POINT ( 'NONE',  ( -1.360316468749996899, 0.4010416670080598767, -0.7853790794158941324 ) ) ;
#201203=( BOUNDED_CURVE ( )  B_SPLINE_CURVE ( 2, ( #65320, #184416, #199593, #67444, #197470, #163933, #3513, #198523, #1383 ),
 .UNSPECIFIED., .F., .T. ) 
 B_SPLINE_CURVE_WITH_KNOTS ( ( 3, 2, 2, 2, 3 ),
 ( 0.2343749999999997780, 0.2395833333333333426, 0.2500000000000000000, 0.2604166666666666852, 0.2656250000000002220 ),
 .UNSPECIFIED. ) 
 CURVE ( )  GEOMETRIC_REPRESENTATION_ITEM ( )  RATIONAL_B_SPLINE_CURVE ( ( 0.9330127018922194093, 0.9330127018922165227, 1.000000000000000000, 0.8660254037844387076, 1.000000000000000000, 0.8660254037844387076, 1.000000000000000000, 0.9330127018922165227, 0.9330127018922194093 ) ) 
 REPRESENTATION_ITEM ( '' )  );
#201266=CARTESIAN_POINT ( 'NONE',  ( -0.6801582343750368631, 1.682291667008048552, 1.178068619123803451 ) ) ;
#201337=CARTESIAN_POINT ( 'NONE',  ( -1.225000000000018074, 2.979166666666678065, -0.7072540797572998139 ) ) ;
#201367=CARTESIAN_POINT ( 'NONE',  ( -3.074561225638268725E-14, 3.499999999999960920, -1.052419468952713544 ) ) ;
#201379=EDGE_LOOP ( 'NONE', ( #151633, #102588, #159750, #81956, #49032, #135061 ) ) ;
#201387=CARTESIAN_POINT ( 'NONE',  ( -1.360316468750033980, 2.906250000341399797, -3.469446951953614189E-14 ) ) ;
#201393=CARTESIAN_POINT ( 'NONE',  ( 0.4288785890452437299, 3.049942316455264812, -0.4196807566835009662 ) ) ;
#201400=DIRECTION ( 'NONE',  ( 1.000000000000000000, -7.771561172376097755E-16, -4.440892098500627148E-16 ) ) ;
#201428=CARTESIAN_POINT ( 'NONE',  ( 1.224999999999989875, -1.062499999317199961, -3.469446951953614189E-15 ) ) ;
#201444=ORIENTED_EDGE ( 'NONE', *, *, #35195, .F. ) ;
#201462=CARTESIAN_POINT ( 'NONE',  ( 1.360316468749969809, -0.6822916663252893699, -0.7853790794159082322 ) ) ;
#201479=CARTESIAN_POINT ( 'NONE',  ( 1.772826578343081660, 3.950000000000036593, -0.4000000000000478728 ) ) ;
#201504=CARTESIAN_POINT ( 'NONE',  ( -0.6801582343750299797, 1.182291667008061875, 1.178068619123820771 ) ) ;
#201596=CYLINDRICAL_SURFACE ( 'NONE', #133717, 0.05000000000000002359 ) ;
#201599=EDGE_LOOP ( 'NONE', ( #168172, #131134, #155611, #176765 ) ) ;
#201628=( BOUNDED_SURFACE ( )  B_SPLINE_SURFACE ( 3, 2, ( 
 ( #9040, #107681, #190972 ),
 ( #108747, #75114, #25285 ),
 ( #126077, #154231, #40492 ),
 ( #188856, #206165, #141226 ) ),
 .UNSPECIFIED., .F., .F., .F. ) 
 B_SPLINE_SURFACE_WITH_KNOTS ( ( 4, 4 ),
 ( 3, 3 ),
 ( 0.5050616349177513564, 1.570796326794896558 ),
 ( 0.000000000000000000, 1.000000000000000000 ),
 .UNSPECIFIED. ) 
 GEOMETRIC_REPRESENTATION_ITEM ( )  RATIONAL_B_SPLINE_SURFACE ( (
 ( 1.000000000000000000, 0.9374448844494494004, 1.000000000000000000),
 ( 1.000000000000000000, 0.8980788380694090245, 1.000000000000000000),
 ( 1.000000000000000000, 0.8161930835858599576, 1.000000000000000000),
 ( 1.000000000000000000, 0.7071067811865933139, 1.000000000000000000) ) ) 
 REPRESENTATION_ITEM ( '' )  SURFACE ( )  );
#201642=EDGE_CURVE ( 'NONE', #124142, #22696, #64954, .T. ) ;
#201694=DIRECTION ( 'NONE',  ( 4.440892098500630106E-16, 3.330669073875473073E-16, 1.000000000000000000 ) ) ;
#201704=CARTESIAN_POINT ( 'NONE',  ( 7.785697387528199762E-15, 0.4375000000000076605, -1.225000000000032951 ) ) ;
#201718=LINE ( 'NONE', #24045, #181961 ) ;
#201734=ORIENTED_EDGE ( 'NONE', *, *, #7576, .T. ) ;
#201770=EDGE_CURVE ( 'NONE', #28948, #60914, #12430, .T. ) ;
#201795=CARTESIAN_POINT ( 'NONE',  ( 1.278248824818062671E-15, 1.062499999999996003, 1.224999999999968781 ) ) ;
#201801=CARTESIAN_POINT ( 'NONE',  ( -0.6124999999999984901, 2.354166667349471886, 1.060881119635896264 ) ) ;
#201858=CARTESIAN_POINT ( 'NONE',  ( 0.3000000000000016542, 4.000000000000003553, -1.007084189318387502 ) ) ;
#201878=VERTEX_POINT ( 'NONE', #89301 ) ;
#201889=CARTESIAN_POINT ( 'NONE',  ( 0.3423093779009768189, 2.999999999999988898, -0.4000000000000409339 ) ) ;
#201999=CARTESIAN_POINT ( 'NONE',  ( 0.6801582343749952297, 2.088541667008066316, -1.178068619123855409 ) ) ;
#202022=CARTESIAN_POINT ( 'NONE',  ( -0.6125000000000279110, 1.291666666666656305, 1.060881119635892933 ) ) ;
#202085=EDGE_CURVE ( 'NONE', #105749, #47983, #30407, .T. ) ;
#202136=AXIS2_PLACEMENT_3D ( 'NONE', #172423, #210228, #175633 ) ;
#202175=EDGE_CURVE ( 'NONE', #177247, #153954, #186275, .T. ) ;
#202208=ORIENTED_EDGE ( 'NONE', *, *, #170740, .T. ) ;
#202331=CARTESIAN_POINT ( 'NONE',  ( 1.360316468749994012, 2.265625000341386919, -1.387778780781445676E-14 ) ) ;
#202345=CARTESIAN_POINT ( 'NONE',  ( -1.734723475976807094E-15, 2.999999999999988898, -6.938893903907228378E-15 ) ) ;
#202495=CARTESIAN_POINT ( 'NONE',  ( -9.514659125335341649E-15, -0.9999999993172007384, -1.414508159514585417 ) ) ;
#202513=CARTESIAN_POINT ( 'NONE',  ( -8.673617379884035472E-15, 3.975067388631681187, -1.561251128379126385E-14 ) ) ;
#202530=CARTESIAN_POINT ( 'NONE',  ( -1.953008978358306879E-14, -0.5156249996585442474, 1.570758158831760287 ) ) ;
#202558=EDGE_LOOP ( 'NONE', ( #61967, #198000, #9144, #69360 ) ) ;
#202562=CARTESIAN_POINT ( 'NONE',  ( -1.360316468750056851, 1.369791667008064540, -0.7853790794159101196 ) ) ;
#202571=CARTESIAN_POINT ( 'NONE',  ( -0.6801582343749917881, 0.4322916670080681478, 1.178068619123841643 ) ) ;
#202602=CARTESIAN_POINT ( 'NONE',  ( 0.4999999999999900080, 3.949999999999974420, 0.4999999999999640288 ) ) ;
#202611=CARTESIAN_POINT ( 'NONE',  ( 6.856061878569608298E-15, 0.9375000000000238698, -1.225000000000010525 ) ) ;
#202839=FACE_OUTER_BOUND ( 'NONE', #137664, .T. ) ;
#202869=CARTESIAN_POINT ( 'NONE',  ( 0.6125000000000071498, 2.395833334016134408, 1.060881119635924019 ) ) ;
#202930=CARTESIAN_POINT ( 'NONE',  ( -3.486133158594716510E-16, 2.687500000000001332, -1.225000000000008749 ) ) ;
#202952=CARTESIAN_POINT ( 'NONE',  ( -0.3000000000000155320, 3.999999999999955147, 1.007084189318345757 ) ) ;
#203057=VERTEX_POINT ( 'NONE', #117079 ) ;
#203080=CARTESIAN_POINT ( 'NONE',  ( 1.360316468749955598, 1.526041667008097180, 0.7853790794158861388 ) ) ;
#203102=CARTESIAN_POINT ( 'NONE',  ( -0.6125000000000089262, 0.7083333333333317050, -1.060881119635948444 ) ) ;
#203145=ORIENTED_EDGE ( 'NONE', *, *, #204483, .F. ) ;
#203156=CARTESIAN_POINT ( 'NONE',  ( 0.4170821662628915183, 3.033599471985643170, 0.4170821662628724225 ) ) ;
#203184=ORIENTED_EDGE ( 'NONE', *, *, #44491, .T. ) ;
#203207=ORIENTED_EDGE ( 'NONE', *, *, #204467, .F. ) ;
#203218=DIRECTION ( 'NONE',  ( -1.276756478318932585E-15, 1.000000000000000000, -1.665334536937738262E-16 ) ) ;
#203384=ADVANCED_FACE ( 'NONE', ( #52024 ), #170021, .F. ) ;
#203393=DIRECTION ( 'NONE',  ( 3.330669073875478989E-16, -3.540251991789410786E-16, -1.000000000000000000 ) ) ;
#203395=ORIENTED_EDGE ( 'NONE', *, *, #35195, .T. ) ;
#203397=CARTESIAN_POINT ( 'NONE',  ( 0.6801582343749935644, 0.9739583336747514863, 1.178068619123805227 ) ) ;
#203399=FACE_OUTER_BOUND ( 'NONE', #107873, .T. ) ;
#203467=CARTESIAN_POINT ( 'NONE',  ( -1.225000000000044276, 1.729166666666672292, -0.7072540797572958171 ) ) ;
#203513=CARTESIAN_POINT ( 'NONE',  ( 1.311466561510864937, 4.574475816212405313E-14, -0.2054205618200592443 ) ) ;
#203561=CARTESIAN_POINT ( 'NONE',  ( 1.224999999999999201, -0.5416666659838705877, -0.7072540797572937077 ) ) ;
#203628=CARTESIAN_POINT ( 'NONE',  ( -0.6801582343750282034, 2.432291667008048996, 1.178068619123807004 ) ) ;
#203637=CARTESIAN_POINT ( 'NONE',  ( 1.360316468749963592, 0.03645833367470611985, -0.7853790794159122290 ) ) ;
#203702=CARTESIAN_POINT ( 'NONE',  ( 0.3282377607281144472, 0.3861645503674552837, 1.224999999999980105 ) ) ;
#203705=CARTESIAN_POINT ( 'NONE',  ( 1.859593142679900613, 3.245846270153683211, 0.3999999999999849787 ) ) ;
#203706=CARTESIAN_POINT ( 'NONE',  ( -0.3769810270651957618, 3.049942316455299451, -0.4288785890453079008 ) ) ;
#203748=( BOUNDED_CURVE ( )  B_SPLINE_CURVE ( 2, ( #183158, #52098, #1182, #115027, #17432, #149596, #148538, #67246, #16370 ),
 .UNSPECIFIED., .F., .T. ) 
 B_SPLINE_CURVE_WITH_KNOTS ( ( 3, 2, 2, 2, 3 ),
 ( 0.2343749999999998057, 0.2395833333333333426, 0.2500000000000000000, 0.2604166666666666852, 0.2656250000000001110 ),
 .UNSPECIFIED. ) 
 CURVE ( )  GEOMETRIC_REPRESENTATION_ITEM ( )  RATIONAL_B_SPLINE_CURVE ( ( 0.9330127018922194093, 0.9330127018922168558, 1.000000000000000000, 0.8660254037844387076, 1.000000000000000000, 0.8660254037844387076, 1.000000000000000000, 0.9330127018922178550, 0.9330127018922192983 ) ) 
 REPRESENTATION_ITEM ( '' )  );
#203756=AXIS2_PLACEMENT_3D ( 'NONE', #136279, #53951, #68024 ) ;
#203769=CARTESIAN_POINT ( 'NONE',  ( -0.4000000000000166755, 3.949999999999995293, -0.8338124244296005738 ) ) ;
#203935=CARTESIAN_POINT ( 'NONE',  ( -5.157946788997579689E-14, 1.250000000682857992, -1.414508159514609620 ) ) ;
#204136=CARTESIAN_POINT ( 'NONE',  ( 1.360316468750007779, 1.296875000341410455, -2.602085213965210642E-14 ) ) ;
#204158=CARTESIAN_POINT ( 'NONE',  ( 0.6125000000000037081, -0.1666666666666691277, 1.060881119635939562 ) ) ;
#204212=( BOUNDED_CURVE ( )  B_SPLINE_CURVE ( 2, ( #12577, #78649, #144776, #63479, #195620, #211841, #129633, #79720, #145837 ),
 .UNSPECIFIED., .F., .T. ) 
 B_SPLINE_CURVE_WITH_KNOTS ( ( 3, 2, 2, 2, 3 ),
 ( 0.2656250000000001110, 0.2708333333333333148, 0.2812500000000000000, 0.2916666666666666852, 0.2968749999999997780 ),
 .UNSPECIFIED. ) 
 CURVE ( )  GEOMETRIC_REPRESENTATION_ITEM ( )  RATIONAL_B_SPLINE_CURVE ( ( 0.9330127018922192983, 0.9330127018922207416, 1.000000000000000000, 0.8660254037844387076, 1.000000000000000000, 0.8660254037844387076, 1.000000000000000000, 0.9330127018922221849, 0.9330127018922194093 ) ) 
 REPRESENTATION_ITEM ( '' )  );
#204293=B_SPLINE_CURVE_WITH_KNOTS ( 'NONE', 3,
 ( #120169, #102783, #170974, #38849 ),
 .UNSPECIFIED., .F., .F.,
 ( 4, 4 ),
 ( 0.000000000000000000, 1.930757672285080358E-06 ),
 .UNSPECIFIED. ) ;
#204296=ORIENTED_EDGE ( 'NONE', *, *, #61620, .T. ) ;
#204304=EDGE_LOOP ( 'NONE', ( #171986, #160548, #208885, #167990, #73679, #181462 ) ) ;
#204313=CARTESIAN_POINT ( 'NONE',  ( -2.353626204688216217E-14, 0.7343750003414535321, 1.570758158831780271 ) ) ;
#204354=VERTEX_POINT ( 'NONE', #109123 ) ;
#204417=PRODUCT_DEFINITION_FORMATION_WITH_SPECIFIED_SOURCE ( 'ANY', '', #80054, .NOT_KNOWN. ) ;
#204464=CARTESIAN_POINT ( 'NONE',  ( -1.360316468750026653, -0.1302083329919105914, -0.7853790794159422051 ) ) ;
#204467=EDGE_CURVE ( 'NONE', #122076, #68973, #210497, .T. ) ;
#204483=EDGE_CURVE ( 'NONE', #42660, #175731, #26366, .T. ) ;
#204516=DIRECTION ( 'NONE',  ( -1.000000000000000000, 7.771561172376097755E-16, 4.440892098500627148E-16 ) ) ;
#204539=CARTESIAN_POINT ( 'NONE',  ( 1.225000000000000311, 1.874999999999994671, -1.734723475976807094E-15 ) ) ;
#204571=CARTESIAN_POINT ( 'NONE',  ( -1.908029163539572748, 3.237038651130945244, 0.4603255239806047228 ) ) ;
#204582=CARTESIAN_POINT ( 'NONE',  ( 0.5227789990447535562, -7.252376619629073204E-15, -1.145890942912077826 ) ) ;
#204622=LINE ( 'NONE', #60522, #57768 ) ;
#204629=CARTESIAN_POINT ( 'NONE',  ( -0.6125000000000192513, -0.9791666659838688114, -1.060881119635955327 ) ) ;
#204676=EDGE_LOOP ( 'NONE', ( #129937, #142109, #39607, #61007 ) ) ;
#204680=CARTESIAN_POINT ( 'NONE',  ( -1.874158809982213958, 3.299964346911606228, -0.4000000000000374922 ) ) ;
#204696=CARTESIAN_POINT ( 'NONE',  ( -4.757329562667670667E-14, 1.953125000341451312, 1.570758158831762286 ) ) ;
#204703=CARTESIAN_POINT ( 'NONE',  ( 0.6801582343749970061, 0.5572916670080683144, -1.178068619123862515 ) ) ;
#204744=( BOUNDED_CURVE ( )  B_SPLINE_CURVE ( 3, ( #104723, #70037, #21289, #67897 ),
 .UNSPECIFIED., .F., .T. ) 
 B_SPLINE_CURVE_WITH_KNOTS ( ( 4, 4 ),
 ( 0.6625062783165582836, 1.570796326794877462 ),
 .UNSPECIFIED. ) 
 CURVE ( )  GEOMETRIC_REPRESENTATION_ITEM ( )  RATIONAL_B_SPLINE_CURVE ( ( 1.000000000000000000, 0.9324242863012628391, 0.9324242863012628391, 1.000000000000000000 ) ) 
 REPRESENTATION_ITEM ( '' )  );
#204765=CYLINDRICAL_SURFACE ( 'NONE', #80509, 1.224999999999996980 ) ;
#204768=CARTESIAN_POINT ( 'NONE',  ( 1.919777701841143713, 3.227564709615617033, 0.3999999999999849787 ) ) ;
#204783=EDGE_CURVE ( 'NONE', #5098, #149263, #188019, .T. ) ;
#204894=CARTESIAN_POINT ( 'NONE',  ( 4.996790860652426159E-15, 0.6250000006827882704, 1.224999999999976330 ) ) ;
#204903=CARTESIAN_POINT ( 'NONE',  ( 0.6124999999999914957, 1.416666666666690944, -1.060881119635986414 ) ) ;
#204929=CARTESIAN_POINT ( 'NONE',  ( 0.6801582343749952297, 2.088541667008066316, -1.178068619123855409 ) ) ;
#204986=CARTESIAN_POINT ( 'NONE',  ( -0.3000000000000103140, 0.6284510210557009424, -1.086836331270430334 ) ) ;
#205010=CARTESIAN_POINT ( 'NONE',  ( 1.224999999999965006, 0.4166666673494939799, 0.7072540797572456350 ) ) ;
#205035=DIRECTION ( 'NONE',  ( 3.330669073875478989E-16, -3.540251991789410786E-16, -1.000000000000000000 ) ) ;
#205076=DIRECTION ( 'NONE',  ( 1.000000000000000000, -7.771561172376097755E-16, -4.440892098500627148E-16 ) ) ;
#205106=CARTESIAN_POINT ( 'NONE',  ( 7.785697387528199762E-15, 0.5624999999999894529, 1.224999999999973443 ) ) ;
#205108=ORIENTED_EDGE ( 'NONE', *, *, #2927, .F. ) ;
#205133=CARTESIAN_POINT ( 'NONE',  ( -0.4500000000000232703, 4.000000000000003553, -0.8627243683430544374 ) ) ;
#205195=EDGE_CURVE ( 'NONE', #109538, #12920, #51644, .T. ) ;
#205220=CARTESIAN_POINT ( 'NONE',  ( 1.360316468749978469, 1.046875000341403128, -2.602085213965210642E-14 ) ) ;
#205242=CARTESIAN_POINT ( 'NONE',  ( 1.360316468749975582, 2.776041667008103175, 0.7853790794158820310 ) ) ;
#205252=AXIS2_PLACEMENT_3D ( 'NONE', #116145, #150738, #2299 ) ;
#205326=CARTESIAN_POINT ( 'NONE',  ( -0.6125000000000105915, 0.04166666666666901664, 1.060881119635925796 ) ) ;
#205366=B_SPLINE_CURVE_WITH_KNOTS ( 'NONE', 3,
 ( #141931, #123604, #172269, #173345, #140864, #71532, #58509, #205812, #124664, #42280, #120385, #186360, #60633, #210068, #77952, #10804, #194900, #159203, #46538, #111591, #160273, #112659 ),
 .UNSPECIFIED., .F., .F.,
 ( 4, 3, 3, 3, 3, 3, 3, 4 ),
 ( -1.454680003632761151E-06, 0.000000000000000000, 2.747234201905744114E-05, 5.316625080982969768E-05, 7.164957654723469569E-05, 8.369272870878160088E-05, 9.574357740280491178E-05, 0.0001078040709964582646 ),
 .UNSPECIFIED. ) ;
#205446=DIRECTION ( 'NONE',  ( -5.421010862427537947E-16, 0.000000000000000000, 1.000000000000000000 ) ) ;
#205468=EDGE_CURVE ( 'NONE', #204354, #40528, #117792, .T. ) ;
#205531=CARTESIAN_POINT ( 'NONE',  ( -1.907519672996902838, 3.236073672982390903, -0.4612874649730039911 ) ) ;
#205545=CARTESIAN_POINT ( 'NONE',  ( 0.6801582343749831283, 1.057291667008075642, -1.178068619123862515 ) ) ;
#205547=CARTESIAN_POINT ( 'NONE',  ( 3.486133158594716510E-16, 2.312499999999992006, 1.224999999999971889 ) ) ;
#205616=CARTESIAN_POINT ( 'NONE',  ( 0.6125000000000001554, 2.166666666666670960, -1.060881119635941339 ) ) ;
#205644=VERTEX_POINT ( 'NONE', #73225 ) ;
#205718=VECTOR ( 'NONE', #49579, 1000.000000000000114 ) ;
#205753=CIRCLE ( 'NONE', #43291, 1.829047314007942848 ) ;
#205779=CARTESIAN_POINT ( 'NONE',  ( -1.360316468750072838, 1.661458333674769694, 0.7853790794158601596 ) ) ;
#205788=CARTESIAN_POINT ( 'NONE',  ( 1.360316468749953600, 0.4947916670081084489, 0.7853790794158861388 ) ) ;
#205812=CARTESIAN_POINT ( 'NONE',  ( 1.914442667406926812, 3.262253226108007720, -0.4355078757044270610 ) ) ;
#205827=EDGE_CURVE ( 'NONE', #23166, #137780, #6081, .T. ) ;
#205954=CARTESIAN_POINT ( 'NONE',  ( -0.3423093779010150106, 2.999999999999981792, -0.3423093779010167315 ) ) ;
#205985=CARTESIAN_POINT ( 'NONE',  ( 1.224999999999971223, 1.354166666666710483, 0.7072540797572898219 ) ) ;
#206001=LINE ( 'NONE', #71719, #57363 ) ;
#206008=CARTESIAN_POINT ( 'NONE',  ( -0.6801582343750368631, 2.130208333674714183, -1.178068619123862515 ) ) ;
#206033=( BOUNDED_CURVE ( )  B_SPLINE_CURVE ( 2, ( #58161, #91756, #6181, #157809, #9407, #175130, #138357, #75478, #10460 ),
 .UNSPECIFIED., .F., .F. ) 
 B_SPLINE_CURVE_WITH_KNOTS ( ( 3, 2, 2, 2, 3 ),
 ( 0.7031250000000002220, 0.7083333333333333703, 0.7187500000000000000, 0.7291666666666666297, 0.7343749999999997780 ),
 .UNSPECIFIED. ) 
 CURVE ( )  GEOMETRIC_REPRESENTATION_ITEM ( )  RATIONAL_B_SPLINE_CURVE ( ( 0.9330127018922194093, 0.9330127018922221849, 1.000000000000000000, 0.8660254037844387076, 1.000000000000000000, 0.8660254037844387076, 1.000000000000000000, 0.9330127018922221849, 0.9330127018922194093 ) ) 
 REPRESENTATION_ITEM ( '' )  );
#206087=CARTESIAN_POINT ( 'NONE',  ( 1.224999999999984768, 0.1875000006827803878, -5.377642775528101993E-14 ) ) ;
#206147=CARTESIAN_POINT ( 'NONE',  ( -0.3282377607281303233, 1.551335450315375786, 1.224999999999979217 ) ) ;
#206165=CARTESIAN_POINT ( 'NONE',  ( -0.4000000000000214495, 3.322650755865464767, 0.5865692111442306622 ) ) ;
#206184=ORIENTED_EDGE ( 'NONE', *, *, #8819, .T. ) ;
#206194=ORIENTED_EDGE ( 'NONE', *, *, #4984, .T. ) ;
#206250=CARTESIAN_POINT ( 'NONE',  ( 3.486133158594716510E-16, 2.312499999999992006, 1.224999999999971889 ) ) ;
#206303=CARTESIAN_POINT ( 'NONE',  ( 1.360316468749957597, 0.3177083336747154596, -0.7853790794158961308 ) ) ;
#206324=CARTESIAN_POINT ( 'NONE',  ( -1.225000000000052269, -0.4791666666666582475, 0.7072540797572637317 ) ) ;
#206335=CARTESIAN_POINT ( 'NONE',  ( -2.449742653233043743, 3.299999999999976730, -0.4000000000000339950 ) ) ;
#206529=CARTESIAN_POINT ( 'NONE',  ( 0.6125000000000019318, 2.666666666666678509, -1.060881119635941339 ) ) ;
#206617=ORIENTED_EDGE ( 'NONE', *, *, #51475, .T. ) ;
#206619=CARTESIAN_POINT ( 'NONE',  ( -1.953008978358306879E-14, 0.7031250003414774019, 1.570758158831782270 ) ) ;
#206690=CARTESIAN_POINT ( 'NONE',  ( -0.6125000000000019318, 2.291666666666664298, 1.060881119635910252 ) ) ;
#206691=EDGE_CURVE ( 'NONE', #213643, #62971, #128936, .T. ) ;
#206726=CARTESIAN_POINT ( 'NONE',  ( -3.755786496842899057E-14, 2.609375000341406459, -1.570758158831778273 ) ) ;
#206839=CARTESIAN_POINT ( 'NONE',  ( 0.3999999999999889200, 3.372708439410121439, -0.5000000000000368594 ) ) ;
#206845=CARTESIAN_POINT ( 'NONE',  ( -4.757329562667670667E-14, 0.5781250003414447614, -1.570758158831812246 ) ) ;
#206901=CARTESIAN_POINT ( 'NONE',  ( 0.2999999999999758415, 3.214163249644268472, 0.5238375172406799507 ) ) ;
#206951=VECTOR ( 'NONE', #122942, 1000.000000000000000 ) ;
#206991=DIRECTION ( 'NONE',  ( 5.828670879282089587E-16, -0.8656921114426509023, 0.5005768354468322912 ) ) ;
#207075=CARTESIAN_POINT ( 'NONE',  ( 0.6801582343749900117, 1.588541667008100511, -1.178068619123890270 ) ) ;
#207087=CARTESIAN_POINT ( 'NONE',  ( -1.394453263437886604E-15, 2.375000000682794266, 1.224999999999975220 ) ) ;
#207125=ORIENTED_EDGE ( 'NONE', *, *, #182709, .T. ) ;
#207137=ORIENTED_EDGE ( 'NONE', *, *, #77201, .T. ) ;
#207161=CARTESIAN_POINT ( 'NONE',  ( -1.752700365193352367E-14, 0.6250000006827908239, 1.414508159514579644 ) ) ;
#207187=EDGE_LOOP ( 'NONE', ( #184941, #35646, #179807, #88063 ) ) ;
#207266=CARTESIAN_POINT ( 'NONE',  ( 0.4499999960734538673, 4.000000000000008882, 0.9281957781481324776 ) ) ;
#207268=ORIENTED_EDGE ( 'NONE', *, *, #240, .F. ) ;
#207277=EDGE_CURVE ( 'NONE', #141384, #44750, #94540, .T. ) ;
#207292=ADVANCED_FACE ( 'NONE', ( #146165 ), #195962, .T. ) ;
#207377=CARTESIAN_POINT ( 'NONE',  ( 0.6801582343749935644, 0.2552083336747196229, 1.178068619123780802 ) ) ;
#207397=CARTESIAN_POINT ( 'NONE',  ( -0.6125000000000105915, 0.04166666666666901664, 1.060881119635925796 ) ) ;
#207439=CARTESIAN_POINT ( 'NONE',  ( -3.122502256758252770E-14, 3.499999999999961364, -3.816391647148975608E-14 ) ) ;
#207567=ORIENTED_EDGE ( 'NONE', *, *, #144969, .T. ) ;
#207600=AXIS2_PLACEMENT_3D ( 'NONE', #163718, #62999, #81387 ) ;
#207655=DIRECTION ( 'NONE',  ( -0.8583236685137344280, 0.5131086435338277907, 0.000000000000000000 ) ) ;
#207687=CARTESIAN_POINT ( 'NONE',  ( -0.6801582343750438575, -0.5677083329919535570, 1.178068619123803451 ) ) ;
#207695=CARTESIAN_POINT ( 'NONE',  ( -0.5000000000000091038, 3.949999999999960654, 0.3999999999999455103 ) ) ;
#207724=CARTESIAN_POINT ( 'NONE',  ( -1.907519672996887294, 3.236073672982363369, 0.4612874649729363785 ) ) ;
#207754=AXIS2_PLACEMENT_3D ( 'NONE', #29413, #110722, #95504 ) ;
#207828=CARTESIAN_POINT ( 'NONE',  ( 1.926045559616737846, 3.520657594693878956, 0.3999999999999681033 ) ) ;
#207829=CARTESIAN_POINT ( 'NONE',  ( 0.4999999999999952260, 3.172938907704321743, -0.4000000000000062395 ) ) ;
#207893=DIRECTION ( 'NONE',  ( -3.497202527569253358E-15, -0.000000000000000000, -1.000000000000000000 ) ) ;
#207910=CARTESIAN_POINT ( 'NONE',  ( 1.360316468749988683, 0.2656250003413990202, -1.387778780781445676E-14 ) ) ;
#207928=ORIENTED_EDGE ( 'NONE', *, *, #87277, .F. ) ;
#207956=CARTESIAN_POINT ( 'NONE',  ( 0.3282377607281112275, 2.323664549684620440, 1.224999999999963229 ) ) ;
#207984=DIRECTION ( 'NONE',  ( 0.000000000000000000, 0.000000000000000000, -1.000000000000000000 ) ) ;
#207987=DIRECTION ( 'NONE',  ( 1.000000000000000000, 0.000000000000000000, -5.421010862427519212E-16 ) ) ;
#208094=CARTESIAN_POINT ( 'NONE',  ( 0.4999999999999900080, 3.950000000000009059, -0.5000000000000160982 ) ) ;
#208138=CARTESIAN_POINT ( 'NONE',  ( -1.752700365193352367E-14, 1.609375000341425777, -1.570758158831794260 ) ) ;
#208177=( BOUNDED_CURVE ( )  B_SPLINE_CURVE ( 2, ( #74607, #125570, #61544, #140711, #173192, #60474, #43195, #109308, #123454, #108240, #127711, #175318, #90875, #110371, #189416, #206726, #11718, #26904, #76722, #24773, #93009, #193671, #10646, #142838, #41060, #208844, #58354, #77793, #190468, #94077, #174264, #45314, #160116, #143913, #214144, #149193, #128764, #179572, #83112, #65770, #768, #129832, #148142, #12773, #31191, #98316, #47452, #210973, #113567, #66834, #97264, #30115, #49554, #34367, #79917, #165438, #48510, #15965, #178505, #213104, #147082, #163319, #14900, #194738, #164381, #162255, #17035, #13841, #82049, #96205, #132977, #181674, #131918, #197928, #198979, #46375, #80994, #50624, #115680, #116750, #64736, #33301, #63678, #182749, #180622, #112494, #195815, #130879, #161187, #196873, #99386, #146027, #78847, #144967, #114630, #62601, #212036, #32245, #87407, #150277, #54901, #55970, #100441, #68985, #137236, #204313, #118893, #135103, #200060, #188087, #122123, #1847, #166512, #52759, #138298, #3980, #67906, #51712, #101510, #18104, #153471, #201117, #121054, #154540, #103661, #22369, #184878, #19180, #84190, #71120, #20244, #169710, #36503, #117831, #85255, #102582, #2912, #134052, #167581, #168642, #183822, #21300, #35434 ),
 .UNSPECIFIED., .F., .T. ) 
 B_SPLINE_CURVE_WITH_KNOTS ( ( 3, 2, 2, 2, 2, 2, 2, 2, 2, 2, 2, 2, 2, 2, 2, 2, 2, 2, 2, 2, 2, 2, 2, 2, 2, 2, 2, 2, 2, 2, 2, 2, 2, 2, 2, 2, 2, 2, 2, 2, 2, 2, 2, 2, 2, 2, 2, 2, 2, 2, 2, 2, 2, 2, 2, 2, 2, 2, 2, 2, 2, 2, 2, 2, 2, 2, 2, 2, 2, 2, 2, 3 ),
 ( 0.000000000000000000, 0.01041666666666666609, 0.02083333333333333218, 0.03125000000000000000, 0.04166666666666666435, 0.05208333333333333565, 0.06250000000000000000, 0.07291666666666667129, 0.08333333333333332871, 0.09375000000000000000, 0.1041666666666666713, 0.1145833333333333287, 0.1250000000000000000, 0.1354166666666666574, 0.1458333333333333426, 0.1562500000000000000, 0.1666666666666666574, 0.1770833333333333426, 0.1875000000000000000, 0.1979166666666666574, 0.2083333333333333426, 0.2187500000000000000, 0.2291666666666666574, 0.2395833333333333426, 0.2500000000000000000, 0.2604166666666666852, 0.2708333333333333148, 0.2812500000000000000, 0.2916666666666666852, 0.3020833333333333148, 0.3125000000000000000, 0.3229166666666666852, 0.3333333333333333148, 0.3437500000000000000, 0.3541666666666666852, 0.3645833333333333148, 0.3750000000000000000, 0.3854166666666666852, 0.3958333333333333148, 0.4062500000000000000, 0.4166666666666666852, 0.4270833333333333148, 0.4375000000000000000, 0.4479166666666666852, 0.4583333333333333148, 0.4687500000000000000, 0.4791666666666666852, 0.4895833333333333148, 0.5000000000000000000, 0.5104166666666666297, 0.5208333333333333703, 0.5312500000000000000, 0.5416666666666666297, 0.5520833333333333703, 0.5625000000000000000, 0.5729166666666666297, 0.5833333333333333703, 0.5937500000000000000, 0.6041666666666666297, 0.6145833333333333703, 0.6250000000000000000, 0.6354166666666666297, 0.6458333333333333703, 0.6562500000000000000, 0.6666666666666666297, 0.6770833333333333703, 0.6875000000000000000, 0.6979166666666666297, 0.7083333333333333703, 0.7187500000000000000, 0.7291666666666666297, 0.7305924012910729459 ),
 .UNSPECIFIED. ) 
 CURVE ( )  GEOMETRIC_REPRESENTATION_ITEM ( )  RATIONAL_B_SPLINE_CURVE ( ( 1.000000000000000000, 0.8660254037844387076, 1.000000000000000000, 0.8660254037844387076, 1.000000000000000000, 0.8660254037844387076, 1.000000000000000000, 0.8660254037844387076, 1.000000000000000000, 0.8660254037844387076, 1.000000000000000000, 0.8660254037844387076, 1.000000000000000000, 0.8660254037844387076, 1.000000000000000000, 0.8660254037844387076, 1.000000000000000000, 0.8660254037844387076, 1.000000000000000000, 0.8660254037844387076, 1.000000000000000000, 0.8660254037844387076, 1.000000000000000000, 0.8660254037844387076, 1.000000000000000000, 0.8660254037844387076, 1.000000000000000000, 0.8660254037844387076, 1.000000000000000000, 0.8660254037844387076, 1.000000000000000000, 0.8660254037844387076, 1.000000000000000000, 0.8660254037844387076, 1.000000000000000000, 0.8660254037844387076, 1.000000000000000000, 0.8660254037844387076, 1.000000000000000000, 0.8660254037844387076, 1.000000000000000000, 0.8660254037844387076, 1.000000000000000000, 0.8660254037844387076, 1.000000000000000000, 0.8660254037844387076, 1.000000000000000000, 0.8660254037844387076, 1.000000000000000000, 0.8660254037844387076, 1.000000000000000000, 0.8660254037844387076, 1.000000000000000000, 0.8660254037844387076, 1.000000000000000000, 0.8660254037844387076, 1.000000000000000000, 0.8660254037844387076, 1.000000000000000000, 0.8660254037844387076, 1.000000000000000000, 0.8660254037844387076, 1.000000000000000000, 0.8660254037844387076, 1.000000000000000000, 0.8660254037844387076, 1.000000000000000000, 0.8660254037844387076, 1.000000000000000000, 0.8660254037844387076, 1.000000000000000000, 0.8660254037844387076, 1.000000000000000000, 0.8660254037844387076, 1.000000000000000000, 0.8660254037844387076, 1.000000000000000000, 0.8660254037844387076, 1.000000000000000000, 0.8660254037844387076, 1.000000000000000000, 0.8660254037844387076, 1.000000000000000000, 0.8660254037844387076, 1.000000000000000000, 0.8660254037844387076, 1.000000000000000000, 0.8660254037844387076, 1.000000000000000000, 0.8660254037844387076, 1.000000000000000000, 0.8660254037844387076, 1.000000000000000000, 0.8660254037844387076, 1.000000000000000000, 0.8660254037844387076, 1.000000000000000000, 0.8660254037844387076, 1.000000000000000000, 0.8660254037844387076, 1.000000000000000000, 0.8660254037844387076, 1.000000000000000000, 0.8660254037844387076, 1.000000000000000000, 0.8660254037844387076, 1.000000000000000000, 0.8660254037844387076, 1.000000000000000000, 0.8660254037844387076, 1.000000000000000000, 0.8660254037844387076, 1.000000000000000000, 0.8660254037844387076, 1.000000000000000000, 0.8660254037844387076, 1.000000000000000000, 0.8660254037844387076, 1.000000000000000000, 0.8660254037844387076, 1.000000000000000000, 0.8660254037844387076, 1.000000000000000000, 0.8660254037844387076, 1.000000000000000000, 0.8660254037844387076, 1.000000000000000000, 0.8660254037844387076, 1.000000000000000000, 0.8660254037844387076, 1.000000000000000000, 0.8660254037844387076, 1.000000000000000000, 0.8660254037844387076, 1.000000000000000000, 0.8660254037844387076, 1.000000000000000000, 0.8660254037844387076, 1.000000000000000000, 0.8660254037844387076, 1.000000000000000000, 0.9816628268209235397, 0.9683452906431546658 ) ) 
 REPRESENTATION_ITEM ( '' )  );
#208217=CARTESIAN_POINT ( 'NONE',  ( -1.225000000000046052, 0.04166666734950023182, -0.7072540797573217963 ) ) ;
#208233=CARTESIAN_POINT ( 'NONE',  ( -0.4500000000000163869, 3.950000000000009059, -1.561251128379126385E-14 ) ) ;
#208265=EDGE_LOOP ( 'NONE', ( #19796, #200127, #103529, #207928, #95206 ) ) ;
#208300=ADVANCED_FACE ( 'NONE', ( #142329 ), #208341, .T. ) ;
#208324=ORIENTED_EDGE ( 'NONE', *, *, #68527, .F. ) ;
#208325=CARTESIAN_POINT ( 'NONE',  ( 0.2999999999999807265, 4.000000000000008882, 1.007084189318371514 ) ) ;
#208341=CYLINDRICAL_SURFACE ( 'NONE', #117016, 1.224999999999996980 ) ;
#208380=CARTESIAN_POINT ( 'NONE',  ( -4.415768667553307481E-15, 0.1250000006828069499, 1.224999999999963229 ) ) ;
#208428=CARTESIAN_POINT ( 'NONE',  ( -1.360316468750021768, 0.1718750003414371008, -3.295974604355933479E-14 ) ) ;
#208448=CARTESIAN_POINT ( 'NONE',  ( -0.6125000000000105915, -0.9583333333333110549, 1.060881119635910252 ) ) ;
#208577=ORIENTED_EDGE ( 'NONE', *, *, #29742, .T. ) ;
#208601=CARTESIAN_POINT ( 'NONE',  ( 0.4465194593917913846, 3.080450244942120719, -0.4155024747329958412 ) ) ;
#208627=CARTESIAN_POINT ( 'NONE',  ( 0.4170821662628897974, 3.033599471985628959, -0.4170821662629418114 ) ) ;
#208641=CYLINDRICAL_SURFACE ( 'NONE', #120458, 0.09999999999999999167 ) ;
#208674=( NAMED_UNIT ( * ) SI_UNIT ( $, .STERADIAN. ) SOLID_ANGLE_UNIT ( ) );
#208742=CARTESIAN_POINT ( 'NONE',  ( 1.360316468749964480, -0.2343749996585806072, -5.204170427930421283E-15 ) ) ;
#208844=CARTESIAN_POINT ( 'NONE',  ( -1.360316468750018659, 2.401041667008069425, -0.7853790794159061228 ) ) ;
#208885=ORIENTED_EDGE ( 'NONE', *, *, #139883, .F. ) ;
#208956=AXIS2_PLACEMENT_3D ( 'NONE', #183117, #34724, #84551 ) ;
#208967=CARTESIAN_POINT ( 'NONE',  ( 0.6801582343749917881, 0.7239583336747443809, 1.178068619123793015 ) ) ;
#208985=CARTESIAN_POINT ( 'NONE',  ( 1.360316468750000896, 2.515625000341401130, -3.469446951953614189E-15 ) ) ;
#208996=ORIENTED_EDGE ( 'NONE', *, *, #90038, .T. ) ;
#209073=EDGE_CURVE ( 'NONE', #73414, #52005, #3475, .T. ) ;
#209103=ORIENTED_EDGE ( 'NONE', *, *, #199193, .T. ) ;
#209172=ORIENTED_EDGE ( 'NONE', *, *, #149834, .T. ) ;
#209196=CARTESIAN_POINT ( 'NONE',  ( 1.360316468749951602, 2.526041667008117830, 0.7853790794158560518 ) ) ;
#209228=CARTESIAN_POINT ( 'NONE',  ( -1.360316468749997565, 2.890625000341401574, 1.734723475976807094E-15 ) ) ;
#209301=VECTOR ( 'NONE', #59127, 1000.000000000000114 ) ;
#209390=CARTESIAN_POINT ( 'NONE',  ( -1.510657702057710340E-15, 1.375000000682792267, 1.224999999999963229 ) ) ;
#209395=CARTESIAN_POINT ( 'NONE',  ( 0.4999999999999674705, 3.999999999999989786, 0.4499999999999625966 ) ) ;
#209424=DIRECTION ( 'NONE',  ( 1.276756478318932585E-15, -1.000000000000000000, 1.665334536937738262E-16 ) ) ;
#209490=CARTESIAN_POINT ( 'NONE',  ( -0.6801582343750438575, 0.7135416670080579893, 1.178068619123810334 ) ) ;
#209517=EDGE_CURVE ( 'NONE', #64456, #76056, #130794, .T. ) ;
#209533=CARTESIAN_POINT ( 'NONE',  ( -1.734723475976807094E-15, 2.999999999999988898, -6.938893903907228378E-15 ) ) ;
#209549=CARTESIAN_POINT ( 'NONE',  ( -0.3282377607281335985, 2.613835450998162280, 1.224999999999989431 ) ) ;
#209593=CARTESIAN_POINT ( 'NONE',  ( -1.734723475976807094E-15, 2.999999999999988898, -6.938893903907228378E-15 ) ) ;
#209606=CARTESIAN_POINT ( 'NONE',  ( -0.4041367621137820221, 3.038026290190013690, -0.4210133165200504179 ) ) ;
#209652=VERTEX_POINT ( 'NONE', #43502 ) ;
#209654=DIRECTION ( 'NONE',  ( -1.000000000000000000, 7.771561172376097755E-16, 4.440892098500627148E-16 ) ) ;
#209666=CARTESIAN_POINT ( 'NONE',  ( -3.097867176628829133E-14, 3.975067388631681187, -1.872309607372827811 ) ) ;
#209694=CARTESIAN_POINT ( 'NONE',  ( 0.3999999999999889200, 0.000000000000000000, -5.204170427930421283E-15 ) ) ;
#209807=CARTESIAN_POINT ( 'NONE',  ( -1.360316468750044860, -0.8385416663252739378, 0.7853790794158720390 ) ) ;
#209874=DIRECTION ( 'NONE',  ( -3.330669073875481947E-16, 4.742150360713068815E-16, 1.000000000000000000 ) ) ;
#209885=LINE ( 'NONE', #7424, #22543 ) ;
#209957=CARTESIAN_POINT ( 'NONE',  ( 1.902112725515536118, 3.289212146679096893, 0.4096023912811769252 ) ) ;
#210027=CARTESIAN_POINT ( 'NONE',  ( 1.253848497529134409, -2.775557561562891351E-14, 0.5275650105875644424 ) ) ;
#210033=CARTESIAN_POINT ( 'NONE',  ( -0.6801582343750247617, 0.09895833367471601472, -1.178068619123872729 ) ) ;
#210068=CARTESIAN_POINT ( 'NONE',  ( 1.902112725515556990, 3.289212146679096893, -0.4096023912812432055 ) ) ;
#210072=EDGE_LOOP ( 'NONE', ( #10862, #116876, #12659, #196616, #192763, #17976, #184285, #187785 ) ) ;
#210153=CARTESIAN_POINT ( 'NONE',  ( -1.931056844935879147, 3.481093093210128053, 0.3999999999999836464 ) ) ;
#210170=CYLINDRICAL_SURFACE ( 'NONE', #212866, 0.04999999999999991257 ) ;
#210192=VECTOR ( 'NONE', #192602, 1000.000000000000000 ) ;
#210228=DIRECTION ( 'NONE',  ( -1.276756478318932585E-15, 1.000000000000000000, -1.665334536937738262E-16 ) ) ;
#210270=CARTESIAN_POINT ( 'NONE',  ( 1.360316468749973140, 0.5468750003413819227, -2.081668171172168513E-14 ) ) ;
#210308=FACE_OUTER_BOUND ( 'NONE', #33754, .T. ) ;
#210310=CARTESIAN_POINT ( 'NONE',  ( 1.360316468749949825, 2.244791667008100511, 0.7853790794158780342 ) ) ;
#210348=EDGE_CURVE ( 'NONE', #47983, #77834, #175728, .T. ) ;
#210373=CARTESIAN_POINT ( 'NONE',  ( -1.734723475976807094E-15, 2.999999999999988898, -6.938893903907228378E-15 ) ) ;
#210385=CARTESIAN_POINT ( 'NONE',  ( 1.772826578343066117, 3.950000000000009059, 0.4499999999999590994 ) ) ;
#210394=ORIENTED_EDGE ( 'NONE', *, *, #37214, .T. ) ;
#210405=VERTEX_POINT ( 'NONE', #66082 ) ;
#210485=CARTESIAN_POINT ( 'NONE',  ( -1.225000000000033396, 2.062500000682796042, -2.949029909160572061E-14 ) ) ;
#210497=CIRCLE ( 'NONE', #58365, 0.05000000000000002359 ) ;
#210573=CARTESIAN_POINT ( 'NONE',  ( -1.360316468750066843, -0.09895833299191045263, -0.7853790794159082322 ) ) ;
#210592=CARTESIAN_POINT ( 'NONE',  ( 0.4254946254920577431, 3.044090126848993716, 0.4192457809173404382 ) ) ;
#210640=DIRECTION ( 'NONE',  ( -1.276756478318932585E-15, 1.000000000000000000, -1.665334536937738262E-16 ) ) ;
#210785=CARTESIAN_POINT ( 'NONE',  ( 0.3423093779009716564, 3.099999999999991651, 0.3999999999999646061 ) ) ;
#210825=CARTESIAN_POINT ( 'NONE',  ( 1.360316468749975582, 2.776041667008103175, 0.7853790794158820310 ) ) ;
#210829=CARTESIAN_POINT ( 'NONE',  ( -1.734723475976807094E-15, 2.999999999999988898, -6.938893903907228378E-15 ) ) ;
#210878=ORIENTED_EDGE ( 'NONE', *, *, #123768, .F. ) ;
#210879=CARTESIAN_POINT ( 'NONE',  ( 0.6801582343749692505, -0.5260416663252707181, 1.178068619123786132 ) ) ;
#210881=CARTESIAN_POINT ( 'NONE',  ( -1.007805743535968412, -8.868899487089072003E-15, 0.8044584510992147663 ) ) ;
#210933=STYLED_ITEM ( 'NONE', ( #12611 ), #156107 ) ;
#210939=ORIENTED_EDGE ( 'NONE', *, *, #68743, .T. ) ;
#210973=CARTESIAN_POINT ( 'NONE',  ( -1.360316468750048857, 1.942708333674827426, 0.7853790794158581612 ) ) ;
#210991=CARTESIAN_POINT ( 'NONE',  ( -0.4465194593918104249, 3.080450244942127380, 0.4155024747329021939 ) ) ;
#210997=DIRECTION ( 'NONE',  ( -1.276756478318932191E-15, 1.000000000000000000, -3.330669073875483426E-16 ) ) ;
#210998=FACE_OUTER_BOUND ( 'NONE', #78955, .T. ) ;
#211024=CARTESIAN_POINT ( 'NONE',  ( 0.2999999999999686806, 3.975028841772344723, -0.9637995837462834947 ) ) ;
#211102=CARTESIAN_POINT ( 'NONE',  ( -0.6801582343750420812, -0.06770833299193229626, 1.178068619123801675 ) ) ;
#211109=FACE_OUTER_BOUND ( 'NONE', #164926, .T. ) ;
#211124=CARTESIAN_POINT ( 'NONE',  ( -3.505400730386704341E-15, 2.703125000341406459, 1.570758158831794260 ) ) ;
#211148=EDGE_CURVE ( 'NONE', #72069, #184329, #145361, .T. ) ;
#211317=DIRECTION ( 'NONE',  ( 1.084202172485501673E-15, -1.000000000000000000, 4.336808689942006692E-15 ) ) ;
#211334=CIRCLE ( 'NONE', #24558, 0.05000000000000002359 ) ;
#211337=CARTESIAN_POINT ( 'NONE',  ( -1.360316468749995789, 0.9218750003414100114, -6.938893903907228378E-15 ) ) ;
#211373=CARTESIAN_POINT ( 'NONE',  ( -0.3423093779010132898, 2.999999999999995559, 0.3423093779010045745 ) ) ;
#211375=CARTESIAN_POINT ( 'NONE',  ( 0.6801582343749761339, 1.973958333674710630, 1.178068619123801675 ) ) ;
#211411=ORIENTED_EDGE ( 'NONE', *, *, #201770, .T. ) ;
#211435=CARTESIAN_POINT ( 'NONE',  ( 0.4499999999999677591, 3.999999999999961808, -0.8338124244296144516 ) ) ;
#211440=DIRECTION ( 'NONE',  ( 9.436895709313856232E-16, -0.8656921114426507913, -0.5005768354468325132 ) ) ;
#211475=ORIENTED_EDGE ( 'NONE', *, *, #191370, .T. ) ;
#211513=CYLINDRICAL_SURFACE ( 'NONE', #97323, 0.09999999999999971412 ) ;
#211576=CARTESIAN_POINT ( 'NONE',  ( 1.743066579297358008E-15, 0.7500000006828128063, -1.225000000000021849 ) ) ;
#211579=CARTESIAN_POINT ( 'NONE',  ( -0.3282377514116611716, 0.01116455005054403302, -1.225000005378890977 ) ) ;
#211630=CARTESIAN_POINT ( 'NONE',  ( -1.360316468750042862, -0.5572916663252566183, 0.7853790794158701516 ) ) ;
#211691=VERTEX_POINT ( 'NONE', #31236 ) ;
#211724=ADVANCED_FACE ( 'NONE', ( #110416 ), #129878, .F. ) ;
#211765=DIRECTION ( 'NONE',  ( -1.000000000000000000, 0.000000000000000000, 0.000000000000000000 ) ) ;
#211779=CARTESIAN_POINT ( 'NONE',  ( -0.5000000000000143219, 3.949999999999981526, 0.4999999999999553690 ) ) ;
#211791=VERTEX_POINT ( 'NONE', #70094 ) ;
#211841=CARTESIAN_POINT ( 'NONE',  ( 1.224999999999976996, 1.666666667349515851, 0.7072540797572517413 ) ) ;
#211942=CARTESIAN_POINT ( 'NONE',  ( 1.224999999999974332, 2.687500000682768508, -4.163336342344337027E-14 ) ) ;
#211971=DIRECTION ( 'NONE',  ( -0.8656921114426504582, -0.5005768354468328463, 3.719247132494280721E-15 ) ) ;
#212036=CARTESIAN_POINT ( 'NONE',  ( -1.360316468749995789, 0.9218750003414100114, -6.938893903907228378E-15 ) ) ;
#212087=CARTESIAN_POINT ( 'NONE',  ( 1.908029163539569417, 3.237038651130959455, 0.4603255239806047228 ) ) ;
#212155=EDGE_CURVE ( 'NONE', #149263, #67541, #77608, .T. ) ;
#212165=EDGE_CURVE ( 'NONE', #6089, #108115, #84236, .T. ) ;
#212167=CARTESIAN_POINT ( 'NONE',  ( -1.360316468750009555, -0.1093749996585596795, -2.081668171172168513E-14 ) ) ;
#212180=CARTESIAN_POINT ( 'NONE',  ( -1.734723475976807094E-15, 2.999999999999988898, -6.938893903907228378E-15 ) ) ;
#212188=CARTESIAN_POINT ( 'NONE',  ( 0.6801582343749987825, 2.557291667008069869, -1.178068619123886718 ) ) ;
#212285=CARTESIAN_POINT ( 'NONE',  ( -1.919771823249095455, 3.227545531266399870, 0.3999999999999835909 ) ) ;
#212331=ADVANCED_FACE ( 'NONE', ( #169756 ), #73310, .F. ) ;
#212351=CARTESIAN_POINT ( 'NONE',  ( 0.3544712801348727238, 3.975028838742718840, -0.9637995819944527032 ) ) ;
#212395=CARTESIAN_POINT ( 'NONE',  ( 1.360316468749980023, 0.7968750003414099004, -3.122502256758252770E-14 ) ) ;
#212397=( BOUNDED_CURVE ( )  B_SPLINE_CURVE ( 2, ( #180283, #96924, #145692, #44967, #97983, #165090, #197577, #162974, #64395 ),
 .UNSPECIFIED., .F., .T. ) 
 B_SPLINE_CURVE_WITH_KNOTS ( ( 3, 2, 2, 2, 3 ),
 ( 0.6093749999999997780, 0.6145833333333333703, 0.6250000000000000000, 0.6354166666666666297, 0.6406250000000002220 ),
 .UNSPECIFIED. ) 
 CURVE ( )  GEOMETRIC_REPRESENTATION_ITEM ( )  RATIONAL_B_SPLINE_CURVE ( ( 0.9330127018922194093, 0.9330127018922165227, 1.000000000000000000, 0.8660254037844387076, 1.000000000000000000, 0.8660254037844387076, 1.000000000000000000, 0.9330127018922165227, 0.9330127018922194093 ) ) 
 REPRESENTATION_ITEM ( '' )  );
#212436=CARTESIAN_POINT ( 'NONE',  ( -2.353626204688216217E-14, 2.828125000341407347, -1.570758158831798257 ) ) ;
#212450=VERTEX_POINT ( 'NONE', #56015 ) ;
#212497=ORIENTED_EDGE ( 'NONE', *, *, #34131, .F. ) ;
#212506=FACE_OUTER_BOUND ( 'NONE', #144462, .T. ) ;
#212545=ORIENTED_EDGE ( 'NONE', *, *, #37910, .T. ) ;
#212583=FACE_OUTER_BOUND ( 'NONE', #75580, .T. ) ;
#212615=CARTESIAN_POINT ( 'NONE',  ( -1.225000000000035172, 1.562500000682809365, -4.510281037539698445E-14 ) ) ;
#212628=DIRECTION ( 'NONE',  ( -1.276756478318932585E-15, 1.000000000000000000, -1.665334536937738262E-16 ) ) ;
#212685=ADVANCED_FACE ( 'NONE', ( #110167 ), #143712, .T. ) ;
#212698=CARTESIAN_POINT ( 'NONE',  ( -1.360316468750006225, 2.640625000341401130, 3.469446951953614189E-15 ) ) ;
#212859=EDGE_CURVE ( 'NONE', #138011, #30458, #96418, .T. ) ;
#212866=AXIS2_PLACEMENT_3D ( 'NONE', #51960, #119143, #53009 ) ;
#213002=ORIENTED_EDGE ( 'NONE', *, *, #197493, .T. ) ;
#213003=CARTESIAN_POINT ( 'NONE',  ( -4.557020949502716471E-14, 1.625000000682779611, 1.414508159514571428 ) ) ;
#213065=EDGE_LOOP ( 'NONE', ( #14096, #159604, #193739, #156379 ) ) ;
#213104=CARTESIAN_POINT ( 'NONE',  ( -1.360316468750028651, 1.692708333674762144, 0.7853790794158620470 ) ) ;
#213116=DIRECTION ( 'NONE',  ( 3.330669073875478989E-16, -3.540251991789410786E-16, -1.000000000000000000 ) ) ;
#213135=EDGE_LOOP ( 'NONE', ( #35051, #136850, #7664, #28139 ) ) ;
#213188=CARTESIAN_POINT ( 'NONE',  ( -0.4500000000000163869, 3.949999999999995293, -0.5000000000000229816 ) ) ;
#213232=CARTESIAN_POINT ( 'NONE',  ( 1.360316468749994012, -0.9843749996586090845, -5.204170427930421283E-15 ) ) ;
#213393=CARTESIAN_POINT ( 'NONE',  ( -1.394453263437886604E-15, 2.375000000682794266, 1.224999999999975220 ) ) ;
#213433=CARTESIAN_POINT ( 'NONE',  ( 0.6124999999999914957, 1.333333333333339255, 1.060881119635932679 ) ) ;
#213454=CARTESIAN_POINT ( 'NONE',  ( -1.360316468749996677, 0.4010416670080598767, -0.7853790794158941324 ) ) ;
#213486=AXIS2_PLACEMENT_3D ( 'NONE', #192934, #194004, #211317 ) ;
#213493=CARTESIAN_POINT ( 'NONE',  ( 1.360316468750001784, 2.286458333674732835, -0.7853790794158941324 ) ) ;
#213515=CARTESIAN_POINT ( 'NONE',  ( 7.320879633048903241E-15, 0.3750000006828252408, 1.224999999999981659 ) ) ;
#213614=ORIENTED_EDGE ( 'NONE', *, *, #150248, .F. ) ;
#213629=CARTESIAN_POINT ( 'NONE',  ( -3.245517230425579371E-14, 3.975067388631681187, 1.872309607372774520 ) ) ;
#213643=VERTEX_POINT ( 'NONE', #188942 ) ;
#213662=CARTESIAN_POINT ( 'NONE',  ( 2.672702088255949078E-15, 1.625000000682787160, 1.224999999999980549 ) ) ;
#213744=CARTESIAN_POINT ( 'NONE',  ( -0.6801582343750229853, -0.8697916663252605041, -1.178068619123862515 ) ) ;
#213886=EDGE_CURVE ( 'NONE', #89507, #62493, #24011, .T. ) ;
#213916=CARTESIAN_POINT ( 'NONE',  ( 2.324088772396477673E-16, 0.6875000000000069944, -1.225000000000008749 ) ) ;
#213992=CARTESIAN_POINT ( 'NONE',  ( -1.360316468750058627, 2.692708333674814991, 0.7853790794158641564 ) ) ;
#214046=CARTESIAN_POINT ( 'NONE',  ( 0.3999999999999442335, 3.248764396332271875, 0.4641653677812440093 ) ) ;
#214057=CARTESIAN_POINT ( 'NONE',  ( 0.3282377607281103393, 2.136164550367433357, 1.224999999999969225 ) ) ;
#214074=PLANE ( 'NONE',  #76812 ) ;
#214106=VECTOR ( 'NONE', #135842, 1000.000000000000000 ) ;
#214144=CARTESIAN_POINT ( 'NONE',  ( -0.6801582343750125492, 2.213541667008059211, 1.178068619123818994 ) ) ;
#214189=CARTESIAN_POINT ( 'NONE',  ( 1.224999999999984990, 1.104166666666725360, 0.7072540797572737237 ) ) ;
#214194=CARTESIAN_POINT ( 'NONE',  ( 1.907519672996849103, 3.236073672982398008, 0.4612874649729346022 ) ) ;
#214253=CARTESIAN_POINT ( 'NONE',  ( 3.602337597214539753E-15, 1.000000000682806034, -1.225000000000015410 ) ) ;
#214269=CARTESIAN_POINT ( 'NONE',  ( 1.360316468749977581, -0.2135416663252950598, -0.7853790794159261068 ) ) ;
#214290=CARTESIAN_POINT ( 'NONE',  ( 0.6801582343749865700, 1.307291667008089853, -1.178068619123883165 ) ) ;
#214363=DIRECTION ( 'NONE',  ( 1.276756478318932585E-15, -1.000000000000000000, 1.665334536937738262E-16 ) ) ;
#214379=EDGE_CURVE ( 'NONE', #28319, #42265, #107116, .T. ) ;
#214381=CARTESIAN_POINT ( 'NONE',  ( -1.886017674307070457, 3.298060805577415877, -0.4014564593431291795 ) ) ;
ENDSEC;
END-ISO-10303-21;
